ISO-10303-21;
HEADER;
/* Generated by software containing ST-Developer
 * from STEP Tools, Inc. (www.steptools.com) 
 */
/* OPTION: using custom renumber hook */

FILE_DESCRIPTION(
/* description */ ('STEP AP242 Edition 2', 'CAx-IF Rec.Pracs.---Representation and Presentation of Product Manufa
cturing Information (PMI)---4.0---2014-10-13', 'CAx-IF Rec.Pracs.---3D Tessellated Geometry---0.4---2014-09-14', '2;1', 'CAx-IF Rec.Pracs.---User Defined Attributes---1.5---2016-08-15'),
/* implementation_level */ '2;1');

FILE_NAME(
/* name */ 'Bottle_Cap.step',
/* time_stamp */ '2026-10-08T12:15:07Z',
/* author */ (''),
/* organization */ (''),
/* preprocessor_version */ 'ST-DEVELOPER v20',
/* originating_system */ 'ONSHAPE BY PTC INC, 1.221',
/* authorisation */ '  ');

FILE_SCHEMA (('AP242_MANAGED_MODEL_BASED_3D_ENGINEERING_MIM_LF { 1 0 10303 442 3 1 4 }'));
ENDSEC;

DATA;
#18=SPHERICAL_SURFACE('',#15260,0.00100018366552404);
#19=SPHERICAL_SURFACE('',#15261,0.00100013782554506);
#20=SPHERICAL_SURFACE('',#15265,0.00100018686855117);
#56=B_SPLINE_SURFACE_WITH_KNOTS('',3,3,((#42010,#42011,#42012,#42013,#42014,
#42015),(#42016,#42017,#42018,#42019,#42020,#42021),(#42022,#42023,#42024,
#42025,#42026,#42027),(#42028,#42029,#42030,#42031,#42032,#42033),(#42034,
#42035,#42036,#42037,#42038,#42039),(#42040,#42041,#42042,#42043,#42044,
#42045),(#42046,#42047,#42048,#42049,#42050,#42051),(#42052,#42053,#42054,
#42055,#42056,#42057),(#42058,#42059,#42060,#42061,#42062,#42063),(#42064,
#42065,#42066,#42067,#42068,#42069)),.UNSPECIFIED.,.F.,.F.,.F.,(4,2,2,2,
4),(4,2,4),(0.000203480753469605,0.000266460935110171,0.000329441116750738,
0.000392421298391305,0.000455401480031871),(0.,0.503069799613008,1.00613959922602),
 .UNSPECIFIED.);
#57=B_SPLINE_SURFACE_WITH_KNOTS('',3,3,((#42215,#42216,#42217,#42218,#42219,
#42220),(#42221,#42222,#42223,#42224,#42225,#42226),(#42227,#42228,#42229,
#42230,#42231,#42232),(#42233,#42234,#42235,#42236,#42237,#42238),(#42239,
#42240,#42241,#42242,#42243,#42244),(#42245,#42246,#42247,#42248,#42249,
#42250)),.UNSPECIFIED.,.F.,.F.,.F.,(4,2,4),(4,2,4),(0.000210081613475223,
0.000328789525150644,0.000447497436826065),(-0.000133121398971735,0.499933439300514,
1.),.UNSPECIFIED.);
#58=B_SPLINE_SURFACE_WITH_KNOTS('',3,3,((#42325,#42326,#42327,#42328),(#42329,
#42330,#42331,#42332),(#42333,#42334,#42335,#42336),(#42337,#42338,#42339,
#42340),(#42341,#42342,#42343,#42344),(#42345,#42346,#42347,#42348),(#42349,
#42350,#42351,#42352),(#42353,#42354,#42355,#42356),(#42357,#42358,#42359,
#42360),(#42361,#42362,#42363,#42364),(#42365,#42366,#42367,#42368),(#42369,
#42370,#42371,#42372),(#42373,#42374,#42375,#42376),(#42377,#42378,#42379,
#42380),(#42381,#42382,#42383,#42384),(#42385,#42386,#42387,#42388),(#42389,
#42390,#42391,#42392),(#42393,#42394,#42395,#42396),(#42397,#42398,#42399,
#42400),(#42401,#42402,#42403,#42404),(#42405,#42406,#42407,#42408),(#42409,
#42410,#42411,#42412),(#42413,#42414,#42415,#42416),(#42417,#42418,#42419,
#42420),(#42421,#42422,#42423,#42424),(#42425,#42426,#42427,#42428),(#42429,
#42430,#42431,#42432),(#42433,#42434,#42435,#42436),(#42437,#42438,#42439,
#42440),(#42441,#42442,#42443,#42444),(#42445,#42446,#42447,#42448),(#42449,
#42450,#42451,#42452),(#42453,#42454,#42455,#42456),(#42457,#42458,#42459,
#42460),(#42461,#42462,#42463,#42464),(#42465,#42466,#42467,#42468),(#42469,
#42470,#42471,#42472),(#42473,#42474,#42475,#42476),(#42477,#42478,#42479,
#42480),(#42481,#42482,#42483,#42484),(#42485,#42486,#42487,#42488),(#42489,
#42490,#42491,#42492),(#42493,#42494,#42495,#42496),(#42497,#42498,#42499,
#42500),(#42501,#42502,#42503,#42504),(#42505,#42506,#42507,#42508),(#42509,
#42510,#42511,#42512),(#42513,#42514,#42515,#42516),(#42517,#42518,#42519,
#42520),(#42521,#42522,#42523,#42524),(#42525,#42526,#42527,#42528),(#42529,
#42530,#42531,#42532),(#42533,#42534,#42535,#42536),(#42537,#42538,#42539,
#42540),(#42541,#42542,#42543,#42544),(#42545,#42546,#42547,#42548),(#42549,
#42550,#42551,#42552),(#42553,#42554,#42555,#42556),(#42557,#42558,#42559,
#42560),(#42561,#42562,#42563,#42564),(#42565,#42566,#42567,#42568),(#42569,
#42570,#42571,#42572),(#42573,#42574,#42575,#42576),(#42577,#42578,#42579,
#42580),(#42581,#42582,#42583,#42584),(#42585,#42586,#42587,#42588),(#42589,
#42590,#42591,#42592),(#42593,#42594,#42595,#42596),(#42597,#42598,#42599,
#42600),(#42601,#42602,#42603,#42604),(#42605,#42606,#42607,#42608),(#42609,
#42610,#42611,#42612),(#42613,#42614,#42615,#42616),(#42617,#42618,#42619,
#42620),(#42621,#42622,#42623,#42624),(#42625,#42626,#42627,#42628),(#42629,
#42630,#42631,#42632),(#42633,#42634,#42635,#42636),(#42637,#42638,#42639,
#42640),(#42641,#42642,#42643,#42644),(#42645,#42646,#42647,#42648),(#42649,
#42650,#42651,#42652),(#42653,#42654,#42655,#42656),(#42657,#42658,#42659,
#42660),(#42661,#42662,#42663,#42664),(#42665,#42666,#42667,#42668),(#42669,
#42670,#42671,#42672),(#42673,#42674,#42675,#42676),(#42677,#42678,#42679,
#42680),(#42681,#42682,#42683,#42684),(#42685,#42686,#42687,#42688),(#42689,
#42690,#42691,#42692),(#42693,#42694,#42695,#42696),(#42697,#42698,#42699,
#42700),(#42701,#42702,#42703,#42704),(#42705,#42706,#42707,#42708),(#42709,
#42710,#42711,#42712),(#42713,#42714,#42715,#42716),(#42717,#42718,#42719,
#42720),(#42721,#42722,#42723,#42724),(#42725,#42726,#42727,#42728),(#42729,
#42730,#42731,#42732),(#42733,#42734,#42735,#42736),(#42737,#42738,#42739,
#42740),(#42741,#42742,#42743,#42744),(#42745,#42746,#42747,#42748),(#42749,
#42750,#42751,#42752),(#42753,#42754,#42755,#42756),(#42757,#42758,#42759,
#42760),(#42761,#42762,#42763,#42764),(#42765,#42766,#42767,#42768),(#42769,
#42770,#42771,#42772),(#42773,#42774,#42775,#42776),(#42777,#42778,#42779,
#42780),(#42781,#42782,#42783,#42784),(#42785,#42786,#42787,#42788),(#42789,
#42790,#42791,#42792),(#42793,#42794,#42795,#42796),(#42797,#42798,#42799,
#42800),(#42801,#42802,#42803,#42804),(#42805,#42806,#42807,#42808),(#42809,
#42810,#42811,#42812),(#42813,#42814,#42815,#42816),(#42817,#42818,#42819,
#42820),(#42821,#42822,#42823,#42824),(#42825,#42826,#42827,#42828),(#42829,
#42830,#42831,#42832),(#42833,#42834,#42835,#42836),(#42837,#42838,#42839,
#42840),(#42841,#42842,#42843,#42844),(#42845,#42846,#42847,#42848),(#42849,
#42850,#42851,#42852)),.UNSPECIFIED.,.F.,.F.,.F.,(4,2,2,2,2,2,2,2,2,2,2,
2,2,2,2,2,2,2,2,2,2,2,2,2,2,2,2,2,2,2,2,2,2,2,2,2,2,2,2,2,2,2,2,2,2,2,2,
2,2,2,2,2,2,2,2,2,2,2,2,2,2,2,2,2,2,4),(4,4),(0.202786906914899,0.208519922794762,
0.214252938674625,0.219985954554488,0.225718970434351,0.231451986314214,
0.237185002194077,0.24291801807394,0.248651033953804,0.254384049833667,
0.26011706571353,0.265850081593393,0.271583097473256,0.277316113353119,
0.283049129232982,0.288782145112846,0.294515160992709,0.300248176872572,
0.305981192752435,0.311714208632298,0.317447224512161,0.323180240392024,
0.328913256271887,0.334646272151751,0.340379288031614,0.346112303911477,
0.35184531979134,0.357578335671203,0.363311351551066,0.369044367430929,
0.374777383310793,0.380510399190656,0.386243415070519,0.391976430950382,
0.397709446830245,0.403442462710108,0.409175478589971,0.414908494469834,
0.420641510349698,0.426374526229561,0.432107542109424,0.437840557989287,
0.44357357386915,0.449306589749013,0.455039605628876,0.460772621508739,
0.466505637388603,0.472238653268466,0.477971669148329,0.483704685028192,
0.489437700908055,0.495170716787918,0.500903732667781,0.506636748547645,
0.512369764427508,0.518102780307371,0.523835796187234,0.529568812067097,
0.53530182794696,0.541034843826823,0.546767859706687,0.55250087558655,0.558233891466413,
0.563966907346276,0.566833415286207,0.569699923226139),(0.,1.00016823335214),
 .UNSPECIFIED.);
#59=B_SPLINE_SURFACE_WITH_KNOTS('',3,3,((#43571,#43572,#43573,#43574),(#43575,
#43576,#43577,#43578),(#43579,#43580,#43581,#43582),(#43583,#43584,#43585,
#43586),(#43587,#43588,#43589,#43590),(#43591,#43592,#43593,#43594),(#43595,
#43596,#43597,#43598),(#43599,#43600,#43601,#43602),(#43603,#43604,#43605,
#43606),(#43607,#43608,#43609,#43610),(#43611,#43612,#43613,#43614),(#43615,
#43616,#43617,#43618),(#43619,#43620,#43621,#43622),(#43623,#43624,#43625,
#43626),(#43627,#43628,#43629,#43630),(#43631,#43632,#43633,#43634),(#43635,
#43636,#43637,#43638),(#43639,#43640,#43641,#43642),(#43643,#43644,#43645,
#43646),(#43647,#43648,#43649,#43650),(#43651,#43652,#43653,#43654),(#43655,
#43656,#43657,#43658),(#43659,#43660,#43661,#43662),(#43663,#43664,#43665,
#43666),(#43667,#43668,#43669,#43670),(#43671,#43672,#43673,#43674),(#43675,
#43676,#43677,#43678),(#43679,#43680,#43681,#43682),(#43683,#43684,#43685,
#43686),(#43687,#43688,#43689,#43690),(#43691,#43692,#43693,#43694),(#43695,
#43696,#43697,#43698),(#43699,#43700,#43701,#43702),(#43703,#43704,#43705,
#43706),(#43707,#43708,#43709,#43710),(#43711,#43712,#43713,#43714),(#43715,
#43716,#43717,#43718),(#43719,#43720,#43721,#43722),(#43723,#43724,#43725,
#43726),(#43727,#43728,#43729,#43730),(#43731,#43732,#43733,#43734),(#43735,
#43736,#43737,#43738),(#43739,#43740,#43741,#43742),(#43743,#43744,#43745,
#43746),(#43747,#43748,#43749,#43750),(#43751,#43752,#43753,#43754),(#43755,
#43756,#43757,#43758),(#43759,#43760,#43761,#43762),(#43763,#43764,#43765,
#43766),(#43767,#43768,#43769,#43770),(#43771,#43772,#43773,#43774),(#43775,
#43776,#43777,#43778),(#43779,#43780,#43781,#43782),(#43783,#43784,#43785,
#43786),(#43787,#43788,#43789,#43790),(#43791,#43792,#43793,#43794),(#43795,
#43796,#43797,#43798),(#43799,#43800,#43801,#43802),(#43803,#43804,#43805,
#43806),(#43807,#43808,#43809,#43810),(#43811,#43812,#43813,#43814),(#43815,
#43816,#43817,#43818),(#43819,#43820,#43821,#43822),(#43823,#43824,#43825,
#43826),(#43827,#43828,#43829,#43830),(#43831,#43832,#43833,#43834),(#43835,
#43836,#43837,#43838),(#43839,#43840,#43841,#43842),(#43843,#43844,#43845,
#43846),(#43847,#43848,#43849,#43850),(#43851,#43852,#43853,#43854),(#43855,
#43856,#43857,#43858),(#43859,#43860,#43861,#43862),(#43863,#43864,#43865,
#43866),(#43867,#43868,#43869,#43870),(#43871,#43872,#43873,#43874),(#43875,
#43876,#43877,#43878),(#43879,#43880,#43881,#43882),(#43883,#43884,#43885,
#43886),(#43887,#43888,#43889,#43890),(#43891,#43892,#43893,#43894),(#43895,
#43896,#43897,#43898),(#43899,#43900,#43901,#43902),(#43903,#43904,#43905,
#43906),(#43907,#43908,#43909,#43910),(#43911,#43912,#43913,#43914),(#43915,
#43916,#43917,#43918),(#43919,#43920,#43921,#43922),(#43923,#43924,#43925,
#43926),(#43927,#43928,#43929,#43930),(#43931,#43932,#43933,#43934),(#43935,
#43936,#43937,#43938),(#43939,#43940,#43941,#43942),(#43943,#43944,#43945,
#43946),(#43947,#43948,#43949,#43950),(#43951,#43952,#43953,#43954),(#43955,
#43956,#43957,#43958),(#43959,#43960,#43961,#43962),(#43963,#43964,#43965,
#43966),(#43967,#43968,#43969,#43970),(#43971,#43972,#43973,#43974),(#43975,
#43976,#43977,#43978),(#43979,#43980,#43981,#43982),(#43983,#43984,#43985,
#43986),(#43987,#43988,#43989,#43990),(#43991,#43992,#43993,#43994),(#43995,
#43996,#43997,#43998),(#43999,#44000,#44001,#44002),(#44003,#44004,#44005,
#44006),(#44007,#44008,#44009,#44010),(#44011,#44012,#44013,#44014),(#44015,
#44016,#44017,#44018),(#44019,#44020,#44021,#44022),(#44023,#44024,#44025,
#44026),(#44027,#44028,#44029,#44030),(#44031,#44032,#44033,#44034),(#44035,
#44036,#44037,#44038),(#44039,#44040,#44041,#44042),(#44043,#44044,#44045,
#44046),(#44047,#44048,#44049,#44050),(#44051,#44052,#44053,#44054),(#44055,
#44056,#44057,#44058),(#44059,#44060,#44061,#44062),(#44063,#44064,#44065,
#44066),(#44067,#44068,#44069,#44070),(#44071,#44072,#44073,#44074),(#44075,
#44076,#44077,#44078),(#44079,#44080,#44081,#44082),(#44083,#44084,#44085,
#44086),(#44087,#44088,#44089,#44090),(#44091,#44092,#44093,#44094),(#44095,
#44096,#44097,#44098)),.UNSPECIFIED.,.F.,.F.,.F.,(4,2,2,2,2,2,2,2,2,2,2,
2,2,2,2,2,2,2,2,2,2,2,2,2,2,2,2,2,2,2,2,2,2,2,2,2,2,2,2,2,2,2,2,2,2,2,2,
2,2,2,2,2,2,2,2,2,2,2,2,2,2,2,2,2,2,4),(4,4),(0.202786898606437,0.208519914194954,
0.214252929783471,0.219985945371988,0.225718960960504,0.231451976549021,
0.237184992137538,0.242918007726055,0.248651023314571,0.254384038903088,
0.260117054491605,0.265850070080122,0.271583085668638,0.277316101257155,
0.283049116845672,0.288782132434189,0.294515148022705,0.300248163611222,
0.305981179199739,0.311714194788256,0.317447210376772,0.323180225965289,
0.328913241553806,0.334646257142323,0.340379272730839,0.346112288319356,
0.351845303907873,0.35757831949639,0.363311335084906,0.369044350673423,
0.37477736626194,0.380510381850457,0.386243397438973,0.39197641302749,0.397709428616007,
0.403442444204524,0.40917545979304,0.414908475381557,0.420641490970074,
0.42637450655859,0.432107522147107,0.437840537735624,0.443573553324141,
0.449306568912657,0.455039584501174,0.460772600089691,0.466505615678208,
0.472238631266724,0.477971646855241,0.483704662443758,0.489437678032275,
0.495170693620791,0.500903709209308,0.506636724797825,0.512369740386342,
0.518102755974858,0.523835771563375,0.529568787151892,0.535301802740409,
0.541034818328925,0.546767833917442,0.552500849505959,0.558233865094476,
0.563966880682992,0.566833388477251,0.569699896271509),(0.,1.00014725118256),
 .UNSPECIFIED.);
#60=COLOUR_RGB('', 0.66274510, 0.83137255, 0.94901961);
#226=SHAPE_REPRESENTATION_RELATIONSHIP('','',#13800,#253);
#253=ADVANCED_BREP_SHAPE_REPRESENTATION('',(#13744),#45490);
#332=TOROIDAL_SURFACE('',#15285,0.0194,0.0002);
#333=TOROIDAL_SURFACE('',#15286,0.019,0.0002);
#334=TOROIDAL_SURFACE('',#15287,0.0130000000000245,0.001);
#335=TOROIDAL_SURFACE('',#15288,0.0192,0.002);
#1046=CIRCLE('',#15259,0.000999999999685245);
#1047=CIRCLE('',#15262,0.0009999999999995);
#1048=CIRCLE('',#15263,0.000999999999471396);
#1049=CIRCLE('',#15266,0.000999999999690151);
#1050=CIRCLE('',#15270,0.0120000000000245);
#1051=CIRCLE('',#15271,0.0192);
#1052=CIRCLE('',#15273,0.019);
#1053=CIRCLE('',#15274,0.0130000000000245);
#1054=CIRCLE('',#15276,0.0212);
#1055=CIRCLE('',#15277,0.0194);
#1056=CIRCLE('',#15279,0.0192);
#1057=CIRCLE('',#15280,0.0192);
#1058=CIRCLE('',#15282,0.0120000000000245);
#1059=CIRCLE('',#15284,0.0212);
#1149=B_SPLINE_CURVE_WITH_KNOTS('',3,(#41969,#41970,#41971,#41972,#41973),
 .UNSPECIFIED.,.F.,.F.,(4,1,4),(0.,0.5,1.),.UNSPECIFIED.);
#1150=B_SPLINE_CURVE_WITH_KNOTS('',3,(#41978,#41979,#41980,#41981),
 .UNSPECIFIED.,.F.,.F.,(4,4),(0.,1.),.UNSPECIFIED.);
#1151=B_SPLINE_CURVE_WITH_KNOTS('',3,(#41983,#41984,#41985,#41986,#41987,
#41988,#41989,#41990),.UNSPECIFIED.,.F.,.F.,(4,1,1,1,1,4),(0.,0.25,0.5,
0.625,0.75,1.),.UNSPECIFIED.);
#1152=B_SPLINE_CURVE_WITH_KNOTS('',3,(#41992,#41993,#41994,#41995,#41996,
#41997,#41998,#41999,#42000,#42001,#42002,#42003,#42004),.UNSPECIFIED.,
 .F.,.F.,(4,1,1,1,1,1,1,1,1,1,4),(0.,0.125,0.25,0.375,0.5,0.5625,0.625,
0.6875,0.75,0.875,1.),.UNSPECIFIED.);
#1153=B_SPLINE_CURVE_WITH_KNOTS('',3,(#42006,#42007,#42008,#42009),
 .UNSPECIFIED.,.F.,.F.,(4,4),(0.,1.),.UNSPECIFIED.);
#1154=B_SPLINE_CURVE_WITH_KNOTS('',3,(#42070,#42071,#42072,#42073,#42074,
#42075,#42076,#42077,#42078,#42079,#42080,#42081,#42082),.UNSPECIFIED.,
 .F.,.F.,(4,1,1,1,1,1,1,1,1,1,4),(0.,0.125,0.1875,0.25,0.3125,0.375,0.4375,
0.5,0.625,0.75,1.),.UNSPECIFIED.);
#1155=B_SPLINE_CURVE_WITH_KNOTS('',3,(#42085,#42086,#42087,#42088),
 .UNSPECIFIED.,.F.,.F.,(4,4),(0.,1.),.UNSPECIFIED.);
#1156=B_SPLINE_CURVE_WITH_KNOTS('',3,(#42090,#42091,#42092,#42093),
 .UNSPECIFIED.,.F.,.F.,(4,4),(0.,1.),.UNSPECIFIED.);
#1157=B_SPLINE_CURVE_WITH_KNOTS('',3,(#42094,#42095,#42096,#42097),
 .UNSPECIFIED.,.F.,.F.,(4,4),(0.,1.),.UNSPECIFIED.);
#1158=B_SPLINE_CURVE_WITH_KNOTS('',3,(#42099,#42100,#42101,#42102,#42103,
#42104,#42105,#42106,#42107),.UNSPECIFIED.,.F.,.F.,(4,1,1,1,1,1,4),(0.,
0.25,0.375,0.5,0.625,0.75,1.),.UNSPECIFIED.);
#1159=B_SPLINE_CURVE_WITH_KNOTS('',3,(#42109,#42110,#42111,#42112),
 .UNSPECIFIED.,.F.,.F.,(4,4),(0.,1.),.UNSPECIFIED.);
#1160=B_SPLINE_CURVE_WITH_KNOTS('',3,(#42137,#42138,#42139,#42140),
 .UNSPECIFIED.,.F.,.F.,(4,4),(0.,1.),.UNSPECIFIED.);
#1161=B_SPLINE_CURVE_WITH_KNOTS('',3,(#42144,#42145,#42146,#42147,#42148),
 .UNSPECIFIED.,.F.,.F.,(4,1,4),(0.,0.5,1.),.UNSPECIFIED.);
#1162=B_SPLINE_CURVE_WITH_KNOTS('',3,(#42173,#42174,#42175,#42176),
 .UNSPECIFIED.,.F.,.F.,(4,4),(0.,1.),.UNSPECIFIED.);
#1163=B_SPLINE_CURVE_WITH_KNOTS('',3,(#42181,#42182,#42183,#42184,#42185),
 .UNSPECIFIED.,.F.,.F.,(4,1,4),(0.,0.5,1.),.UNSPECIFIED.);
#1164=B_SPLINE_CURVE_WITH_KNOTS('',3,(#42187,#42188,#42189,#42190,#42191,
#42192,#42193,#42194,#42195,#42196,#42197,#42198),.UNSPECIFIED.,.F.,.F.,
(4,1,1,1,1,1,1,1,1,4),(0.,0.0625,0.125,0.25,0.375,0.4375,0.5,0.625,0.75,
1.),.UNSPECIFIED.);
#1165=B_SPLINE_CURVE_WITH_KNOTS('',3,(#42200,#42201,#42202,#42203,#42204,
#42205,#42206,#42207,#42208,#42209),.UNSPECIFIED.,.F.,.F.,(4,1,1,1,1,1,
1,4),(0.,0.25,0.375,0.5,0.625,0.75,0.875,1.),.UNSPECIFIED.);
#1166=B_SPLINE_CURVE_WITH_KNOTS('',3,(#42211,#42212,#42213,#42214),
 .UNSPECIFIED.,.F.,.F.,(4,4),(0.,1.),.UNSPECIFIED.);
#1167=B_SPLINE_CURVE_WITH_KNOTS('',3,(#42251,#42252,#42253,#42254,#42255,
#42256,#42257,#42258,#42259),.UNSPECIFIED.,.F.,.F.,(4,1,1,1,1,1,4),(0.,
0.25,0.375,0.5,0.75,0.875,1.),.UNSPECIFIED.);
#1168=B_SPLINE_CURVE_WITH_KNOTS('',3,(#42262,#42263,#42264,#42265),
 .UNSPECIFIED.,.F.,.F.,(4,4),(0.,1.),.UNSPECIFIED.);
#1169=B_SPLINE_CURVE_WITH_KNOTS('',3,(#42266,#42267,#42268,#42269),
 .UNSPECIFIED.,.F.,.F.,(4,4),(0.,1.),.UNSPECIFIED.);
#1170=B_SPLINE_CURVE_WITH_KNOTS('',3,(#42271,#42272,#42273,#42274),
 .UNSPECIFIED.,.F.,.F.,(4,4),(0.,1.),.UNSPECIFIED.);
#1171=B_SPLINE_CURVE_WITH_KNOTS('',3,(#42276,#42277,#42278,#42279,#42280,
#42281,#42282,#42283),.UNSPECIFIED.,.F.,.F.,(4,1,1,1,1,4),(0.,0.125,0.25,
0.5,0.75,1.),.UNSPECIFIED.);
#1172=B_SPLINE_CURVE_WITH_KNOTS('',3,(#42285,#42286,#42287,#42288),
 .UNSPECIFIED.,.F.,.F.,(4,4),(0.,1.),.UNSPECIFIED.);
#1173=B_SPLINE_CURVE_WITH_KNOTS('',3,(#42313,#42314,#42315,#42316,#42317),
 .UNSPECIFIED.,.F.,.F.,(4,1,4),(0.,0.5,1.),.UNSPECIFIED.);
#1174=B_SPLINE_CURVE_WITH_KNOTS('',3,(#42321,#42322,#42323,#42324),
 .UNSPECIFIED.,.F.,.F.,(4,4),(0.,1.),.UNSPECIFIED.);
#1175=B_SPLINE_CURVE_WITH_KNOTS('',3,(#42853,#42854,#42855,#42856,#42857,
#42858,#42859,#42860,#42861,#42862,#42863,#42864,#42865,#42866,#42867,#42868,
#42869,#42870,#42871,#42872,#42873,#42874,#42875,#42876,#42877,#42878,#42879,
#42880,#42881,#42882,#42883,#42884,#42885,#42886,#42887,#42888,#42889,#42890,
#42891,#42892,#42893,#42894,#42895,#42896,#42897,#42898,#42899,#42900,#42901,
#42902,#42903,#42904,#42905,#42906,#42907,#42908,#42909,#42910,#42911,#42912,
#42913,#42914,#42915,#42916,#42917,#42918,#42919,#42920,#42921,#42922,#42923,
#42924,#42925,#42926,#42927,#42928,#42929,#42930,#42931,#42932,#42933,#42934,
#42935,#42936,#42937,#42938,#42939,#42940,#42941,#42942,#42943,#42944,#42945,
#42946,#42947,#42948,#42949,#42950,#42951),.UNSPECIFIED.,.F.,.F.,(4,1,1,
1,1,1,1,1,1,1,1,1,1,1,1,1,1,1,1,1,1,1,1,1,1,1,1,1,1,1,1,1,1,1,1,1,1,1,1,
1,1,1,1,1,1,1,1,1,1,1,1,1,1,1,1,1,1,1,1,1,1,1,1,1,1,1,1,1,1,1,1,1,1,1,1,
1,1,1,1,1,1,1,1,1,1,1,1,1,1,1,1,1,1,1,1,1,4),(1.77834376359015E-8,0.0156250175055714,
0.0312500172277052,0.046875016949839,0.0546875168109059,0.0625000166719728,
0.0703125165330397,0.0781250163941066,0.0937500161162403,0.109375015838374,
0.125000015560508,0.140625015282642,0.156250015004775,0.171875014726909,
0.179687514587976,0.18359376451851,0.187500014449043,0.191406264379577,
0.19531251431011,0.203125014171177,0.218750013893311,0.234375013615444,
0.242187513476511,0.250000013337578,0.257812513198645,0.265625013059712,
0.281250012781846,0.312500012226113,0.343750011670381,0.359375011392515,
0.367187511253582,0.375000011114649,0.382812510975715,0.390625010836782,
0.406250010558916,0.437500010003184,0.468750009447451,0.484375009169585,
0.492187509030652,0.496093758961185,0.500000008891719,0.503906258822252,
0.507812508752786,0.515625008613853,0.531250008335986,0.562500007780254,
0.578125007502388,0.593750007224522,0.601562507085588,0.609375006946655,
0.617187506807722,0.621093756738256,0.623046881703522,0.625000006668789,
0.626953131634056,0.628906256599323,0.632812506529856,0.640625006390923,
0.656250006113057,0.664062505974124,0.671875005835191,0.679687505696257,
0.683593755626791,0.687500005557324,0.691406255487858,0.695312505418391,
0.703125005279458,0.718750005001592,0.734375004723726,0.742187504584793,
0.746093754515326,0.750000004445859,0.753906254376393,0.757812504306926,
0.765625004167993,0.781250003890127,0.789062503751194,0.796875003612261,
0.804687503473328,0.808593753403861,0.810546878369128,0.812500003334395,
0.814453128299661,0.816406253264928,0.820312503195461,0.828125003056528,
0.835937502917595,0.843750002778662,0.859375002500796,0.867187502361863,
0.87500000222293,0.882812502083997,0.890625001945063,0.906250001667197,
0.937500001111465,0.968750000555732,1.),.UNSPECIFIED.);
#1176=B_SPLINE_CURVE_WITH_KNOTS('',3,(#42954,#42955,#42956,#42957,#42958,
#42959),.UNSPECIFIED.,.F.,.F.,(4,1,1,4),(0.,0.25,0.5,1.),.UNSPECIFIED.);
#1177=B_SPLINE_CURVE_WITH_KNOTS('',3,(#42960,#42961,#42962,#42963,#42964,
#42965,#42966,#42967,#42968,#42969,#42970,#42971,#42972,#42973,#42974,#42975,
#42976,#42977,#42978,#42979,#42980,#42981,#42982,#42983,#42984,#42985,#42986,
#42987,#42988,#42989,#42990,#42991,#42992,#42993,#42994,#42995,#42996,#42997,
#42998,#42999,#43000,#43001,#43002,#43003,#43004,#43005,#43006,#43007,#43008,
#43009,#43010,#43011,#43012,#43013,#43014,#43015,#43016,#43017,#43018,#43019,
#43020,#43021,#43022,#43023,#43024,#43025,#43026,#43027,#43028,#43029,#43030,
#43031,#43032,#43033,#43034,#43035,#43036,#43037,#43038,#43039,#43040,#43041,
#43042,#43043,#43044,#43045,#43046,#43047,#43048,#43049,#43050,#43051,#43052,
#43053,#43054,#43055,#43056,#43057,#43058,#43059,#43060,#43061,#43062,#43063,
#43064,#43065,#43066,#43067,#43068,#43069,#43070,#43071,#43072,#43073,#43074,
#43075,#43076,#43077),.UNSPECIFIED.,.F.,.F.,(4,1,1,1,1,1,1,1,1,1,1,1,1,
1,1,1,1,1,1,1,1,1,1,1,1,1,1,1,1,1,1,1,1,1,1,1,1,1,1,1,1,1,1,1,1,1,1,1,1,
1,1,1,1,1,1,1,1,1,1,1,1,1,1,1,1,1,1,1,1,1,1,1,1,1,1,1,1,1,1,1,1,1,1,1,1,
1,1,1,1,1,1,1,1,1,1,1,1,1,1,1,1,1,1,1,1,1,1,1,1,1,1,1,1,1,1,4),(0.,0.015625,
0.0234375,0.03125,0.0390625,0.046875,0.0546875,0.0625,0.078125,0.0859375,
0.09375,0.1015625,0.109375,0.1171875,0.125,0.140625,0.1484375,0.15625,0.1640625,
0.171875,0.1796875,0.1875,0.203125,0.2109375,0.21875,0.2265625,0.234375,
0.2421875,0.25,0.2578125,0.265625,0.2734375,0.28125,0.2890625,0.296875,
0.3125,0.3203125,0.328125,0.3359375,0.34375,0.3515625,0.359375,0.375,0.3828125,
0.390625,0.3984375,0.40625,0.4140625,0.421875,0.4375,0.4453125,0.453125,
0.4609375,0.46875,0.4765625,0.484375,0.4921875,0.5,0.515625,0.5234375,0.53125,
0.5390625,0.546875,0.5546875,0.5625,0.578125,0.5859375,0.59375,0.6015625,
0.609375,0.6171875,0.625,0.6328125,0.640625,0.6484375,0.65625,0.6640625,
0.671875,0.6875,0.6953125,0.703125,0.7109375,0.71875,0.7265625,0.734375,
0.75,0.7578125,0.765625,0.7734375,0.78125,0.7890625,0.796875,0.8125,0.8203125,
0.828125,0.8359375,0.84375,0.8515625,0.859375,0.8671875,0.875,0.8828125,
0.890625,0.8984375,0.90625,0.9140625,0.921875,0.9296875,0.9375,0.9453125,
0.953125,0.9609375,0.96875,0.984375,0.9921875,1.),.UNSPECIFIED.);
#1178=B_SPLINE_CURVE_WITH_KNOTS('',3,(#43078,#43079,#43080,#43081,#43082,
#43083),.UNSPECIFIED.,.F.,.F.,(4,1,1,4),(0.,0.5,0.75,1.),.UNSPECIFIED.);
#1179=B_SPLINE_CURVE_WITH_KNOTS('',3,(#43085,#43086,#43087,#43088,#43089,
#43090,#43091,#43092,#43093,#43094,#43095,#43096,#43097,#43098,#43099,#43100,
#43101,#43102,#43103,#43104,#43105,#43106,#43107,#43108,#43109,#43110,#43111,
#43112,#43113,#43114,#43115,#43116),.UNSPECIFIED.,.F.,.F.,(4,1,1,1,1,1,
1,1,1,1,1,1,1,1,1,1,1,1,1,1,1,1,1,1,1,1,1,1,1,4),(0.,0.0624999888291916,
0.124999977658383,0.187499966487575,0.218749960902171,0.234374958109469,
0.249999955316766,0.265624952524064,0.273437451127713,0.281249949731362,
0.285156199033187,0.289062448335011,0.29687494693866,0.312499944145958,
0.343749938560554,0.37499993297515,0.406249927389746,0.437499921804341,
0.499999910633533,0.531249905048129,0.546874902255427,0.562499899462725,
0.570312398066374,0.578124896670023,0.59374989387732,0.624999888291916,
0.687499877121108,0.7499998659503,0.874999843608683,0.999999821267066),
 .UNSPECIFIED.);
#1180=B_SPLINE_CURVE_WITH_KNOTS('',3,(#43118,#43119,#43120,#43121,#43122,
#43123,#43124,#43125,#43126,#43127,#43128,#43129,#43130,#43131,#43132,#43133,
#43134,#43135,#43136,#43137,#43138,#43139,#43140,#43141,#43142,#43143,#43144,
#43145,#43146,#43147,#43148,#43149,#43150,#43151,#43152,#43153,#43154,#43155,
#43156,#43157,#43158,#43159,#43160,#43161,#43162,#43163,#43164,#43165,#43166,
#43167,#43168,#43169,#43170,#43171,#43172,#43173,#43174,#43175,#43176,#43177,
#43178,#43179,#43180,#43181,#43182,#43183,#43184,#43185,#43186,#43187,#43188,
#43189,#43190,#43191,#43192,#43193,#43194,#43195,#43196,#43197,#43198,#43199,
#43200,#43201,#43202,#43203,#43204,#43205,#43206,#43207,#43208,#43209,#43210,
#43211,#43212,#43213,#43214,#43215,#43216,#43217,#43218,#43219,#43220,#43221,
#43222,#43223,#43224,#43225,#43226,#43227,#43228,#43229,#43230,#43231,#43232,
#43233,#43234,#43235,#43236,#43237,#43238),.UNSPECIFIED.,.F.,.F.,(4,1,1,
1,1,1,1,1,1,1,1,1,1,1,1,1,1,1,1,1,1,1,1,1,1,1,1,1,1,1,1,1,1,1,1,1,1,1,1,
1,1,1,1,1,1,1,1,1,1,1,1,1,1,1,1,1,1,1,1,1,1,1,1,1,1,1,1,1,1,1,1,1,1,1,1,
1,1,1,1,1,1,1,1,1,1,1,1,1,1,1,1,1,1,1,1,1,1,1,1,1,1,1,1,1,1,1,1,1,1,1,1,
1,1,1,1,1,1,1,4),(0.,0.03125,0.0625,0.09375,0.109375,0.125,0.1328125,0.140625,
0.15625,0.171875,0.1796875,0.18359375,0.1875,0.19140625,0.1953125,0.203125,
0.21875,0.2265625,0.234375,0.2421875,0.24609375,0.248046875,0.25,0.251953125,
0.25390625,0.2578125,0.265625,0.2734375,0.28125,0.296875,0.3046875,0.30859375,
0.310546875,0.3125,0.314453125,0.31640625,0.3203125,0.328125,0.3359375,
0.34375,0.3515625,0.359375,0.3671875,0.37109375,0.373046875,0.375,0.376953125,
0.37890625,0.3828125,0.390625,0.40625,0.4140625,0.421875,0.4296875,0.43359375,
0.435546875,0.4375,0.439453125,0.44140625,0.4453125,0.453125,0.4609375,
0.46875,0.484375,0.4921875,0.49609375,0.5,0.50390625,0.5078125,0.515625,
0.53125,0.5625,0.578125,0.59375,0.6015625,0.609375,0.61328125,0.6171875,
0.62109375,0.623046875,0.625,0.626953125,0.62890625,0.6328125,0.640625,
0.6484375,0.65234375,0.654296875,0.65625,0.658203125,0.66015625,0.6640625,
0.671875,0.6796875,0.6875,0.6953125,0.703125,0.71875,0.7265625,0.734375,
0.7421875,0.74609375,0.75,0.75390625,0.7578125,0.765625,0.78125,0.796875,
0.8125,0.84375,0.859375,0.8671875,0.875,0.8828125,0.890625,0.90625,0.9375,
0.96875,1.),.UNSPECIFIED.);
#1181=B_SPLINE_CURVE_WITH_KNOTS('',3,(#43240,#43241,#43242,#43243,#43244,
#43245,#43246,#43247,#43248,#43249,#43250,#43251,#43252,#43253,#43254,#43255,
#43256,#43257,#43258,#43259,#43260,#43261,#43262,#43263,#43264,#43265,#43266,
#43267,#43268,#43269,#43270,#43271,#43272,#43273,#43274,#43275,#43276,#43277,
#43278,#43279,#43280,#43281,#43282,#43283,#43284,#43285,#43286,#43287,#43288,
#43289,#43290,#43291,#43292,#43293,#43294,#43295,#43296,#43297,#43298,#43299,
#43300,#43301,#43302,#43303,#43304,#43305,#43306,#43307,#43308,#43309,#43310,
#43311,#43312,#43313,#43314,#43315,#43316,#43317,#43318,#43319,#43320,#43321,
#43322,#43323,#43324,#43325,#43326,#43327,#43328,#43329,#43330,#43331,#43332,
#43333,#43334,#43335,#43336,#43337,#43338,#43339,#43340,#43341,#43342,#43343,
#43344,#43345,#43346,#43347,#43348,#43349,#43350,#43351,#43352,#43353,#43354,
#43355,#43356,#43357,#43358,#43359,#43360,#43361,#43362,#43363,#43364,#43365,
#43366,#43367,#43368,#43369,#43370,#43371,#43372,#43373,#43374,#43375,#43376,
#43377,#43378,#43379,#43380,#43381,#43382,#43383),.UNSPECIFIED.,.F.,.F.,
(4,1,1,1,1,1,1,1,1,1,1,1,1,1,1,1,1,1,1,1,1,1,1,1,1,1,1,1,1,1,1,1,1,1,1,
1,1,1,1,1,1,1,1,1,1,1,1,1,1,1,1,1,1,1,1,1,1,1,1,1,1,1,1,1,1,1,1,1,1,1,1,
1,1,1,1,1,1,1,1,1,1,1,1,1,1,1,1,1,1,1,1,1,1,1,1,1,1,1,1,1,1,1,1,1,1,1,1,
1,1,1,1,1,1,1,1,1,1,1,1,1,1,1,1,1,1,1,1,1,1,1,1,1,1,1,1,1,1,1,1,1,1,4),
(0.,0.03125,0.046875,0.0625,0.078125,0.09375,0.1015625,0.109375,0.1171875,
0.12109375,0.123046875,0.125,0.126953125,0.12890625,0.1328125,0.140625,
0.1484375,0.15234375,0.15625,0.1640625,0.171875,0.1796875,0.1875,0.19140625,
0.1953125,0.203125,0.21875,0.2265625,0.234375,0.2421875,0.24609375,0.248046875,
0.25,0.251953125,0.25390625,0.2578125,0.265625,0.2734375,0.28125,0.296875,
0.3046875,0.30859375,0.3125,0.31640625,0.3203125,0.328125,0.34375,0.359375,
0.3671875,0.37109375,0.375,0.37890625,0.3828125,0.390625,0.40625,0.421875,
0.4375,0.453125,0.46875,0.4765625,0.484375,0.4921875,0.49609375,0.498046875,
0.5,0.501953125,0.50390625,0.5078125,0.515625,0.5234375,0.53125,0.5390625,
0.546875,0.5546875,0.55859375,0.560546875,0.5625,0.564453125,0.56640625,
0.5703125,0.578125,0.5859375,0.59375,0.609375,0.625,0.65625,0.671875,0.6875,
0.703125,0.71875,0.7265625,0.734375,0.73828125,0.7421875,0.74609375,0.748046875,
0.75,0.751953125,0.75390625,0.7578125,0.765625,0.7734375,0.78125,0.7890625,
0.796875,0.80078125,0.8046875,0.80859375,0.810546875,0.8115234375,0.8125,
0.8134765625,0.814453125,0.81640625,0.8203125,0.82421875,0.828125,0.8359375,
0.84375,0.859375,0.8671875,0.87109375,0.875,0.87890625,0.8828125,0.890625,
0.8984375,0.90625,0.9140625,0.921875,0.9296875,0.93359375,0.935546875,0.9375,
0.939453125,0.94140625,0.9453125,0.953125,0.9609375,0.96875,0.984375,1.),
 .UNSPECIFIED.);
#1182=B_SPLINE_CURVE_WITH_KNOTS('',3,(#43385,#43386,#43387,#43388,#43389,
#43390,#43391,#43392,#43393,#43394,#43395,#43396,#43397,#43398,#43399,#43400,
#43401,#43402,#43403,#43404,#43405,#43406,#43407,#43408,#43409,#43410,#43411,
#43412,#43413,#43414,#43415,#43416,#43417,#43418,#43419,#43420,#43421,#43422,
#43423,#43424,#43425,#43426,#43427,#43428,#43429,#43430,#43431,#43432,#43433,
#43434,#43435,#43436,#43437,#43438,#43439,#43440,#43441,#43442,#43443,#43444,
#43445,#43446,#43447,#43448,#43449,#43450,#43451,#43452,#43453,#43454,#43455,
#43456,#43457,#43458,#43459,#43460,#43461,#43462,#43463,#43464,#43465,#43466,
#43467,#43468,#43469,#43470,#43471,#43472,#43473,#43474,#43475,#43476,#43477,
#43478,#43479,#43480,#43481,#43482,#43483,#43484,#43485,#43486,#43487,#43488,
#43489,#43490,#43491,#43492,#43493,#43494,#43495,#43496,#43497,#43498,#43499,
#43500,#43501,#43502,#43503,#43504,#43505,#43506,#43507,#43508,#43509,#43510,
#43511,#43512,#43513,#43514,#43515,#43516,#43517,#43518),.UNSPECIFIED.,
 .F.,.F.,(4,1,1,1,1,1,1,1,1,1,1,1,1,1,1,1,1,1,1,1,1,1,1,1,1,1,1,1,1,1,1,
1,1,1,1,1,1,1,1,1,1,1,1,1,1,1,1,1,1,1,1,1,1,1,1,1,1,1,1,1,1,1,1,1,1,1,1,
1,1,1,1,1,1,1,1,1,1,1,1,1,1,1,1,1,1,1,1,1,1,1,1,1,1,1,1,1,1,1,1,1,1,1,1,
1,1,1,1,1,1,1,1,1,1,1,1,1,1,1,1,1,1,1,1,1,1,1,1,1,1,1,1,4),(0.,0.015625,
0.03125,0.046875,0.0546875,0.05859375,0.0625,0.06640625,0.0703125,0.078125,
0.09375,0.125,0.15625,0.171875,0.1875,0.203125,0.21875,0.2265625,0.234375,
0.2421875,0.24609375,0.248046875,0.25,0.251953125,0.25390625,0.2578125,
0.265625,0.2734375,0.27734375,0.28125,0.2890625,0.296875,0.3046875,0.30859375,
0.3125,0.31640625,0.3203125,0.328125,0.34375,0.359375,0.3671875,0.375,0.3828125,
0.390625,0.40625,0.421875,0.4296875,0.43359375,0.4375,0.44140625,0.4453125,
0.453125,0.46875,0.484375,0.4921875,0.49609375,0.5,0.50390625,0.5078125,
0.515625,0.53125,0.546875,0.5625,0.578125,0.59375,0.6015625,0.609375,0.6171875,
0.62109375,0.623046875,0.625,0.626953125,0.62890625,0.6328125,0.640625,
0.65625,0.6640625,0.671875,0.6796875,0.68359375,0.685546875,0.6875,0.689453125,
0.69140625,0.6953125,0.703125,0.71875,0.734375,0.7421875,0.74609375,0.75,
0.75390625,0.7578125,0.765625,0.78125,0.796875,0.8125,0.828125,0.84375,
0.8515625,0.859375,0.86328125,0.8671875,0.87109375,0.873046875,0.8740234375,
0.875,0.876953125,0.87890625,0.8828125,0.88671875,0.890625,0.8984375,0.90625,
0.9140625,0.921875,0.92578125,0.9296875,0.93359375,0.935546875,0.9365234375,
0.9375,0.9384765625,0.939453125,0.94140625,0.9453125,0.94921875,0.953125,
0.9609375,0.96875,0.984375,1.),.UNSPECIFIED.);
#1183=B_SPLINE_CURVE_WITH_KNOTS('',3,(#43520,#43521,#43522,#43523,#43524,
#43525,#43526,#43527,#43528,#43529,#43530),.UNSPECIFIED.,.F.,.F.,(4,1,1,
1,1,1,1,1,4),(0.,0.125,0.25,0.375,0.5,0.625,0.75,0.875,1.),
 .UNSPECIFIED.);
#1184=B_SPLINE_CURVE_WITH_KNOTS('',3,(#43532,#43533,#43534,#43535,#43536,
#43537,#43538,#43539,#43540,#43541,#43542),.UNSPECIFIED.,.F.,.F.,(4,1,1,
1,1,1,1,1,4),(0.,0.125,0.25,0.375,0.5,0.625,0.75,0.875,1.),
 .UNSPECIFIED.);
#1185=B_SPLINE_CURVE_WITH_KNOTS('',3,(#43544,#43545,#43546,#43547),
 .UNSPECIFIED.,.F.,.F.,(4,4),(0.,0.999935365761805),.UNSPECIFIED.);
#1186=B_SPLINE_CURVE_WITH_KNOTS('',3,(#43549,#43550,#43551,#43552),
 .UNSPECIFIED.,.F.,.F.,(4,4),(2.06275312002674E-5,0.999974447229001),
 .UNSPECIFIED.);
#1187=B_SPLINE_CURVE_WITH_KNOTS('',3,(#43553,#43554,#43555,#43556),
 .UNSPECIFIED.,.F.,.F.,(4,4),(8.00007213080448E-5,1.),.UNSPECIFIED.);
#1188=B_SPLINE_CURVE_WITH_KNOTS('',3,(#43558,#43559,#43560,#43561),
 .UNSPECIFIED.,.F.,.F.,(4,4),(2.02588963018075E-5,0.999973166574012),
 .UNSPECIFIED.);
#1189=B_SPLINE_CURVE_WITH_KNOTS('',3,(#43563,#43564,#43565,#43566),
 .UNSPECIFIED.,.F.,.F.,(4,4),(8.39549495919811E-5,1.),.UNSPECIFIED.);
#1190=B_SPLINE_CURVE_WITH_KNOTS('',3,(#43567,#43568,#43569,#43570),
 .UNSPECIFIED.,.F.,.F.,(4,4),(0.,0.99993649865183),.UNSPECIFIED.);
#1191=B_SPLINE_CURVE_WITH_KNOTS('',3,(#44099,#44100,#44101,#44102,#44103,
#44104,#44105,#44106,#44107,#44108,#44109,#44110,#44111,#44112,#44113,#44114,
#44115,#44116,#44117,#44118,#44119,#44120,#44121,#44122,#44123,#44124,#44125,
#44126,#44127,#44128,#44129,#44130,#44131,#44132,#44133,#44134,#44135,#44136,
#44137,#44138,#44139,#44140,#44141,#44142,#44143,#44144,#44145,#44146,#44147,
#44148,#44149,#44150,#44151,#44152,#44153,#44154,#44155,#44156,#44157,#44158,
#44159,#44160,#44161,#44162,#44163,#44164,#44165,#44166,#44167,#44168,#44169,
#44170,#44171,#44172,#44173,#44174,#44175,#44176,#44177,#44178,#44179,#44180,
#44181,#44182,#44183,#44184,#44185,#44186,#44187,#44188,#44189,#44190,#44191,
#44192,#44193,#44194,#44195,#44196,#44197,#44198,#44199,#44200,#44201,#44202,
#44203,#44204,#44205,#44206,#44207,#44208,#44209,#44210,#44211,#44212,#44213,
#44214,#44215,#44216),.UNSPECIFIED.,.F.,.F.,(4,1,1,1,1,1,1,1,1,1,1,1,1,
1,1,1,1,1,1,1,1,1,1,1,1,1,1,1,1,1,1,1,1,1,1,1,1,1,1,1,1,1,1,1,1,1,1,1,1,
1,1,1,1,1,1,1,1,1,1,1,1,1,1,1,1,1,1,1,1,1,1,1,1,1,1,1,1,1,1,1,1,1,1,1,1,
1,1,1,1,1,1,1,1,1,1,1,1,1,1,1,1,1,1,1,1,1,1,1,1,1,1,1,1,1,1,4),(0.,0.015625,
0.0234375,0.03125,0.0390625,0.046875,0.0546875,0.0625,0.078125,0.0859375,
0.09375,0.1015625,0.109375,0.1171875,0.125,0.140625,0.1484375,0.15625,0.1640625,
0.171875,0.1796875,0.1875,0.203125,0.2109375,0.21875,0.2265625,0.234375,
0.2421875,0.25,0.2578125,0.265625,0.2734375,0.28125,0.2890625,0.296875,
0.3125,0.3203125,0.328125,0.3359375,0.34375,0.3515625,0.359375,0.375,0.3828125,
0.390625,0.3984375,0.40625,0.4140625,0.421875,0.4375,0.4453125,0.453125,
0.4609375,0.46875,0.4765625,0.484375,0.4921875,0.5,0.515625,0.5234375,0.53125,
0.5390625,0.546875,0.5546875,0.5625,0.578125,0.5859375,0.59375,0.6015625,
0.609375,0.6171875,0.625,0.6328125,0.640625,0.6484375,0.65625,0.6640625,
0.671875,0.6875,0.6953125,0.703125,0.7109375,0.71875,0.7265625,0.734375,
0.75,0.7578125,0.765625,0.7734375,0.78125,0.7890625,0.796875,0.8125,0.8203125,
0.828125,0.8359375,0.84375,0.8515625,0.859375,0.8671875,0.875,0.8828125,
0.890625,0.8984375,0.90625,0.9140625,0.921875,0.9296875,0.9375,0.9453125,
0.953125,0.9609375,0.96875,0.984375,0.9921875,1.),.UNSPECIFIED.);
#1192=B_SPLINE_CURVE_WITH_KNOTS('',3,(#44217,#44218,#44219,#44220,#44221,
#44222),.UNSPECIFIED.,.F.,.F.,(4,1,1,4),(0.,0.5,0.75,1.),.UNSPECIFIED.);
#1193=B_SPLINE_CURVE_WITH_KNOTS('',3,(#44223,#44224,#44225,#44226,#44227,
#44228,#44229,#44230,#44231,#44232,#44233,#44234,#44235,#44236,#44237,#44238,
#44239,#44240,#44241,#44242,#44243,#44244,#44245,#44246,#44247,#44248,#44249,
#44250,#44251,#44252,#44253,#44254,#44255,#44256,#44257,#44258,#44259,#44260,
#44261,#44262,#44263,#44264,#44265,#44266,#44267,#44268,#44269,#44270,#44271,
#44272,#44273,#44274,#44275,#44276,#44277,#44278,#44279,#44280,#44281,#44282,
#44283,#44284,#44285,#44286,#44287,#44288,#44289,#44290,#44291,#44292,#44293,
#44294,#44295,#44296,#44297,#44298,#44299,#44300),.UNSPECIFIED.,.F.,.F.,
(4,1,1,1,1,1,1,1,1,1,1,1,1,1,1,1,1,1,1,1,1,1,1,1,1,1,1,1,1,1,1,1,1,1,1,
1,1,1,1,1,1,1,1,1,1,1,1,1,1,1,1,1,1,1,1,1,1,1,1,1,1,1,1,1,1,1,1,1,1,1,1,
1,1,1,1,4),(0.,0.0312499974019096,0.0624999948038192,0.0937499922057288,
0.109374990906684,0.117187490257161,0.124999989607638,0.132812488958116,
0.140624988308593,0.156249987009548,0.187499984411458,0.203124983112412,
0.218749981813367,0.234374980514322,0.242187479864799,0.246093729540038,
0.249999979215277,0.253906228890515,0.257812478565754,0.265624977916232,
0.281249976617186,0.296874975318141,0.304687474668619,0.312499974019096,
0.328124972720051,0.343749971421006,0.351562470771483,0.35937497012196,
0.367187469472438,0.371093719147676,0.374999968822915,0.378906218498154,
0.382812468173393,0.39062496752387,0.406249966224825,0.42187496492578,0.429687464276257,
0.437499963626734,0.445312462977212,0.453124962327689,0.468749961028644,
0.499999958430554,0.515624957131508,0.531249955832463,0.562499953234373,
0.593749950636282,0.609374949337237,0.617187448687714,0.624999948038192,
0.632812447388669,0.640624946739147,0.656249945440102,0.687499942842011,
0.718749940243921,0.74999993764583,0.765624936346785,0.78124993504774,0.796874933748695,
0.804687433099172,0.812499932449649,0.820312431800127,0.828124931150604,
0.843749929851559,0.859374928552514,0.867187427902991,0.87109367757823,
0.874999927253469,0.878906176928707,0.882812426603946,0.890624925954423,
0.906249924655378,0.921874923356333,0.937499922057288,0.953124920758243,
0.968749919459197,0.999999916861107),.UNSPECIFIED.);
#1194=B_SPLINE_CURVE_WITH_KNOTS('',3,(#44302,#44303,#44304,#44305,#44306,
#44307,#44308,#44309,#44310,#44311,#44312,#44313,#44314,#44315,#44316,#44317,
#44318,#44319,#44320,#44321,#44322,#44323,#44324,#44325,#44326,#44327,#44328,
#44329,#44330,#44331,#44332,#44333,#44334,#44335,#44336,#44337,#44338,#44339,
#44340,#44341,#44342,#44343,#44344,#44345,#44346,#44347,#44348,#44349,#44350,
#44351,#44352,#44353,#44354,#44355,#44356,#44357,#44358,#44359,#44360,#44361,
#44362,#44363,#44364,#44365,#44366,#44367,#44368,#44369,#44370,#44371,#44372,
#44373,#44374,#44375,#44376,#44377,#44378,#44379,#44380,#44381,#44382,#44383,
#44384,#44385,#44386,#44387,#44388,#44389,#44390,#44391,#44392,#44393,#44394,
#44395,#44396,#44397,#44398,#44399,#44400,#44401,#44402,#44403,#44404,#44405,
#44406,#44407,#44408,#44409,#44410,#44411,#44412,#44413,#44414,#44415,#44416,
#44417,#44418,#44419,#44420,#44421,#44422,#44423,#44424,#44425,#44426,#44427,
#44428,#44429,#44430,#44431,#44432,#44433,#44434,#44435,#44436,#44437,#44438,
#44439,#44440,#44441,#44442,#44443,#44444,#44445,#44446,#44447,#44448,#44449,
#44450,#44451,#44452,#44453,#44454),.UNSPECIFIED.,.F.,.F.,(4,1,1,1,1,1,
1,1,1,1,1,1,1,1,1,1,1,1,1,1,1,1,1,1,1,1,1,1,1,1,1,1,1,1,1,1,1,1,1,1,1,1,
1,1,1,1,1,1,1,1,1,1,1,1,1,1,1,1,1,1,1,1,1,1,1,1,1,1,1,1,1,1,1,1,1,1,1,1,
1,1,1,1,1,1,1,1,1,1,1,1,1,1,1,1,1,1,1,1,1,1,1,1,1,1,1,1,1,1,1,1,1,1,1,1,
1,1,1,1,1,1,1,1,1,1,1,1,1,1,1,1,1,1,1,1,1,1,1,1,1,1,1,1,1,1,1,1,1,1,1,1,
4),(0.,0.015625,0.03125,0.0390625,0.046875,0.0546875,0.05859375,0.060546875,
0.0625,0.064453125,0.06640625,0.0703125,0.078125,0.0859375,0.09375,0.109375,
0.125,0.140625,0.15625,0.171875,0.1875,0.203125,0.21875,0.2265625,0.234375,
0.23828125,0.2421875,0.24609375,0.248046875,0.25,0.251953125,0.25390625,
0.2578125,0.265625,0.2734375,0.28125,0.2890625,0.296875,0.30078125,0.3046875,
0.30859375,0.310546875,0.3115234375,0.3125,0.3134765625,0.314453125,0.31640625,
0.3203125,0.32421875,0.328125,0.3359375,0.34375,0.359375,0.3671875,0.37109375,
0.375,0.37890625,0.3828125,0.390625,0.3984375,0.40625,0.4140625,0.421875,
0.4296875,0.43359375,0.435546875,0.4375,0.439453125,0.44140625,0.4453125,
0.453125,0.4609375,0.46875,0.4765625,0.484375,0.4921875,0.49609375,0.498046875,
0.5,0.501953125,0.50390625,0.5078125,0.515625,0.5234375,0.53125,0.546875,
0.5625,0.59375,0.609375,0.625,0.6328125,0.640625,0.65625,0.671875,0.6796875,
0.68359375,0.6875,0.69140625,0.6953125,0.703125,0.71875,0.7265625,0.734375,
0.7421875,0.74609375,0.748046875,0.75,0.751953125,0.75390625,0.7578125,
0.765625,0.7734375,0.78125,0.7890625,0.796875,0.8046875,0.80859375,0.810546875,
0.8125,0.814453125,0.81640625,0.8203125,0.828125,0.8359375,0.84375,0.8515625,
0.859375,0.8671875,0.87109375,0.873046875,0.875,0.876953125,0.87890625,
0.8828125,0.890625,0.8984375,0.90625,0.9140625,0.921875,0.9296875,0.93359375,
0.935546875,0.9375,0.939453125,0.94140625,0.9453125,0.953125,0.9609375,
0.96875,0.984375,1.),.UNSPECIFIED.);
#1195=B_SPLINE_CURVE_WITH_KNOTS('',3,(#44456,#44457,#44458,#44459,#44460,
#44461,#44462,#44463,#44464,#44465,#44466),.UNSPECIFIED.,.F.,.F.,(4,1,1,
1,1,1,1,1,4),(0.,0.125,0.25,0.375,0.5,0.625,0.75,0.875,1.),
 .UNSPECIFIED.);
#1196=B_SPLINE_CURVE_WITH_KNOTS('',3,(#44468,#44469,#44470,#44471,#44472,
#44473,#44474,#44475,#44476,#44477,#44478,#44479,#44480,#44481,#44482,#44483,
#44484,#44485,#44486,#44487,#44488,#44489,#44490,#44491,#44492,#44493,#44494,
#44495,#44496,#44497,#44498,#44499,#44500,#44501,#44502,#44503,#44504,#44505,
#44506,#44507,#44508,#44509,#44510,#44511,#44512,#44513,#44514,#44515,#44516,
#44517,#44518,#44519,#44520,#44521,#44522,#44523,#44524,#44525,#44526,#44527,
#44528,#44529,#44530,#44531,#44532,#44533,#44534,#44535,#44536,#44537,#44538,
#44539,#44540,#44541,#44542,#44543,#44544,#44545,#44546,#44547,#44548,#44549,
#44550,#44551,#44552,#44553,#44554,#44555,#44556,#44557,#44558,#44559,#44560,
#44561,#44562,#44563,#44564,#44565,#44566,#44567,#44568,#44569,#44570,#44571,
#44572,#44573,#44574,#44575,#44576,#44577,#44578,#44579,#44580,#44581,#44582,
#44583,#44584,#44585,#44586,#44587,#44588,#44589,#44590,#44591,#44592),
 .UNSPECIFIED.,.F.,.F.,(4,1,1,1,1,1,1,1,1,1,1,1,1,1,1,1,1,1,1,1,1,1,1,1,
1,1,1,1,1,1,1,1,1,1,1,1,1,1,1,1,1,1,1,1,1,1,1,1,1,1,1,1,1,1,1,1,1,1,1,1,
1,1,1,1,1,1,1,1,1,1,1,1,1,1,1,1,1,1,1,1,1,1,1,1,1,1,1,1,1,1,1,1,1,1,1,1,
1,1,1,1,1,1,1,1,1,1,1,1,1,1,1,1,1,1,1,1,1,1,1,1,1,1,4),(0.,0.03125,0.046875,
0.0625,0.078125,0.09375,0.1015625,0.109375,0.11328125,0.1171875,0.12109375,
0.123046875,0.125,0.126953125,0.12890625,0.1328125,0.140625,0.1484375,0.15234375,
0.154296875,0.15625,0.158203125,0.16015625,0.1640625,0.171875,0.1796875,
0.1875,0.1953125,0.203125,0.21875,0.234375,0.2421875,0.24609375,0.248046875,
0.25,0.251953125,0.25390625,0.2578125,0.265625,0.28125,0.296875,0.3125,
0.328125,0.34375,0.359375,0.3671875,0.375,0.3828125,0.390625,0.40625,0.421875,
0.4375,0.453125,0.46875,0.4765625,0.484375,0.4921875,0.49609375,0.498046875,
0.5,0.501953125,0.50390625,0.5078125,0.515625,0.53125,0.5390625,0.546875,
0.5546875,0.55859375,0.560546875,0.5625,0.564453125,0.56640625,0.5703125,
0.578125,0.5859375,0.59375,0.609375,0.625,0.640625,0.65625,0.671875,0.6875,
0.703125,0.71875,0.7265625,0.734375,0.7421875,0.74609375,0.748046875,0.75,
0.751953125,0.75390625,0.7578125,0.765625,0.7734375,0.77734375,0.78125,
0.7890625,0.796875,0.8046875,0.80859375,0.8125,0.81640625,0.8203125,0.828125,
0.84375,0.859375,0.8671875,0.875,0.8828125,0.890625,0.90625,0.921875,0.9296875,
0.93359375,0.9375,0.94140625,0.9453125,0.953125,0.96875,0.984375,1.),
 .UNSPECIFIED.);
#1197=B_SPLINE_CURVE_WITH_KNOTS('',3,(#44594,#44595,#44596,#44597,#44598,
#44599,#44600,#44601,#44602,#44603,#44604,#44605,#44606,#44607,#44608,#44609,
#44610,#44611,#44612,#44613,#44614,#44615,#44616,#44617,#44618,#44619,#44620,
#44621,#44622,#44623,#44624,#44625,#44626,#44627,#44628,#44629,#44630,#44631,
#44632,#44633,#44634,#44635,#44636,#44637,#44638,#44639,#44640,#44641,#44642,
#44643,#44644,#44645,#44646,#44647,#44648,#44649,#44650,#44651,#44652,#44653,
#44654,#44655,#44656,#44657,#44658,#44659,#44660,#44661,#44662,#44663,#44664,
#44665,#44666,#44667,#44668,#44669,#44670,#44671,#44672,#44673,#44674,#44675,
#44676,#44677,#44678,#44679,#44680,#44681,#44682,#44683,#44684,#44685,#44686,
#44687,#44688,#44689,#44690,#44691,#44692,#44693,#44694,#44695,#44696,#44697,
#44698,#44699,#44700,#44701,#44702,#44703,#44704,#44705,#44706,#44707,#44708,
#44709,#44710,#44711,#44712,#44713,#44714,#44715,#44716,#44717,#44718,#44719,
#44720,#44721,#44722,#44723,#44724,#44725,#44726,#44727,#44728,#44729,#44730,
#44731,#44732,#44733,#44734,#44735,#44736,#44737,#44738,#44739,#44740,#44741,
#44742,#44743,#44744,#44745,#44746,#44747),.UNSPECIFIED.,.F.,.F.,(4,1,1,
1,1,1,1,1,1,1,1,1,1,1,1,1,1,1,1,1,1,1,1,1,1,1,1,1,1,1,1,1,1,1,1,1,1,1,1,
1,1,1,1,1,1,1,1,1,1,1,1,1,1,1,1,1,1,1,1,1,1,1,1,1,1,1,1,1,1,1,1,1,1,1,1,
1,1,1,1,1,1,1,1,1,1,1,1,1,1,1,1,1,1,1,1,1,1,1,1,1,1,1,1,1,1,1,1,1,1,1,1,
1,1,1,1,1,1,1,1,1,1,1,1,1,1,1,1,1,1,1,1,1,1,1,1,1,1,1,1,1,1,1,1,1,1,1,1,
1,1,1,1,4),(0.,0.015625,0.03125,0.0390625,0.046875,0.0546875,0.05859375,
0.060546875,0.0625,0.064453125,0.06640625,0.0703125,0.078125,0.09375,0.109375,
0.125,0.140625,0.15625,0.171875,0.1875,0.203125,0.21875,0.2265625,0.234375,
0.23828125,0.2421875,0.24609375,0.248046875,0.25,0.251953125,0.25390625,
0.2578125,0.265625,0.2734375,0.28125,0.2890625,0.296875,0.30078125,0.3046875,
0.30859375,0.310546875,0.3115234375,0.3125,0.3134765625,0.314453125,0.31640625,
0.3203125,0.32421875,0.328125,0.3359375,0.34375,0.359375,0.3671875,0.37109375,
0.375,0.37890625,0.3828125,0.390625,0.40625,0.4140625,0.421875,0.4296875,
0.43359375,0.435546875,0.4375,0.439453125,0.44140625,0.4453125,0.453125,
0.4609375,0.46875,0.4765625,0.484375,0.4921875,0.49609375,0.498046875,0.5,
0.501953125,0.50390625,0.5078125,0.515625,0.5234375,0.53125,0.546875,0.5625,
0.59375,0.609375,0.6171875,0.625,0.6328125,0.640625,0.65625,0.671875,0.6796875,
0.68359375,0.6875,0.69140625,0.6953125,0.703125,0.71875,0.7265625,0.734375,
0.7421875,0.74609375,0.748046875,0.75,0.751953125,0.75390625,0.7578125,
0.76171875,0.765625,0.7734375,0.78125,0.7890625,0.796875,0.8046875,0.80859375,
0.810546875,0.8125,0.814453125,0.81640625,0.8203125,0.82421875,0.828125,
0.8359375,0.84375,0.8515625,0.859375,0.8671875,0.87109375,0.873046875,0.875,
0.876953125,0.87890625,0.8828125,0.890625,0.90625,0.9140625,0.921875,0.92578125,
0.9296875,0.93359375,0.935546875,0.9375,0.939453125,0.94140625,0.9453125,
0.953125,0.9609375,0.96875,0.984375,1.),.UNSPECIFIED.);
#1198=B_SPLINE_CURVE_WITH_KNOTS('',3,(#44749,#44750,#44751,#44752,#44753,
#44754,#44755,#44756,#44757,#44758,#44759),.UNSPECIFIED.,.F.,.F.,(4,1,1,
1,1,1,1,1,4),(0.,0.125,0.25,0.375,0.5,0.625,0.75,0.875,1.),
 .UNSPECIFIED.);
#1199=B_SPLINE_CURVE_WITH_KNOTS('',3,(#44761,#44762,#44763,#44764,#44765,
#44766,#44767,#44768,#44769,#44770,#44771,#44772,#44773,#44774,#44775,#44776,
#44777,#44778,#44779,#44780,#44781,#44782,#44783,#44784,#44785,#44786,#44787,
#44788,#44789,#44790,#44791,#44792,#44793,#44794,#44795,#44796),
 .UNSPECIFIED.,.F.,.F.,(4,1,1,1,1,1,1,1,1,1,1,1,1,1,1,1,1,1,1,1,1,1,1,1,
1,1,1,1,1,1,1,1,1,4),(3.38284667726637E-8,0.0625000317141876,0.125000029599908,
0.187500027485629,0.21875002642849,0.25000002537135,0.26562502484278,0.273437524578495,
0.281250024314211,0.285156274182068,0.289062524049926,0.296875023785641,
0.312500023257071,0.343750022199931,0.375000021142792,0.437500019028513,
0.468750017971373,0.500000016914233,0.531250015857094,0.546875015328524,
0.562500014799954,0.566406264667812,0.570312514535669,0.578125014271384,
0.585937514007099,0.593750013742815,0.625000012685675,0.687500010571396,
0.750000008457117,0.781250007399977,0.812500006342838,0.875000004228558,
0.937500002114279,1.),.UNSPECIFIED.);
#1200=B_SPLINE_CURVE_WITH_KNOTS('',3,(#44797,#44798,#44799,#44800,#44801,
#44802),.UNSPECIFIED.,.F.,.F.,(4,1,1,4),(0.,0.25,0.5,1.),.UNSPECIFIED.);
#1535=PLANE('',#15269);
#1536=PLANE('',#15272);
#1537=PLANE('',#15275);
#1819=CYLINDRICAL_SURFACE('',#15264,0.00100009891588755);
#1820=CYLINDRICAL_SURFACE('',#15267,0.000199929791356894);
#1821=CYLINDRICAL_SURFACE('',#15268,0.000199893207290678);
#1822=CYLINDRICAL_SURFACE('',#15278,0.0192);
#1823=CYLINDRICAL_SURFACE('',#15281,0.0120000000000245);
#1824=CYLINDRICAL_SURFACE('',#15283,0.0212);
#5494=ORIENTED_EDGE('',*,*,#7394,.F.);
#5495=ORIENTED_EDGE('',*,*,#7395,.T.);
#5496=ORIENTED_EDGE('',*,*,#7396,.F.);
#5497=ORIENTED_EDGE('',*,*,#7397,.T.);
#5498=ORIENTED_EDGE('',*,*,#7398,.T.);
#5499=ORIENTED_EDGE('',*,*,#7399,.F.);
#5500=ORIENTED_EDGE('',*,*,#7397,.F.);
#5501=ORIENTED_EDGE('',*,*,#7400,.T.);
#5502=ORIENTED_EDGE('',*,*,#7401,.F.);
#5503=ORIENTED_EDGE('',*,*,#7402,.F.);
#5504=ORIENTED_EDGE('',*,*,#7398,.F.);
#5505=ORIENTED_EDGE('',*,*,#7403,.F.);
#5506=ORIENTED_EDGE('',*,*,#7404,.T.);
#5507=ORIENTED_EDGE('',*,*,#7405,.F.);
#5508=ORIENTED_EDGE('',*,*,#7400,.F.);
#5509=ORIENTED_EDGE('',*,*,#7406,.F.);
#5510=ORIENTED_EDGE('',*,*,#7407,.T.);
#5511=ORIENTED_EDGE('',*,*,#7408,.F.);
#5512=ORIENTED_EDGE('',*,*,#7404,.F.);
#5513=ORIENTED_EDGE('',*,*,#7409,.F.);
#5514=ORIENTED_EDGE('',*,*,#7410,.T.);
#5515=ORIENTED_EDGE('',*,*,#7411,.F.);
#5516=ORIENTED_EDGE('',*,*,#7412,.T.);
#5517=ORIENTED_EDGE('',*,*,#7413,.T.);
#5518=ORIENTED_EDGE('',*,*,#7412,.F.);
#5519=ORIENTED_EDGE('',*,*,#7414,.F.);
#5520=ORIENTED_EDGE('',*,*,#7415,.T.);
#5521=ORIENTED_EDGE('',*,*,#7416,.F.);
#5522=ORIENTED_EDGE('',*,*,#7413,.F.);
#5523=ORIENTED_EDGE('',*,*,#7417,.F.);
#5524=ORIENTED_EDGE('',*,*,#7418,.F.);
#5525=ORIENTED_EDGE('',*,*,#7419,.T.);
#5526=ORIENTED_EDGE('',*,*,#7415,.F.);
#5527=ORIENTED_EDGE('',*,*,#7420,.F.);
#5528=ORIENTED_EDGE('',*,*,#7421,.F.);
#5529=ORIENTED_EDGE('',*,*,#7422,.T.);
#5530=ORIENTED_EDGE('',*,*,#7423,.F.);
#5531=ORIENTED_EDGE('',*,*,#7419,.F.);
#5532=ORIENTED_EDGE('',*,*,#7424,.F.);
#5533=ORIENTED_EDGE('',*,*,#7425,.T.);
#5534=ORIENTED_EDGE('',*,*,#7421,.T.);
#5535=ORIENTED_EDGE('',*,*,#7426,.F.);
#5536=ORIENTED_EDGE('',*,*,#7408,.T.);
#5537=ORIENTED_EDGE('',*,*,#7427,.T.);
#5538=ORIENTED_EDGE('',*,*,#7428,.F.);
#5539=ORIENTED_EDGE('',*,*,#7429,.F.);
#5540=ORIENTED_EDGE('',*,*,#7430,.F.);
#5541=ORIENTED_EDGE('',*,*,#7431,.F.);
#5542=ORIENTED_EDGE('',*,*,#7432,.F.);
#5543=ORIENTED_EDGE('',*,*,#7433,.F.);
#5544=ORIENTED_EDGE('',*,*,#7403,.T.);
#5545=ORIENTED_EDGE('',*,*,#7396,.T.);
#5546=ORIENTED_EDGE('',*,*,#7434,.T.);
#5547=ORIENTED_EDGE('',*,*,#7435,.F.);
#5548=ORIENTED_EDGE('',*,*,#7436,.T.);
#5549=ORIENTED_EDGE('',*,*,#7406,.T.);
#5550=ORIENTED_EDGE('',*,*,#7437,.F.);
#5551=ORIENTED_EDGE('',*,*,#7438,.T.);
#5552=ORIENTED_EDGE('',*,*,#7409,.T.);
#5553=ORIENTED_EDGE('',*,*,#7416,.T.);
#5554=ORIENTED_EDGE('',*,*,#7423,.T.);
#5555=ORIENTED_EDGE('',*,*,#7439,.T.);
#5556=ORIENTED_EDGE('',*,*,#7440,.F.);
#5557=ORIENTED_EDGE('',*,*,#7411,.T.);
#5558=ORIENTED_EDGE('',*,*,#7441,.T.);
#5559=ORIENTED_EDGE('',*,*,#7442,.F.);
#5560=ORIENTED_EDGE('',*,*,#7443,.F.);
#5561=ORIENTED_EDGE('',*,*,#7444,.F.);
#5562=ORIENTED_EDGE('',*,*,#7445,.F.);
#5563=ORIENTED_EDGE('',*,*,#7446,.F.);
#5564=ORIENTED_EDGE('',*,*,#7447,.F.);
#5565=ORIENTED_EDGE('',*,*,#7448,.F.);
#5566=ORIENTED_EDGE('',*,*,#7449,.T.);
#5567=ORIENTED_EDGE('',*,*,#7394,.T.);
#5568=ORIENTED_EDGE('',*,*,#7450,.T.);
#5569=ORIENTED_EDGE('',*,*,#7451,.T.);
#5570=ORIENTED_EDGE('',*,*,#7452,.T.);
#5571=ORIENTED_EDGE('',*,*,#7453,.T.);
#5572=ORIENTED_EDGE('',*,*,#7454,.T.);
#5573=ORIENTED_EDGE('',*,*,#7455,.T.);
#5574=ORIENTED_EDGE('',*,*,#7410,.F.);
#5575=ORIENTED_EDGE('',*,*,#7438,.F.);
#5576=ORIENTED_EDGE('',*,*,#7441,.F.);
#5577=ORIENTED_EDGE('',*,*,#7422,.F.);
#5578=ORIENTED_EDGE('',*,*,#7425,.F.);
#5579=ORIENTED_EDGE('',*,*,#7439,.F.);
#5580=ORIENTED_EDGE('',*,*,#7395,.F.);
#5581=ORIENTED_EDGE('',*,*,#7449,.F.);
#5582=ORIENTED_EDGE('',*,*,#7434,.F.);
#5583=ORIENTED_EDGE('',*,*,#7407,.F.);
#5584=ORIENTED_EDGE('',*,*,#7436,.F.);
#5585=ORIENTED_EDGE('',*,*,#7427,.F.);
#5586=ORIENTED_EDGE('',*,*,#7447,.T.);
#5587=ORIENTED_EDGE('',*,*,#7446,.T.);
#5588=ORIENTED_EDGE('',*,*,#7445,.T.);
#5589=ORIENTED_EDGE('',*,*,#7444,.T.);
#5590=ORIENTED_EDGE('',*,*,#7443,.T.);
#5591=ORIENTED_EDGE('',*,*,#7442,.T.);
#5592=ORIENTED_EDGE('',*,*,#7437,.T.);
#5593=ORIENTED_EDGE('',*,*,#7424,.T.);
#5594=ORIENTED_EDGE('',*,*,#7433,.T.);
#5595=ORIENTED_EDGE('',*,*,#7432,.T.);
#5596=ORIENTED_EDGE('',*,*,#7431,.T.);
#5597=ORIENTED_EDGE('',*,*,#7430,.T.);
#5598=ORIENTED_EDGE('',*,*,#7429,.T.);
#5599=ORIENTED_EDGE('',*,*,#7428,.T.);
#5600=ORIENTED_EDGE('',*,*,#7435,.T.);
#5601=ORIENTED_EDGE('',*,*,#7448,.T.);
#5602=ORIENTED_EDGE('',*,*,#7456,.T.);
#5603=ORIENTED_EDGE('',*,*,#7457,.T.);
#5604=ORIENTED_EDGE('',*,*,#7458,.T.);
#5605=ORIENTED_EDGE('',*,*,#7450,.F.);
#5606=ORIENTED_EDGE('',*,*,#7454,.F.);
#5607=ORIENTED_EDGE('',*,*,#7459,.T.);
#5608=ORIENTED_EDGE('',*,*,#7402,.T.);
#5609=ORIENTED_EDGE('',*,*,#7401,.T.);
#5610=ORIENTED_EDGE('',*,*,#7405,.T.);
#5611=ORIENTED_EDGE('',*,*,#7426,.T.);
#5612=ORIENTED_EDGE('',*,*,#7420,.T.);
#5613=ORIENTED_EDGE('',*,*,#7418,.T.);
#5614=ORIENTED_EDGE('',*,*,#7417,.T.);
#5615=ORIENTED_EDGE('',*,*,#7414,.T.);
#5616=ORIENTED_EDGE('',*,*,#7440,.T.);
#5617=ORIENTED_EDGE('',*,*,#7399,.T.);
#5618=ORIENTED_EDGE('',*,*,#7455,.F.);
#5619=ORIENTED_EDGE('',*,*,#7457,.F.);
#5620=ORIENTED_EDGE('',*,*,#7452,.F.);
#5621=ORIENTED_EDGE('',*,*,#7456,.F.);
#5622=ORIENTED_EDGE('',*,*,#7453,.F.);
#5623=ORIENTED_EDGE('',*,*,#7458,.F.);
#5624=ORIENTED_EDGE('',*,*,#7459,.F.);
#5625=ORIENTED_EDGE('',*,*,#7451,.F.);
#7394=EDGE_CURVE('',#8723,#8724,#1149,.F.);
#7395=EDGE_CURVE('',#8723,#8725,#1046,.T.);
#7396=EDGE_CURVE('',#8726,#8725,#1150,.T.);
#7397=EDGE_CURVE('',#8726,#8724,#1151,.F.);
#7398=EDGE_CURVE('',#8726,#8727,#1152,.T.);
#7399=EDGE_CURVE('',#8724,#8727,#1153,.F.);
#7400=EDGE_CURVE('',#8728,#8729,#1154,.F.);
#7401=EDGE_CURVE('',#8730,#8729,#1155,.F.);
#7402=EDGE_CURVE('',#8727,#8730,#1156,.F.);
#7403=EDGE_CURVE('',#8728,#8726,#1157,.T.);
#7404=EDGE_CURVE('',#8728,#8731,#1158,.T.);
#7405=EDGE_CURVE('',#8729,#8731,#1159,.F.);
#7406=EDGE_CURVE('',#8732,#8728,#1160,.T.);
#7407=EDGE_CURVE('',#8732,#8733,#1047,.T.);
#7408=EDGE_CURVE('',#8731,#8733,#1161,.F.);
#7409=EDGE_CURVE('',#8734,#8735,#1162,.T.);
#7410=EDGE_CURVE('',#8734,#8736,#1048,.T.);
#7411=EDGE_CURVE('',#8737,#8736,#1163,.F.);
#7412=EDGE_CURVE('',#8737,#8735,#1164,.F.);
#7413=EDGE_CURVE('',#8738,#8735,#1165,.T.);
#7414=EDGE_CURVE('',#8738,#8737,#1166,.F.);
#7415=EDGE_CURVE('',#8739,#8740,#1167,.F.);
#7416=EDGE_CURVE('',#8735,#8740,#1168,.T.);
#7417=EDGE_CURVE('',#8741,#8738,#1169,.F.);
#7418=EDGE_CURVE('',#8739,#8741,#1170,.F.);
#7419=EDGE_CURVE('',#8742,#8740,#1171,.T.);
#7420=EDGE_CURVE('',#8742,#8739,#1172,.F.);
#7421=EDGE_CURVE('',#8743,#8742,#1173,.F.);
#7422=EDGE_CURVE('',#8743,#8744,#1049,.T.);
#7423=EDGE_CURVE('',#8740,#8744,#1174,.T.);
#7424=EDGE_CURVE('',#8745,#8746,#1175,.T.);
#7425=EDGE_CURVE('',#8745,#8743,#1176,.T.);
#7426=EDGE_CURVE('',#8731,#8742,#1177,.F.);
#7427=EDGE_CURVE('',#8733,#8747,#1178,.T.);
#7428=EDGE_CURVE('',#8748,#8747,#1179,.T.);
#7429=EDGE_CURVE('',#8749,#8748,#1180,.T.);
#7430=EDGE_CURVE('',#8750,#8749,#1181,.T.);
#7431=EDGE_CURVE('',#8751,#8750,#1182,.T.);
#7432=EDGE_CURVE('',#8752,#8751,#1183,.T.);
#7433=EDGE_CURVE('',#8746,#8752,#1184,.T.);
#7434=EDGE_CURVE('',#8725,#8753,#1185,.T.);
#7435=EDGE_CURVE('',#8747,#8753,#1186,.F.);
#7436=EDGE_CURVE('',#8747,#8732,#1187,.T.);
#7437=EDGE_CURVE('',#8754,#8745,#1188,.F.);
#7438=EDGE_CURVE('',#8754,#8734,#1189,.T.);
#7439=EDGE_CURVE('',#8744,#8745,#1190,.T.);
#7440=EDGE_CURVE('',#8737,#8724,#1191,.F.);
#7441=EDGE_CURVE('',#8736,#8754,#1192,.T.);
#7442=EDGE_CURVE('',#8755,#8754,#1193,.T.);
#7443=EDGE_CURVE('',#8756,#8755,#1194,.T.);
#7444=EDGE_CURVE('',#8757,#8756,#1195,.T.);
#7445=EDGE_CURVE('',#8758,#8757,#1196,.T.);
#7446=EDGE_CURVE('',#8759,#8758,#1197,.T.);
#7447=EDGE_CURVE('',#8760,#8759,#1198,.T.);
#7448=EDGE_CURVE('',#8753,#8760,#1199,.T.);
#7449=EDGE_CURVE('',#8753,#8723,#1200,.T.);
#7450=EDGE_CURVE('',#8761,#8761,#1050,.T.);
#7451=EDGE_CURVE('',#8762,#8762,#1051,.T.);
#7452=EDGE_CURVE('',#8763,#8763,#1052,.T.);
#7453=EDGE_CURVE('',#8764,#8764,#1053,.T.);
#7454=EDGE_CURVE('',#8765,#8765,#1054,.T.);
#7455=EDGE_CURVE('',#8766,#8766,#1055,.T.);
#7456=EDGE_CURVE('',#8767,#8767,#1056,.T.);
#7457=EDGE_CURVE('',#8768,#8768,#1057,.T.);
#7458=EDGE_CURVE('',#8769,#8769,#1058,.T.);
#7459=EDGE_CURVE('',#8770,#8770,#1059,.T.);
#8723=VERTEX_POINT('',#41974);
#8724=VERTEX_POINT('',#41975);
#8725=VERTEX_POINT('',#41977);
#8726=VERTEX_POINT('',#41982);
#8727=VERTEX_POINT('',#42005);
#8728=VERTEX_POINT('',#42083);
#8729=VERTEX_POINT('',#42084);
#8730=VERTEX_POINT('',#42089);
#8731=VERTEX_POINT('',#42108);
#8732=VERTEX_POINT('',#42141);
#8733=VERTEX_POINT('',#42143);
#8734=VERTEX_POINT('',#42177);
#8735=VERTEX_POINT('',#42178);
#8736=VERTEX_POINT('',#42180);
#8737=VERTEX_POINT('',#42186);
#8738=VERTEX_POINT('',#42210);
#8739=VERTEX_POINT('',#42260);
#8740=VERTEX_POINT('',#42261);
#8741=VERTEX_POINT('',#42270);
#8742=VERTEX_POINT('',#42284);
#8743=VERTEX_POINT('',#42318);
#8744=VERTEX_POINT('',#42320);
#8745=VERTEX_POINT('',#42952);
#8746=VERTEX_POINT('',#42953);
#8747=VERTEX_POINT('',#43084);
#8748=VERTEX_POINT('',#43117);
#8749=VERTEX_POINT('',#43239);
#8750=VERTEX_POINT('',#43384);
#8751=VERTEX_POINT('',#43519);
#8752=VERTEX_POINT('',#43531);
#8753=VERTEX_POINT('',#43548);
#8754=VERTEX_POINT('',#43562);
#8755=VERTEX_POINT('',#44301);
#8756=VERTEX_POINT('',#44455);
#8757=VERTEX_POINT('',#44467);
#8758=VERTEX_POINT('',#44593);
#8759=VERTEX_POINT('',#44748);
#8760=VERTEX_POINT('',#44760);
#8761=VERTEX_POINT('',#44805);
#8762=VERTEX_POINT('',#44807);
#8763=VERTEX_POINT('',#44810);
#8764=VERTEX_POINT('',#44812);
#8765=VERTEX_POINT('',#44815);
#8766=VERTEX_POINT('',#44817);
#8767=VERTEX_POINT('',#44868);
#8768=VERTEX_POINT('',#44870);
#8769=VERTEX_POINT('',#44873);
#8770=VERTEX_POINT('',#44876);
#11500=EDGE_LOOP('',(#5494,#5495,#5496,#5497));
#11501=EDGE_LOOP('',(#5498,#5499,#5500));
#11502=EDGE_LOOP('',(#5501,#5502,#5503,#5504,#5505));
#11503=EDGE_LOOP('',(#5506,#5507,#5508));
#11504=EDGE_LOOP('',(#5509,#5510,#5511,#5512));
#11505=EDGE_LOOP('',(#5513,#5514,#5515,#5516));
#11506=EDGE_LOOP('',(#5517,#5518,#5519));
#11507=EDGE_LOOP('',(#5520,#5521,#5522,#5523,#5524));
#11508=EDGE_LOOP('',(#5525,#5526,#5527));
#11509=EDGE_LOOP('',(#5528,#5529,#5530,#5531));
#11510=EDGE_LOOP('',(#5532,#5533,#5534,#5535,#5536,#5537,#5538,#5539,#5540,
#5541,#5542,#5543));
#11511=EDGE_LOOP('',(#5544,#5545,#5546,#5547,#5548,#5549));
#11512=EDGE_LOOP('',(#5550,#5551,#5552,#5553,#5554,#5555));
#11513=EDGE_LOOP('',(#5556,#5557,#5558,#5559,#5560,#5561,#5562,#5563,#5564,
#5565,#5566,#5567));
#11514=EDGE_LOOP('',(#5568));
#11515=EDGE_LOOP('',(#5569));
#11516=EDGE_LOOP('',(#5570));
#11517=EDGE_LOOP('',(#5571));
#11518=EDGE_LOOP('',(#5572));
#11519=EDGE_LOOP('',(#5573));
#11520=EDGE_LOOP('',(#5574,#5575,#5576));
#11521=EDGE_LOOP('',(#5577,#5578,#5579));
#11522=EDGE_LOOP('',(#5580,#5581,#5582));
#11523=EDGE_LOOP('',(#5583,#5584,#5585));
#11524=EDGE_LOOP('',(#5586,#5587,#5588,#5589,#5590,#5591,#5592,#5593,#5594,
#5595,#5596,#5597,#5598,#5599,#5600,#5601));
#11525=EDGE_LOOP('',(#5602));
#11526=EDGE_LOOP('',(#5603));
#11527=EDGE_LOOP('',(#5604));
#11528=EDGE_LOOP('',(#5605));
#11529=EDGE_LOOP('',(#5606));
#11530=EDGE_LOOP('',(#5607));
#11531=EDGE_LOOP('',(#5608,#5609,#5610,#5611,#5612,#5613,#5614,#5615,#5616,
#5617));
#11532=EDGE_LOOP('',(#5618));
#11533=EDGE_LOOP('',(#5619));
#11534=EDGE_LOOP('',(#5620));
#11535=EDGE_LOOP('',(#5621));
#11536=EDGE_LOOP('',(#5622));
#11537=EDGE_LOOP('',(#5623));
#11538=EDGE_LOOP('',(#5624));
#11539=EDGE_LOOP('',(#5625));
#12619=FACE_BOUND('',#11500,.T.);
#12620=FACE_BOUND('',#11501,.T.);
#12621=FACE_BOUND('',#11502,.T.);
#12622=FACE_BOUND('',#11503,.T.);
#12623=FACE_BOUND('',#11504,.T.);
#12624=FACE_BOUND('',#11505,.T.);
#12625=FACE_BOUND('',#11506,.T.);
#12626=FACE_BOUND('',#11507,.T.);
#12627=FACE_BOUND('',#11508,.T.);
#12628=FACE_BOUND('',#11509,.T.);
#12629=FACE_BOUND('',#11510,.T.);
#12630=FACE_BOUND('',#11511,.T.);
#12631=FACE_BOUND('',#11512,.T.);
#12632=FACE_BOUND('',#11513,.T.);
#12633=FACE_BOUND('',#11514,.T.);
#12634=FACE_BOUND('',#11515,.T.);
#12635=FACE_BOUND('',#11516,.T.);
#12636=FACE_BOUND('',#11517,.T.);
#12637=FACE_BOUND('',#11518,.T.);
#12638=FACE_BOUND('',#11519,.T.);
#12639=FACE_BOUND('',#11520,.T.);
#12640=FACE_BOUND('',#11521,.T.);
#12641=FACE_BOUND('',#11522,.T.);
#12642=FACE_BOUND('',#11523,.T.);
#12643=FACE_BOUND('',#11524,.T.);
#12644=FACE_BOUND('',#11525,.T.);
#12645=FACE_BOUND('',#11526,.T.);
#12646=FACE_BOUND('',#11527,.T.);
#12647=FACE_BOUND('',#11528,.T.);
#12648=FACE_BOUND('',#11529,.T.);
#12649=FACE_BOUND('',#11530,.T.);
#12650=FACE_BOUND('',#11531,.T.);
#12651=FACE_BOUND('',#11532,.T.);
#12652=FACE_BOUND('',#11533,.T.);
#12653=FACE_BOUND('',#11534,.T.);
#12654=FACE_BOUND('',#11535,.T.);
#12655=FACE_BOUND('',#11536,.T.);
#12656=FACE_BOUND('',#11537,.T.);
#12657=FACE_BOUND('',#11538,.T.);
#12658=FACE_BOUND('',#11539,.T.);
#12697=(
BOUNDED_SURFACE()
B_SPLINE_SURFACE(2,3,((#41945,#41946,#41947,#41948,#41949,#41950,#41951,
#41952),(#41953,#41954,#41955,#41956,#41957,#41958,#41959,#41960),(#41961,
#41962,#41963,#41964,#41965,#41966,#41967,#41968)),.UNSPECIFIED.,.F.,.F.,
 .F.)
B_SPLINE_SURFACE_WITH_KNOTS((3,3),(4,2,2,4),(0.,1.),(5.64528975859604,6.035253330946,
6.23023511712098,6.42521690329596),.UNSPECIFIED.)
GEOMETRIC_REPRESENTATION_ITEM()
RATIONAL_B_SPLINE_SURFACE(((1.,1.,1.,1.,1.,1.,1.,1.),(0.942691264760503,
0.928068462055693,0.9086240744066,0.860023699971551,0.8404696873878,0.79362173087887,
0.766309763902536,0.736695531754573),(1.,1.,1.,1.,1.,1.,1.,1.)))
REPRESENTATION_ITEM('')
SURFACE()
);
#12698=(
BOUNDED_SURFACE()
B_SPLINE_SURFACE(2,3,((#42113,#42114,#42115,#42116,#42117,#42118,#42119,
#42120),(#42121,#42122,#42123,#42124,#42125,#42126,#42127,#42128),(#42129,
#42130,#42131,#42132,#42133,#42134,#42135,#42136)),.UNSPECIFIED.,.F.,.F.,
 .F.)
B_SPLINE_SURFACE_WITH_KNOTS((3,3),(4,2,2,4),(0.,1.),(5.6742522838321,6.06152855173275,
6.25516668568308,6.4488048196334),.UNSPECIFIED.)
GEOMETRIC_REPRESENTATION_ITEM()
RATIONAL_B_SPLINE_SURFACE(((1.,1.,1.,1.,1.,1.,1.,1.),(0.942182847766815,
0.927521546778884,0.908040805109983,0.859614915545788,0.840162397176485,
0.793600157760153,0.766477590108873,0.736968386371289),(1.,1.,1.,1.,1.,
1.,1.,1.)))
REPRESENTATION_ITEM('')
SURFACE()
);
#12699=(
BOUNDED_SURFACE()
B_SPLINE_SURFACE(2,3,((#42149,#42150,#42151,#42152,#42153,#42154,#42155,
#42156),(#42157,#42158,#42159,#42160,#42161,#42162,#42163,#42164),(#42165,
#42166,#42167,#42168,#42169,#42170,#42171,#42172)),.UNSPECIFIED.,.F.,.F.,
 .F.)
B_SPLINE_SURFACE_WITH_KNOTS((3,3),(4,2,2,4),(0.,1.),(5.6738139462659,6.06124835213276,
6.2549655550662,6.44868275799963),.UNSPECIFIED.)
GEOMETRIC_REPRESENTATION_ITEM()
RATIONAL_B_SPLINE_SURFACE(((1.,1.,1.,1.,1.,1.,1.,1.),(0.942306493740219,
0.927647470996889,0.908169604074547,0.859723335117858,0.840259633125994,
0.793659840617052,0.766511109665431,0.736965071389808),(1.,1.,1.,1.,1.,
1.,1.,1.)))
REPRESENTATION_ITEM('')
SURFACE()
);
#12700=(
BOUNDED_SURFACE()
B_SPLINE_SURFACE(2,3,((#42289,#42290,#42291,#42292,#42293,#42294,#42295,
#42296),(#42297,#42298,#42299,#42300,#42301,#42302,#42303,#42304),(#42305,
#42306,#42307,#42308,#42309,#42310,#42311,#42312)),.UNSPECIFIED.,.F.,.F.,
 .F.)
B_SPLINE_SURFACE_WITH_KNOTS((3,3),(4,2,2,4),(0.,1.),(5.64530724788913,6.03520062826121,
6.23014731844725,6.42509400863329),.UNSPECIFIED.)
GEOMETRIC_REPRESENTATION_ITEM()
RATIONAL_B_SPLINE_SURFACE(((1.,1.,1.,1.,1.,1.,1.,1.),(0.942681470688419,
0.928057129687536,0.90861120034166,0.860012856248506,0.840460372376393,
0.793616444798703,0.766307120509746,0.73669216706025),(1.,1.,1.,1.,1.,1.,
1.,1.)))
REPRESENTATION_ITEM('')
SURFACE()
);
#12701=(
BOUNDED_SURFACE()
B_SPLINE_SURFACE(3,2,((#44818,#44819,#44820),(#44821,#44822,#44823),(#44824,
#44825,#44826),(#44827,#44828,#44829)),.UNSPECIFIED.,.F.,.F.,.F.)
B_SPLINE_SURFACE_WITH_KNOTS((4,4),(3,3),(0.0010803423654197,0.00187374355164022),
(0.,1.),.PIECEWISE_BEZIER_KNOTS.)
GEOMETRIC_REPRESENTATION_ITEM()
RATIONAL_B_SPLINE_SURFACE(((1.,0.942306493778178,1.),(1.,0.979942913916364,
1.),(1.,1.00003953052366,1.),(1.,1.,1.)))
REPRESENTATION_ITEM('')
SURFACE()
);
#12702=(
BOUNDED_SURFACE()
B_SPLINE_SURFACE(3,2,((#44830,#44831,#44832),(#44833,#44834,#44835),(#44836,
#44837,#44838),(#44839,#44840,#44841)),.UNSPECIFIED.,.F.,.F.,.F.)
B_SPLINE_SURFACE_WITH_KNOTS((4,4),(3,3),(0.00108592744242376,0.00187664954092587),
(0.,1.),.PIECEWISE_BEZIER_KNOTS.)
GEOMETRIC_REPRESENTATION_ITEM()
RATIONAL_B_SPLINE_SURFACE(((1.,0.942681470709034,1.),(1.,0.980061484884565,
1.),(1.,1.00004724548358,1.),(1.,1.,1.)))
REPRESENTATION_ITEM('')
SURFACE()
);
#12703=(
BOUNDED_SURFACE()
B_SPLINE_SURFACE(3,2,((#44842,#44843,#44844),(#44845,#44846,#44847),(#44848,
#44849,#44850),(#44851,#44852,#44853)),.UNSPECIFIED.,.F.,.F.,.F.)
B_SPLINE_SURFACE_WITH_KNOTS((4,4),(3,3),(0.00108607226657091,0.00187673136426867),
(0.,1.),.PIECEWISE_BEZIER_KNOTS.)
GEOMETRIC_REPRESENTATION_ITEM()
RATIONAL_B_SPLINE_SURFACE(((1.,0.942691264781529,1.),(1.,0.980064039746506,
1.),(1.,1.00004742170994,1.),(1.,1.,1.)))
REPRESENTATION_ITEM('')
SURFACE()
);
#12704=(
BOUNDED_SURFACE()
B_SPLINE_SURFACE(3,2,((#44854,#44855,#44856),(#44857,#44858,#44859),(#44860,
#44861,#44862),(#44863,#44864,#44865)),.UNSPECIFIED.,.F.,.F.,.F.)
B_SPLINE_SURFACE_WITH_KNOTS((4,4),(3,3),(0.00108339687485018,0.00187989260341564),
(0.,1.),.PIECEWISE_BEZIER_KNOTS.)
GEOMETRIC_REPRESENTATION_ITEM()
RATIONAL_B_SPLINE_SURFACE(((1.,0.942182847767366,1.),(1.,0.979809074317455,
1.),(1.,1.00013954302122,1.),(1.,1.,1.)))
REPRESENTATION_ITEM('')
SURFACE()
);
#12705=(
BOUNDED_SURFACE()
B_SPLINE_SURFACE(3,3,((#44877,#44878,#44879,#44880,#44881,#44882,#44883,
#44884,#44885,#44886,#44887,#44888,#44889,#44890,#44891,#44892,#44893,#44894,
#44895,#44896,#44897,#44898,#44899,#44900,#44901,#44902,#44903,#44904,#44905,
#44906,#44907,#44908,#44909,#44910,#44911,#44912,#44913,#44914,#44915,#44916,
#44917,#44918,#44919,#44920,#44921,#44922,#44923,#44924,#44925,#44926,#44927,
#44928,#44929,#44930,#44931,#44932,#44933,#44934,#44935,#44936,#44937,#44938,
#44939,#44940,#44941,#44942,#44943,#44944,#44945,#44946,#44947,#44948,#44949,
#44950,#44951,#44952,#44953,#44954,#44955,#44956,#44957,#44958),(#44959,
#44960,#44961,#44962,#44963,#44964,#44965,#44966,#44967,#44968,#44969,#44970,
#44971,#44972,#44973,#44974,#44975,#44976,#44977,#44978,#44979,#44980,#44981,
#44982,#44983,#44984,#44985,#44986,#44987,#44988,#44989,#44990,#44991,#44992,
#44993,#44994,#44995,#44996,#44997,#44998,#44999,#45000,#45001,#45002,#45003,
#45004,#45005,#45006,#45007,#45008,#45009,#45010,#45011,#45012,#45013,#45014,
#45015,#45016,#45017,#45018,#45019,#45020,#45021,#45022,#45023,#45024,#45025,
#45026,#45027,#45028,#45029,#45030,#45031,#45032,#45033,#45034,#45035,#45036,
#45037,#45038,#45039,#45040),(#45041,#45042,#45043,#45044,#45045,#45046,
#45047,#45048,#45049,#45050,#45051,#45052,#45053,#45054,#45055,#45056,#45057,
#45058,#45059,#45060,#45061,#45062,#45063,#45064,#45065,#45066,#45067,#45068,
#45069,#45070,#45071,#45072,#45073,#45074,#45075,#45076,#45077,#45078,#45079,
#45080,#45081,#45082,#45083,#45084,#45085,#45086,#45087,#45088,#45089,#45090,
#45091,#45092,#45093,#45094,#45095,#45096,#45097,#45098,#45099,#45100,#45101,
#45102,#45103,#45104,#45105,#45106,#45107,#45108,#45109,#45110,#45111,#45112,
#45113,#45114,#45115,#45116,#45117,#45118,#45119,#45120,#45121,#45122),
(#45123,#45124,#45125,#45126,#45127,#45128,#45129,#45130,#45131,#45132,
#45133,#45134,#45135,#45136,#45137,#45138,#45139,#45140,#45141,#45142,#45143,
#45144,#45145,#45146,#45147,#45148,#45149,#45150,#45151,#45152,#45153,#45154,
#45155,#45156,#45157,#45158,#45159,#45160,#45161,#45162,#45163,#45164,#45165,
#45166,#45167,#45168,#45169,#45170,#45171,#45172,#45173,#45174,#45175,#45176,
#45177,#45178,#45179,#45180,#45181,#45182,#45183,#45184,#45185,#45186,#45187,
#45188,#45189,#45190,#45191,#45192,#45193,#45194,#45195,#45196,#45197,#45198,
#45199,#45200,#45201,#45202,#45203,#45204),(#45205,#45206,#45207,#45208,
#45209,#45210,#45211,#45212,#45213,#45214,#45215,#45216,#45217,#45218,#45219,
#45220,#45221,#45222,#45223,#45224,#45225,#45226,#45227,#45228,#45229,#45230,
#45231,#45232,#45233,#45234,#45235,#45236,#45237,#45238,#45239,#45240,#45241,
#45242,#45243,#45244,#45245,#45246,#45247,#45248,#45249,#45250,#45251,#45252,
#45253,#45254,#45255,#45256,#45257,#45258,#45259,#45260,#45261,#45262,#45263,
#45264,#45265,#45266,#45267,#45268,#45269,#45270,#45271,#45272,#45273,#45274,
#45275,#45276,#45277,#45278,#45279,#45280,#45281,#45282,#45283,#45284,#45285,
#45286),(#45287,#45288,#45289,#45290,#45291,#45292,#45293,#45294,#45295,
#45296,#45297,#45298,#45299,#45300,#45301,#45302,#45303,#45304,#45305,#45306,
#45307,#45308,#45309,#45310,#45311,#45312,#45313,#45314,#45315,#45316,#45317,
#45318,#45319,#45320,#45321,#45322,#45323,#45324,#45325,#45326,#45327,#45328,
#45329,#45330,#45331,#45332,#45333,#45334,#45335,#45336,#45337,#45338,#45339,
#45340,#45341,#45342,#45343,#45344,#45345,#45346,#45347,#45348,#45349,#45350,
#45351,#45352,#45353,#45354,#45355,#45356,#45357,#45358,#45359,#45360,#45361,
#45362,#45363,#45364,#45365,#45366,#45367,#45368),(#45369,#45370,#45371,
#45372,#45373,#45374,#45375,#45376,#45377,#45378,#45379,#45380,#45381,#45382,
#45383,#45384,#45385,#45386,#45387,#45388,#45389,#45390,#45391,#45392,#45393,
#45394,#45395,#45396,#45397,#45398,#45399,#45400,#45401,#45402,#45403,#45404,
#45405,#45406,#45407,#45408,#45409,#45410,#45411,#45412,#45413,#45414,#45415,
#45416,#45417,#45418,#45419,#45420,#45421,#45422,#45423,#45424,#45425,#45426,
#45427,#45428,#45429,#45430,#45431,#45432,#45433,#45434,#45435,#45436,#45437,
#45438,#45439,#45440,#45441,#45442,#45443,#45444,#45445,#45446,#45447,#45448,
#45449,#45450)),.UNSPECIFIED.,.F.,.F.,.F.)
B_SPLINE_SURFACE_WITH_KNOTS((4,3,4),(4,2,2,2,2,2,2,2,2,2,2,2,2,2,2,2,2,
2,2,2,2,2,2,2,2,2,2,2,2,2,2,2,2,2,2,2,2,2,2,2,4),(0.786869258805392,1.,
1.21306714374991),(0.,0.00290159839858374,0.0290642712719717,0.0552269441453597,
0.0813896170215754,0.107552289897791,0.133714962774007,0.159877635650223,
0.186040308526438,0.212202981402654,0.23836565427887,0.264528327155085,
0.290691000031301,0.316853672907516,0.343016345783732,0.369179018659948,
0.395341691536163,0.42150436441238,0.447667037288595,0.473829710164811,
0.499992383041026,0.526155055917242,0.552317728793458,0.578480401669673,
0.604643074545889,0.630805747422105,0.656968420298321,0.683131093174536,
0.709293766050752,0.735456438926968,0.761619111803183,0.787781784679399,
0.813944457555615,0.840107130431831,0.866269803308046,0.892432476184262,
0.918595149060478,0.944757821936694,0.970920494812909,0.997083167689125,
1.),.UNSPECIFIED.)
GEOMETRIC_REPRESENTATION_ITEM()
RATIONAL_B_SPLINE_SURFACE(((0.510874737958872,0.510874737958872,0.510874737958872,
0.510874737958872,0.510874737958872,0.510874737958872,0.510874737958872,
0.510874737958872,0.510874737958872,0.510874737958872,0.510874737958872,
0.510874737958872,0.510874737958872,0.510874737958872,0.510874737958872,
0.510874737958872,0.510874737958872,0.510874737958872,0.510874737958872,
0.510874737958872,0.510874737958872,0.510874737958872,0.510874737958872,
0.510874737958872,0.510874737958872,0.510874737958872,0.510874737958872,
0.510874737958872,0.510874737958872,0.510874737958872,0.510874737958872,
0.510874737958872,0.510874737958872,0.510874737958872,0.510874737958872,
0.510874737958872,0.510874737958872,0.510874737958872,0.510874737958872,
0.510874737958872,0.510874737958872,0.510874737958872,0.510874737958872,
0.510874737958872,0.510874737958872,0.510874737958872,0.510874737958872,
0.510874737958872,0.510874737958872,0.510874737958872,0.510874737958872,
0.510874737958872,0.510874737958872,0.510874737958872,0.510874737958872,
0.510874737958872,0.510874737958872,0.510874737958872,0.510874737958872,
0.510874737958872,0.510874737958872,0.510874737958872,0.510874737958872,
0.510874737958872,0.510874737958872,0.510874737958872,0.510874737958872,
0.510874737958872,0.510874737958872,0.510874737958872,0.510874737958872,
0.510874737958872,0.510874737958872,0.510874737958872,0.510874737958872,
0.510874737958872,0.510874737958872,0.510874737958872,0.510874737958872,
0.510874737958872,0.510874737958872,0.510874737958872),(0.552783924393481,
0.552783924393481,0.552783924393481,0.552783924393481,0.552783924393481,
0.552783924393481,0.552783924393481,0.552783924393481,0.552783924393481,
0.552783924393481,0.552783924393481,0.552783924393481,0.552783924393481,
0.552783924393481,0.552783924393481,0.552783924393481,0.552783924393481,
0.552783924393481,0.552783924393481,0.552783924393481,0.552783924393481,
0.552783924393481,0.552783924393481,0.552783924393481,0.552783924393481,
0.552783924393481,0.552783924393481,0.552783924393481,0.552783924393481,
0.552783924393481,0.552783924393481,0.552783924393481,0.552783924393481,
0.552783924393481,0.552783924393481,0.552783924393481,0.552783924393481,
0.552783924393481,0.552783924393481,0.552783924393481,0.552783924393481,
0.552783924393481,0.552783924393481,0.552783924393481,0.552783924393481,
0.552783924393481,0.552783924393481,0.552783924393481,0.552783924393481,
0.552783924393481,0.552783924393481,0.552783924393481,0.552783924393481,
0.552783924393481,0.552783924393481,0.552783924393481,0.552783924393481,
0.552783924393481,0.552783924393481,0.552783924393481,0.552783924393481,
0.552783924393481,0.552783924393481,0.552783924393481,0.552783924393481,
0.552783924393481,0.552783924393481,0.552783924393481,0.552783924393481,
0.552783924393481,0.552783924393481,0.552783924393481,0.552783924393481,
0.552783924393481,0.552783924393481,0.552783924393481,0.552783924393481,
0.552783924393481,0.552783924393481,0.552783924393481,0.552783924393481,
0.552783924393481),(0.71582567840719,0.71582567840719,0.71582567840719,
0.71582567840719,0.71582567840719,0.71582567840719,0.71582567840719,0.71582567840719,
0.71582567840719,0.71582567840719,0.71582567840719,0.71582567840719,0.71582567840719,
0.71582567840719,0.71582567840719,0.71582567840719,0.71582567840719,0.71582567840719,
0.71582567840719,0.71582567840719,0.71582567840719,0.71582567840719,0.71582567840719,
0.71582567840719,0.71582567840719,0.71582567840719,0.71582567840719,0.71582567840719,
0.71582567840719,0.71582567840719,0.71582567840719,0.71582567840719,0.71582567840719,
0.71582567840719,0.71582567840719,0.71582567840719,0.71582567840719,0.71582567840719,
0.71582567840719,0.71582567840719,0.71582567840719,0.71582567840719,0.71582567840719,
0.71582567840719,0.71582567840719,0.71582567840719,0.71582567840719,0.71582567840719,
0.71582567840719,0.71582567840719,0.71582567840719,0.71582567840719,0.71582567840719,
0.71582567840719,0.71582567840719,0.71582567840719,0.71582567840719,0.71582567840719,
0.71582567840719,0.71582567840719,0.71582567840719,0.71582567840719,0.71582567840719,
0.71582567840719,0.71582567840719,0.71582567840719,0.71582567840719,0.71582567840719,
0.71582567840719,0.71582567840719,0.71582567840719,0.71582567840719,0.71582567840719,
0.71582567840719,0.71582567840719,0.71582567840719,0.71582567840719,0.71582567840719,
0.71582567840719,0.71582567840719,0.71582567840719,0.71582567840719),(1.,
1.,1.,1.,1.,1.,1.,1.,1.,1.,1.,1.,1.,1.,1.,1.,1.,1.,1.,1.,1.,1.,1.,1.,1.,
1.,1.,1.,1.,1.,1.,1.,1.,1.,1.,1.,1.,1.,1.,1.,1.,1.,1.,1.,1.,1.,1.,1.,1.,
1.,1.,1.,1.,1.,1.,1.,1.,1.,1.,1.,1.,1.,1.,1.,1.,1.,1.,1.,1.,1.,1.,1.,1.,
1.,1.,1.,1.,1.,1.,1.,1.,1.),(0.715910475000114,0.715910475000114,0.715910475000114,
0.715910475000114,0.715910475000114,0.715910475000114,0.715910475000114,
0.715910475000114,0.715910475000114,0.715910475000114,0.715910475000114,
0.715910475000114,0.715910475000114,0.715910475000114,0.715910475000114,
0.715910475000114,0.715910475000114,0.715910475000114,0.715910475000114,
0.715910475000114,0.715910475000114,0.715910475000114,0.715910475000114,
0.715910475000114,0.715910475000114,0.715910475000114,0.715910475000114,
0.715910475000114,0.715910475000114,0.715910475000114,0.715910475000114,
0.715910475000114,0.715910475000114,0.715910475000114,0.715910475000114,
0.715910475000114,0.715910475000114,0.715910475000114,0.715910475000114,
0.715910475000114,0.715910475000114,0.715910475000114,0.715910475000114,
0.715910475000114,0.715910475000114,0.715910475000114,0.715910475000114,
0.715910475000114,0.715910475000114,0.715910475000114,0.715910475000114,
0.715910475000114,0.715910475000114,0.715910475000114,0.715910475000114,
0.715910475000114,0.715910475000114,0.715910475000114,0.715910475000114,
0.715910475000114,0.715910475000114,0.715910475000114,0.715910475000114,
0.715910475000114,0.715910475000114,0.715910475000114,0.715910475000114,
0.715910475000114,0.715910475000114,0.715910475000114,0.715910475000114,
0.715910475000114,0.715910475000114,0.715910475000114,0.715910475000114,
0.715910475000114,0.715910475000114,0.715910475000114,0.715910475000114,
0.715910475000114,0.715910475000114,0.715910475000114),(0.552881237322219,
0.552881237322219,0.552881237322219,0.552881237322219,0.552881237322219,
0.552881237322219,0.552881237322219,0.552881237322219,0.552881237322219,
0.552881237322219,0.552881237322219,0.552881237322219,0.552881237322219,
0.552881237322219,0.552881237322219,0.552881237322219,0.552881237322219,
0.552881237322219,0.552881237322219,0.552881237322219,0.552881237322219,
0.552881237322219,0.552881237322219,0.552881237322219,0.552881237322219,
0.552881237322219,0.552881237322219,0.552881237322219,0.552881237322219,
0.552881237322219,0.552881237322219,0.552881237322219,0.552881237322219,
0.552881237322219,0.552881237322219,0.552881237322219,0.552881237322219,
0.552881237322219,0.552881237322219,0.552881237322219,0.552881237322219,
0.552881237322219,0.552881237322219,0.552881237322219,0.552881237322219,
0.552881237322219,0.552881237322219,0.552881237322219,0.552881237322219,
0.552881237322219,0.552881237322219,0.552881237322219,0.552881237322219,
0.552881237322219,0.552881237322219,0.552881237322219,0.552881237322219,
0.552881237322219,0.552881237322219,0.552881237322219,0.552881237322219,
0.552881237322219,0.552881237322219,0.552881237322219,0.552881237322219,
0.552881237322219,0.552881237322219,0.552881237322219,0.552881237322219,
0.552881237322219,0.552881237322219,0.552881237322219,0.552881237322219,
0.552881237322219,0.552881237322219,0.552881237322219,0.552881237322219,
0.552881237322219,0.552881237322219,0.552881237322219,0.552881237322219,
0.552881237322219),(0.510912286966316,0.510912286966316,0.510912286966316,
0.510912286966316,0.510912286966316,0.510912286966316,0.510912286966316,
0.510912286966316,0.510912286966316,0.510912286966316,0.510912286966316,
0.510912286966316,0.510912286966316,0.510912286966316,0.510912286966316,
0.510912286966316,0.510912286966316,0.510912286966316,0.510912286966316,
0.510912286966316,0.510912286966316,0.510912286966316,0.510912286966316,
0.510912286966316,0.510912286966316,0.510912286966316,0.510912286966316,
0.510912286966316,0.510912286966316,0.510912286966316,0.510912286966316,
0.510912286966316,0.510912286966316,0.510912286966316,0.510912286966316,
0.510912286966316,0.510912286966316,0.510912286966316,0.510912286966316,
0.510912286966316,0.510912286966316,0.510912286966316,0.510912286966316,
0.510912286966316,0.510912286966316,0.510912286966316,0.510912286966316,
0.510912286966316,0.510912286966316,0.510912286966316,0.510912286966316,
0.510912286966316,0.510912286966316,0.510912286966316,0.510912286966316,
0.510912286966316,0.510912286966316,0.510912286966316,0.510912286966316,
0.510912286966316,0.510912286966316,0.510912286966316,0.510912286966316,
0.510912286966316,0.510912286966316,0.510912286966316,0.510912286966316,
0.510912286966316,0.510912286966316,0.510912286966316,0.510912286966316,
0.510912286966316,0.510912286966316,0.510912286966316,0.510912286966316,
0.510912286966316,0.510912286966316,0.510912286966316,0.510912286966316,
0.510912286966316,0.510912286966316,0.510912286966316)))
REPRESENTATION_ITEM('')
SURFACE()
);
#13471=ADVANCED_FACE('',(#12619),#12697,.F.);
#13472=ADVANCED_FACE('',(#12620),#18,.F.);
#13473=ADVANCED_FACE('',(#12621),#56,.F.);
#13474=ADVANCED_FACE('',(#12622),#19,.F.);
#13475=ADVANCED_FACE('',(#12623),#12698,.F.);
#13476=ADVANCED_FACE('',(#12624),#12699,.F.);
#13477=ADVANCED_FACE('',(#12625),#1819,.F.);
#13478=ADVANCED_FACE('',(#12626),#57,.F.);
#13479=ADVANCED_FACE('',(#12627),#20,.F.);
#13480=ADVANCED_FACE('',(#12628),#12700,.F.);
#13481=ADVANCED_FACE('',(#12629),#58,.T.);
#13482=ADVANCED_FACE('',(#12630),#1820,.T.);
#13483=ADVANCED_FACE('',(#12631),#1821,.T.);
#13484=ADVANCED_FACE('',(#12632),#59,.T.);
#13485=ADVANCED_FACE('',(#12633,#12634),#1535,.F.);
#13486=ADVANCED_FACE('',(#12635,#12636),#1536,.F.);
#13487=ADVANCED_FACE('',(#12637,#12638),#1537,.F.);
#13488=ADVANCED_FACE('',(#12639),#12701,.F.);
#13489=ADVANCED_FACE('',(#12640),#12702,.F.);
#13490=ADVANCED_FACE('',(#12641),#12703,.F.);
#13491=ADVANCED_FACE('',(#12642),#12704,.F.);
#13492=ADVANCED_FACE('',(#12643,#12644,#12645),#1822,.F.);
#13493=ADVANCED_FACE('',(#12646,#12647),#1823,.F.);
#13494=ADVANCED_FACE('',(#12648,#12649),#1824,.T.);
#13495=ADVANCED_FACE('',(#12650),#12705,.F.);
#13496=ADVANCED_FACE('',(#12651,#12652),#332,.T.);
#13497=ADVANCED_FACE('',(#12653,#12654),#333,.F.);
#13498=ADVANCED_FACE('',(#12655,#12656),#334,.T.);
#13499=ADVANCED_FACE('',(#12657,#12658),#335,.T.);
#13527=CLOSED_SHELL('',(#13471,#13472,#13473,#13474,#13475,#13476,#13477,
#13478,#13479,#13480,#13481,#13482,#13483,#13484,#13485,#13486,#13487,#13488,
#13489,#13490,#13491,#13492,#13493,#13494,#13495,#13496,#13497,#13498,#13499));
#13554=STYLED_ITEM('',(#13581),#13744);
#13581=PRESENTATION_STYLE_ASSIGNMENT((#13608));
#13608=SURFACE_STYLE_USAGE(.BOTH.,#13635);
#13635=SURFACE_SIDE_STYLE('',(#13662));
#13662=SURFACE_STYLE_FILL_AREA(#13689);
#13689=FILL_AREA_STYLE('',(#13716));
#13716=FILL_AREA_STYLE_COLOUR('',#60);
#13744=MANIFOLD_SOLID_BREP('Bottle_Cap',#13527);
#13772=SHAPE_DEFINITION_REPRESENTATION(#45581,#13800);
#13800=SHAPE_REPRESENTATION('Bottle_Cap',(#13802),#45490);
#13802=AXIS2_PLACEMENT_3D('',#19109,#15295,#15296);
#15259=AXIS2_PLACEMENT_3D('',#41976,#19037,#19038);
#15260=AXIS2_PLACEMENT_3D('',#41991,#19039,#19040);
#15261=AXIS2_PLACEMENT_3D('',#42098,#19041,#19042);
#15262=AXIS2_PLACEMENT_3D('',#42142,#19043,#19044);
#15263=AXIS2_PLACEMENT_3D('',#42179,#19045,#19046);
#15264=AXIS2_PLACEMENT_3D('',#42199,#19047,#19048);
#15265=AXIS2_PLACEMENT_3D('',#42275,#19049,#19050);
#15266=AXIS2_PLACEMENT_3D('',#42319,#19051,#19052);
#15267=AXIS2_PLACEMENT_3D('',#43543,#19053,#19054);
#15268=AXIS2_PLACEMENT_3D('',#43557,#19055,#19056);
#15269=AXIS2_PLACEMENT_3D('',#44803,#19057,#19058);
#15270=AXIS2_PLACEMENT_3D('',#44804,#19059,#19060);
#15271=AXIS2_PLACEMENT_3D('',#44806,#19061,#19062);
#15272=AXIS2_PLACEMENT_3D('',#44808,#19063,#19064);
#15273=AXIS2_PLACEMENT_3D('',#44809,#19065,#19066);
#15274=AXIS2_PLACEMENT_3D('',#44811,#19067,#19068);
#15275=AXIS2_PLACEMENT_3D('',#44813,#19069,#19070);
#15276=AXIS2_PLACEMENT_3D('',#44814,#19071,#19072);
#15277=AXIS2_PLACEMENT_3D('',#44816,#19073,#19074);
#15278=AXIS2_PLACEMENT_3D('',#44866,#19075,#19076);
#15279=AXIS2_PLACEMENT_3D('',#44867,#19077,#19078);
#15280=AXIS2_PLACEMENT_3D('',#44869,#19079,#19080);
#15281=AXIS2_PLACEMENT_3D('',#44871,#19081,#19082);
#15282=AXIS2_PLACEMENT_3D('',#44872,#19083,#19084);
#15283=AXIS2_PLACEMENT_3D('',#44874,#19085,#19086);
#15284=AXIS2_PLACEMENT_3D('',#44875,#19087,#19088);
#15285=AXIS2_PLACEMENT_3D('',#45451,#19089,#19090);
#15286=AXIS2_PLACEMENT_3D('',#45452,#19091,#19092);
#15287=AXIS2_PLACEMENT_3D('',#45453,#19093,#19094);
#15288=AXIS2_PLACEMENT_3D('',#45454,#19095,#19096);
#15295=DIRECTION('',(0.,0.,1.));
#15296=DIRECTION('',(1.,0.,0.));
#19037=DIRECTION('',(-0.692749665477858,0.211756051343751,0.689389059747556));
#19038=DIRECTION('',(0.647043889936958,0.604649334921695,0.46447108227962));
#19039=DIRECTION('',(1.,0.,0.));
#19040=DIRECTION('',(0.,0.,-1.));
#19041=DIRECTION('',(1.,0.,0.));
#19042=DIRECTION('',(0.,0.,-1.));
#19043=DIRECTION('',(-0.718059051153575,0.231804019712156,-0.656245453699845));
#19044=DIRECTION('',(0.297719501993842,0.954585044452634,0.0114232674791869));
#19045=DIRECTION('',(0.232156425308651,-0.717834774122639,0.656366232562437));
#19046=DIRECTION('',(0.954423306777422,0.298238056715909,-0.0114110913750513));
#19047=DIRECTION('',(-0.414036995247424,-0.847901151391589,0.331114789816619));
#19048=DIRECTION('',(0.898590191828426,-0.43878886397646,0.));
#19049=DIRECTION('',(1.,0.,0.));
#19050=DIRECTION('',(0.,0.,-1.));
#19051=DIRECTION('',(0.211730516675233,-0.692753880604064,-0.689392666929703));
#19052=DIRECTION('',(0.604625619479393,0.647043750571463,-0.464502147589842));
#19053=DIRECTION('',(-0.0179186792471205,0.0175760353025328,-0.999684952331025));
#19054=DIRECTION('',(-0.999839397961794,0.,0.0179214475809965));
#19055=DIRECTION('',(-0.0175715912801442,0.0178848093900984,-0.999685636974426));
#19056=DIRECTION('',(0.,0.999840004600917,0.0178875710938518));
#19057=DIRECTION('',(0.,0.,-1.));
#19058=DIRECTION('',(-1.,0.,0.));
#19059=DIRECTION('',(0.,0.,-1.));
#19060=DIRECTION('',(-1.,0.,0.));
#19061=DIRECTION('',(0.,0.,1.));
#19062=DIRECTION('',(-1.,0.,0.));
#19063=DIRECTION('',(0.,0.,1.));
#19064=DIRECTION('',(1.,0.,0.));
#19065=DIRECTION('',(0.,0.,-1.));
#19066=DIRECTION('',(1.,0.,0.));
#19067=DIRECTION('',(0.,0.,1.));
#19068=DIRECTION('',(1.,0.,0.));
#19069=DIRECTION('',(0.,0.,1.));
#19070=DIRECTION('',(1.,0.,0.));
#19071=DIRECTION('',(0.,0.,-1.));
#19072=DIRECTION('',(-1.,0.,0.));
#19073=DIRECTION('',(0.,0.,1.));
#19074=DIRECTION('',(1.,0.,0.));
#19075=DIRECTION('',(0.,0.,-1.));
#19076=DIRECTION('',(-1.,0.,0.));
#19077=DIRECTION('',(0.,0.,1.));
#19078=DIRECTION('',(1.,0.,0.));
#19079=DIRECTION('',(0.,0.,-1.));
#19080=DIRECTION('',(1.,0.,0.));
#19081=DIRECTION('',(0.,0.,-1.));
#19082=DIRECTION('',(-1.,0.,0.));
#19083=DIRECTION('',(0.,0.,-1.));
#19084=DIRECTION('',(1.,0.,0.));
#19085=DIRECTION('',(0.,0.,-1.));
#19086=DIRECTION('',(-1.,0.,0.));
#19087=DIRECTION('',(0.,0.,-1.));
#19088=DIRECTION('',(-1.,0.,0.));
#19089=DIRECTION('',(0.,0.,1.));
#19090=DIRECTION('',(1.,0.,0.));
#19091=DIRECTION('',(0.,0.,1.));
#19092=DIRECTION('',(1.,0.,0.));
#19093=DIRECTION('',(0.,0.,1.));
#19094=DIRECTION('',(1.,0.,0.));
#19095=DIRECTION('',(0.,0.,-1.));
#19096=DIRECTION('',(-1.,0.,0.));
#19109=CARTESIAN_POINT('',(0.,0.,0.));
#41945=CARTESIAN_POINT('',(0.0135274197783234,0.0136559722321699,0.044681301720925));
#41946=CARTESIAN_POINT('',(0.0135383476416825,0.0136533363661855,0.0446112569865791));
#41947=CARTESIAN_POINT('',(0.0135507663442154,0.0136510730091971,0.0445355922223623));
#41948=CARTESIAN_POINT('',(0.0135793099051906,0.0136514390447496,0.0443921469902879));
#41949=CARTESIAN_POINT('',(0.0135905144371587,0.0136521608730817,0.0443390104257923));
#41950=CARTESIAN_POINT('',(0.0136202080437242,0.0136581861183181,0.0442206495600809));
#41951=CARTESIAN_POINT('',(0.0136379804308225,0.0136624072587615,0.0441533771102119));
#41952=CARTESIAN_POINT('',(0.0136649436921374,0.0136770530453923,0.0440953250454317));
#41953=CARTESIAN_POINT('',(0.0137591216979031,0.0135793490080381,0.0449376690887614));
#41954=CARTESIAN_POINT('',(0.0137955294557406,0.0135840244482818,0.044914581390673));
#41955=CARTESIAN_POINT('',(0.0138333620004707,0.0135966273451604,0.04489665312379));
#41956=CARTESIAN_POINT('',(0.0138821413352717,0.0136375372183026,0.0448929276695706));
#41957=CARTESIAN_POINT('',(0.0138977270969142,0.0136560593344022,0.0448960471700173));
#41958=CARTESIAN_POINT('',(0.0139209788879496,0.0137061451050335,0.0449176882817704));
#41959=CARTESIAN_POINT('',(0.0139284648226078,0.0137390765639426,0.0449375945732147));
#41960=CARTESIAN_POINT('',(0.0139245922828118,0.0137803595242899,0.0449696705691722));
#41961=CARTESIAN_POINT('',(0.0138718493710985,0.0133075760157319,0.0451344253785385));
#41962=CARTESIAN_POINT('',(0.0139238880279802,0.0132619733864548,0.0451212971220347));
#41963=CARTESIAN_POINT('',(0.0139802559536868,0.0132132977462015,0.0451071500355097));
#41964=CARTESIAN_POINT('',(0.0140916894400597,0.0131247754923386,0.0450799876902406));
#41965=CARTESIAN_POINT('',(0.0141335589045852,0.0130924063246476,0.0450698729824398));
#41966=CARTESIAN_POINT('',(0.0142313592568437,0.01302462045826,0.0450470959743368));
#41967=CARTESIAN_POINT('',(0.0142878782764567,0.0129864541955381,0.0450340100292577));
#41968=CARTESIAN_POINT('',(0.014346765827375,0.0129670186229265,0.0450227345929722));
#41969=CARTESIAN_POINT('',(0.014346765827375,0.0129670186229265,0.0450227345929722));
#41970=CARTESIAN_POINT('',(0.0142289907255384,0.0130058897681498,0.0450452854655432));
#41971=CARTESIAN_POINT('',(0.0140326505124449,0.0131746342432835,0.0450947923168716));
#41972=CARTESIAN_POINT('',(0.0139238880279802,0.0132619733864548,0.0451212971220347));
#41973=CARTESIAN_POINT('',(0.0138718493710985,0.0133075760157319,0.0451344253785385));
#41974=CARTESIAN_POINT('',(0.0138718493710985,0.0133075760157319,0.0451344253785385));
#41975=CARTESIAN_POINT('',(0.014346765827375,0.0129670186229265,0.0450227345929722));
#41976=CARTESIAN_POINT('',(0.0132248054813652,0.0127029266810005,0.0446699542964051));
#41977=CARTESIAN_POINT('',(0.0135274197783234,0.0136559722321699,0.044681301720925));
#41978=CARTESIAN_POINT('',(0.0136653071058316,0.0136772649389237,0.0440945308487834));
#41979=CARTESIAN_POINT('',(0.0136256373571829,0.0136555971622692,0.0441800375577949));
#41980=CARTESIAN_POINT('',(0.0135751070889845,0.0136444699217395,0.0443756388757358));
#41981=CARTESIAN_POINT('',(0.0135274210106334,0.0136559761133743,0.0446813017670743));
#41982=CARTESIAN_POINT('',(0.0136658374374733,0.0136775045728404,0.0440948376110462));
#41983=CARTESIAN_POINT('',(0.0143467558525134,0.0129670108776811,0.0450226952968607));
#41984=CARTESIAN_POINT('',(0.0143015465745449,0.0130541036653512,0.0450170051989192));
#41985=CARTESIAN_POINT('',(0.0141568573863817,0.0132997211390049,0.0449524875713156));
#41986=CARTESIAN_POINT('',(0.0140077224005055,0.0134863714630881,0.0447938026846776));
#41987=CARTESIAN_POINT('',(0.0138687740643729,0.0136139860601651,0.044580075342522));
#41988=CARTESIAN_POINT('',(0.01377445274251,0.0136755825517951,0.0444016168251007));
#41989=CARTESIAN_POINT('',(0.0136973975352464,0.0136900403740722,0.0442047157383087));
#41990=CARTESIAN_POINT('',(0.0136648649317818,0.0136771029055344,0.0440951738724241));
#41991=CARTESIAN_POINT('',(0.014105046329742,0.0127793291184313,0.0440704771345536));
#41992=CARTESIAN_POINT('',(0.0136667248958405,0.0136780328466249,0.0440944206993372));
#41993=CARTESIAN_POINT('',(0.0136861745689291,0.0136861421671065,0.0441460977181257));
#41994=CARTESIAN_POINT('',(0.0137287539986456,0.0136962243778536,0.0442503416155328));
#41995=CARTESIAN_POINT('',(0.0138254982236743,0.0136720093947,0.044436272884352));
#41996=CARTESIAN_POINT('',(0.013894272333865,0.0136395602741699,0.0445501271419491));
#41997=CARTESIAN_POINT('',(0.0140067954073001,0.0135525740966713,0.0447011391172071));
#41998=CARTESIAN_POINT('',(0.0140483773118853,0.0135136202857098,0.0447487234029328));
#41999=CARTESIAN_POINT('',(0.0141167481244794,0.0134440767451732,0.04482159174837));
#42000=CARTESIAN_POINT('',(0.0141793305834479,0.0133692749075648,0.0448758648631172));
#42001=CARTESIAN_POINT('',(0.0142269874670527,0.0133090276484192,0.0449131690072696));
#42002=CARTESIAN_POINT('',(0.0143333169163945,0.013155955993812,0.0449771088685464));
#42003=CARTESIAN_POINT('',(0.0143845245824868,0.0130657505275901,0.044988523237714));
#42004=CARTESIAN_POINT('',(0.0144087800451138,0.0130212016472391,0.0449922205233206));
#42005=CARTESIAN_POINT('',(0.0144088164060123,0.0130212306025444,0.0449923308680604));
#42006=CARTESIAN_POINT('',(0.0144087800451138,0.0130212016472391,0.0449922205233206));
#42007=CARTESIAN_POINT('',(0.0143883014579014,0.0130038037933579,0.0450035339760893));
#42008=CARTESIAN_POINT('',(0.0143676124044562,0.0129856909365987,0.0450137192723785));
#42009=CARTESIAN_POINT('',(0.0143467558525134,0.0129670108776811,0.0450226952968608));
#42010=CARTESIAN_POINT('',(0.0143543358721172,0.0129734997731774,0.0450223912595732));
#42011=CARTESIAN_POINT('',(0.0142498869604617,0.0131740311774407,0.0450086019078322));
#42012=CARTESIAN_POINT('',(0.0141071842607483,0.0133876340631727,0.0449084250872999));
#42013=CARTESIAN_POINT('',(0.0138413738506828,0.0136573423337213,0.0445489378073578));
#42014=CARTESIAN_POINT('',(0.0137286338022633,0.0137025434390836,0.0443029940318597));
#42015=CARTESIAN_POINT('',(0.0136626755570935,0.0136761558919233,0.0440873901519572));
#42016=CARTESIAN_POINT('',(0.0145100291225004,0.013109903869032,0.0449364853455191));
#42017=CARTESIAN_POINT('',(0.0143981204627331,0.0132993225006228,0.0449155041230904));
#42018=CARTESIAN_POINT('',(0.0142374830299031,0.0134883269982029,0.0448187565584134));
#42019=CARTESIAN_POINT('',(0.0139151016581816,0.0137039062309166,0.0444926329796269));
#42020=CARTESIAN_POINT('',(0.0137645876753501,0.013722544285296,0.0442739751078847));
#42021=CARTESIAN_POINT('',(0.0136641876361022,0.0136770327619371,0.0440804304725095));
#42022=CARTESIAN_POINT('',(0.0146565930206288,0.0132401123010691,0.0448110693510974));
#42023=CARTESIAN_POINT('',(0.0145353397028751,0.0134178028227805,0.0447873548684827));
#42024=CARTESIAN_POINT('',(0.0143562676911,0.0135837736709856,0.0447005316646434));
#42025=CARTESIAN_POINT('',(0.0139812259277474,0.0137490376643148,0.0444203306717967));
#42026=CARTESIAN_POINT('',(0.0137970658203665,0.0137425238909612,0.0442352488688624));
#42027=CARTESIAN_POINT('',(0.0136655812754718,0.0136779519004114,0.0440700642907236));
#42028=CARTESIAN_POINT('',(0.0148561869420901,0.0134245298225879,0.0444401372985064));
#42029=CARTESIAN_POINT('',(0.0147202361893934,0.0135851348071275,0.0444253746420989));
#42030=CARTESIAN_POINT('',(0.014514736203999,0.0137195113669646,0.0443775701105716));
#42031=CARTESIAN_POINT('',(0.0140682376951201,0.0138148735734959,0.0442272197318363));
#42032=CARTESIAN_POINT('',(0.0138397494067089,0.0137724753618642,0.0441285697805939));
#42033=CARTESIAN_POINT('',(0.0136672108305557,0.0136795271082228,0.0440391292696259));
#42034=CARTESIAN_POINT('',(0.0149102056749342,0.0134789301609788,0.0442095873452684));
#42035=CARTESIAN_POINT('',(0.0147697219839977,0.0136345088744832,0.0442047360754924));
#42036=CARTESIAN_POINT('',(0.0145566753949533,0.0137600265713512,0.044183579961384));
#42037=CARTESIAN_POINT('',(0.01409085414887,0.0138352218867532,0.0441124227906861));
#42038=CARTESIAN_POINT('',(0.0138507650317711,0.0137820491623528,0.0440642589994173));
#42039=CARTESIAN_POINT('',(0.0136674754888846,0.0136801592884,0.0440198285274441));
#42040=CARTESIAN_POINT('',(0.0149021535947794,0.0134874946220255,0.0437414750071867));
#42041=CARTESIAN_POINT('',(0.0147620013685623,0.0136426853747751,0.043756733998497));
#42042=CARTESIAN_POINT('',(0.0145498776236904,0.013767193588292,0.0437896627013868));
#42043=CARTESIAN_POINT('',(0.0140868194117618,0.0138394359615844,0.0438793233746439));
#42044=CARTESIAN_POINT('',(0.0138484956243084,0.0137843974750378,0.0439336850792973));
#42045=CARTESIAN_POINT('',(0.0136667755709176,0.013680850707678,0.0439806208483835));
#42046=CARTESIAN_POINT('',(0.0148408481024395,0.0134420273546197,0.0435127120710071));
#42047=CARTESIAN_POINT('',(0.0147055074066387,0.0136018084704029,0.0435378464395097));
#42048=CARTESIAN_POINT('',(0.0145017549573871,0.0137340910675512,0.0435972739054557));
#42049=CARTESIAN_POINT('',(0.0140605129996015,0.0138234042994072,0.0437655308068245));
#42050=CARTESIAN_POINT('',(0.0138353874056037,0.013777210507569,0.0438699383119697));
#42051=CARTESIAN_POINT('',(0.0136658319590425,0.0136809004841067,0.0439614578877055));
#42052=CARTESIAN_POINT('',(0.0146288177262632,0.013271447945054,0.0431420114315051));
#42053=CARTESIAN_POINT('',(0.0145084480711531,0.0134479229339361,0.0431762790242411));
#42054=CARTESIAN_POINT('',(0.0143324238504282,0.0136102716028767,0.0432749864733467));
#42055=CARTESIAN_POINT('',(0.0139669857610103,0.0137646036720782,0.0435731045341093));
#42056=CARTESIAN_POINT('',(0.0137890792080722,0.0137511116143412,0.0437636448274475));
#42057=CARTESIAN_POINT('',(0.013663097969023,0.0136804172320355,0.0439304809596632));
#42058=CARTESIAN_POINT('',(0.0144769486791919,0.013145005762609,0.0430154533168616));
#42059=CARTESIAN_POINT('',(0.0143659106593811,0.0133333811663706,0.0430471596869001));
#42060=CARTESIAN_POINT('',(0.0142088058302736,0.0135185141682279,0.0431561613858893));
#42061=CARTESIAN_POINT('',(0.0138979585191121,0.0137217698081853,0.0435006909193419));
#42062=CARTESIAN_POINT('',(0.0137550537397556,0.0137323746885259,0.0437248623853491));
#42063=CARTESIAN_POINT('',(0.0136613139372126,0.0136798578520549,0.0439199607480119));
#42064=CARTESIAN_POINT('',(0.0143182670268424,0.013011683094371,0.0429304918108316));
#42065=CARTESIAN_POINT('',(0.0142144398487442,0.0132114126772654,0.0429551488197019));
#42066=CARTESIAN_POINT('',(0.0140753928366151,0.0134210089472879,0.0430678050943401));
#42067=CARTESIAN_POINT('',(0.0138222829792609,0.013677197407846,0.0434455292881368));
#42068=CARTESIAN_POINT('',(0.0137181015819516,0.0137133992748758,0.0436965210630945));
#42069=CARTESIAN_POINT('',(0.0136595668833152,0.0136792312485303,0.0439130710733126));
#42070=CARTESIAN_POINT('',(0.0143722462106869,0.0130570322249862,0.0429594753784009));
#42071=CARTESIAN_POINT('',(0.0143488177373289,0.0131002062692814,0.0429654421756892));
#42072=CARTESIAN_POINT('',(0.0143064663956776,0.0131728485372548,0.0429817556535115));
#42073=CARTESIAN_POINT('',(0.0142441468438431,0.013269940183715,0.0430178358493532));
#42074=CARTESIAN_POINT('',(0.014176653268755,0.0133632559502267,0.0430702966139033));
#42075=CARTESIAN_POINT('',(0.0141597634282231,0.0133851885762827,0.0430845337421948));
#42076=CARTESIAN_POINT('',(0.0140819711780693,0.0134790357196756,0.0431602339511191));
#42077=CARTESIAN_POINT('',(0.0140279139033517,0.0135334375005743,0.0432248312851544));
#42078=CARTESIAN_POINT('',(0.0139771134946773,0.0135816930189672,0.0432884874805865));
#42079=CARTESIAN_POINT('',(0.0138779116499055,0.0136563552298041,0.0434358682978622));
#42080=CARTESIAN_POINT('',(0.0137833434819359,0.0137000933638628,0.0436056258056102));
#42081=CARTESIAN_POINT('',(0.0136988366239239,0.0137013802102704,0.043800906436155));
#42082=CARTESIAN_POINT('',(0.0136633334931184,0.0136813096353833,0.0439059502094003));
#42083=CARTESIAN_POINT('',(0.0136624515029435,0.0136808390639733,0.0439055621987736));
#42084=CARTESIAN_POINT('',(0.01437226696962,0.0130570532827275,0.0429594045199949));
#42085=CARTESIAN_POINT('',(0.01437226696962,0.0130570532827275,0.0429594045199949));
#42086=CARTESIAN_POINT('',(0.0146717499392492,0.0133086757482844,0.0431197540232505));
#42087=CARTESIAN_POINT('',(0.0148987545636125,0.0134914264033247,0.0435343329240457));
#42088=CARTESIAN_POINT('',(0.0149061886432635,0.0134832026201001,0.0439760606041642));
#42089=CARTESIAN_POINT('',(0.0149061886621837,0.0134832026369253,0.043976060604159));
#42090=CARTESIAN_POINT('',(0.0149061886432635,0.0134832026201001,0.0439760606041642));
#42091=CARTESIAN_POINT('',(0.0149136041538308,0.0134749993785061,0.0444166849226565));
#42092=CARTESIAN_POINT('',(0.0147019253362106,0.013278025669204,0.0448306039434562));
#42093=CARTESIAN_POINT('',(0.0144088164060122,0.0130212306025443,0.0449923308680605));
#42094=CARTESIAN_POINT('',(0.0136618759636351,0.0136805582427143,0.0439058480849644));
#42095=CARTESIAN_POINT('',(0.0136762744475629,0.0136866778567627,0.0439408460490943));
#42096=CARTESIAN_POINT('',(0.0136785483540271,0.0136846917340837,0.0440583127451966));
#42097=CARTESIAN_POINT('',(0.0136652248748306,0.013677224092152,0.0440945546229615));
#42098=CARTESIAN_POINT('',(0.0141018423856368,0.012782736153729,0.0438824700191097));
#42099=CARTESIAN_POINT('',(0.0136615152461314,0.0136804379623559,0.0439052547308507));
#42100=CARTESIAN_POINT('',(0.0136896569272057,0.0136969637596643,0.0437980033320951));
#42101=CARTESIAN_POINT('',(0.0137528858452649,0.0136935190147541,0.0436143884579431));
#42102=CARTESIAN_POINT('',(0.0138468528121099,0.0136371892690744,0.0434158218904349));
#42103=CARTESIAN_POINT('',(0.0139473868333189,0.0135469564206017,0.0432442411871308));
#42104=CARTESIAN_POINT('',(0.0140414782289585,0.0134368471581768,0.0431210525142315));
#42105=CARTESIAN_POINT('',(0.0141699419719539,0.0132607029984888,0.0429892353980327));
#42106=CARTESIAN_POINT('',(0.0142655458067999,0.0130945904910373,0.0429410276813476));
#42107=CARTESIAN_POINT('',(0.0143115126415105,0.013005915311329,0.0429303643960295));
#42108=CARTESIAN_POINT('',(0.0143115133909795,0.0130059161090858,0.0429303609927156));
#42109=CARTESIAN_POINT('',(0.0143115126415105,0.013005915311329,0.0429303643960295));
#42110=CARTESIAN_POINT('',(0.0143319072137059,0.0130235212915782,0.0429389825816724));
#42111=CARTESIAN_POINT('',(0.0143521649453348,0.0130406035866204,0.0429487100267025));
#42112=CARTESIAN_POINT('',(0.0143722462106869,0.0130570322249862,0.0429594753784009));
#42113=CARTESIAN_POINT('',(0.0138344560634004,0.0133469119961904,0.0428477145766624));
#42114=CARTESIAN_POINT('',(0.013886971005638,0.0133011649381436,0.0428574018561204));
#42115=CARTESIAN_POINT('',(0.0139438740787491,0.013252321577593,0.0428678503498006));
#42116=CARTESIAN_POINT('',(0.0140559810540401,0.0131637316702822,0.0428879083042912));
#42117=CARTESIAN_POINT('',(0.0140980505445236,0.0131313782827532,0.0428953757342894));
#42118=CARTESIAN_POINT('',(0.0141960853061902,0.01306368791893,0.042912215084704));
#42119=CARTESIAN_POINT('',(0.0142526252182071,0.0130257039963108,0.0429218802990572));
#42120=CARTESIAN_POINT('',(0.0143115133909795,0.0130059161090858,0.0429303609927156));
#42121=CARTESIAN_POINT('',(0.0137278240280471,0.0136129157959791,0.0430583504712026));
#42122=CARTESIAN_POINT('',(0.0137649908061728,0.013617058002644,0.0430801705136134));
#42123=CARTESIAN_POINT('',(0.0138033385422682,0.0136293033632107,0.0430970391927033));
#42124=CARTESIAN_POINT('',(0.0138520538399427,0.0136703266625429,0.0431003684914596));
#42125=CARTESIAN_POINT('',(0.0138674524027168,0.0136890038261722,0.0430973409796219));
#42126=CARTESIAN_POINT('',(0.0138898631504268,0.0137398103119725,0.0430767697306566));
#42127=CARTESIAN_POINT('',(0.0138966556662956,0.0137733367122553,0.0430579265936399));
#42128=CARTESIAN_POINT('',(0.0138918161470185,0.0138156031282396,0.0430276581554502));
#42129=CARTESIAN_POINT('',(0.0135040802168541,0.013679486763382,0.0433266840430606));
#42130=CARTESIAN_POINT('',(0.0135175127884876,0.0136744672531597,0.0433960521860028));
#42131=CARTESIAN_POINT('',(0.0135326432571359,0.0136696332551146,0.0434710039130298));
#42132=CARTESIAN_POINT('',(0.01356619801545,0.0136651356705284,0.0436126800003295));
#42133=CARTESIAN_POINT('',(0.0135792417840673,0.0136640591417054,0.04366509795279));
#42134=CARTESIAN_POINT('',(0.0136129108043982,0.0136660366205628,0.043781672082727));
#42135=CARTESIAN_POINT('',(0.0136329175571453,0.0136679793370068,0.0438477716337234));
#42136=CARTESIAN_POINT('',(0.0136615731878359,0.0136804198319751,0.0439051085754789));
#42137=CARTESIAN_POINT('',(0.0135040830062575,0.0136794957015745,0.04332668415021));
#42138=CARTESIAN_POINT('',(0.0135623712422786,0.0136576965251136,0.0436277204281935));
#42139=CARTESIAN_POINT('',(0.0136194652626658,0.0136620381699811,0.04382077118711));
#42140=CARTESIAN_POINT('',(0.0136619480096978,0.013680592991384,0.0439058672119058));
#42141=CARTESIAN_POINT('',(0.0135040802168541,0.013679486763382,0.0433266840430606));
#42142=CARTESIAN_POINT('',(0.0132063607148604,0.0127249017189299,0.0433152607755814));
#42143=CARTESIAN_POINT('',(0.0138344560634004,0.0133469119961904,0.0428477145766624));
#42144=CARTESIAN_POINT('',(0.0138344560634004,0.0133469119961904,0.0428477145766624));
#42145=CARTESIAN_POINT('',(0.013886971005638,0.0133011649381436,0.0428574018561204));
#42146=CARTESIAN_POINT('',(0.0139968700990166,0.0132131948679319,0.0428770439081624));
#42147=CARTESIAN_POINT('',(0.0141937370454347,0.0130454918835358,0.0429133996053987));
#42148=CARTESIAN_POINT('',(0.0143115133909795,0.0130059161090858,0.0429303609927156));
#42149=CARTESIAN_POINT('',(0.0133472984199313,0.0138340105634861,0.0361523640312129));
#42150=CARTESIAN_POINT('',(0.0133015007188745,0.0138865737234961,0.0361426658713359));
#42151=CARTESIAN_POINT('',(0.0132526083035492,0.013943522820677,0.0361322064277899));
#42152=CARTESIAN_POINT('',(0.0131639195283671,0.0140557264582103,0.0361121250269432));
#42153=CARTESIAN_POINT('',(0.0131315285880089,0.0140978328998557,0.0361046485389464));
#42154=CARTESIAN_POINT('',(0.0130637485736462,0.0141959634642915,0.0360877864006782));
#42155=CARTESIAN_POINT('',(0.0130257052961867,0.0142525630871666,0.0360781066097589));
#42156=CARTESIAN_POINT('',(0.0130058820419269,0.0143115230386036,0.0360696121138117));
#42157=CARTESIAN_POINT('',(0.0136128985927667,0.0137274518465749,0.0359418834605835));
#42158=CARTESIAN_POINT('',(0.0136169976274488,0.0137646732519322,0.0359199974709124));
#42159=CARTESIAN_POINT('',(0.0136292072606399,0.0138030888752574,0.0359030588909682));
#42160=CARTESIAN_POINT('',(0.0136702118163053,0.0138519200410911,0.0358996434566288));
#42161=CARTESIAN_POINT('',(0.0136888896648635,0.013867362410277,0.0359026444980052));
#42162=CARTESIAN_POINT('',(0.013739724994142,0.0138898605074415,0.0359231850985355));
#42163=CARTESIAN_POINT('',(0.0137732834801289,0.0138966982922935,0.035942026510332));
#42164=CARTESIAN_POINT('',(0.0138156107733477,0.0138918841669157,0.0359723251855485));
#42165=CARTESIAN_POINT('',(0.0136795294309768,0.0135039659523988,0.0356739008696862));
#42166=CARTESIAN_POINT('',(0.0136744997547652,0.0135174052624958,0.0356044661013661));
#42167=CARTESIAN_POINT('',(0.0136696558812933,0.0135325422766957,0.0355294490737307));
#42168=CARTESIAN_POINT('',(0.0136651420516113,0.0135661141628188,0.0353876400937255));
#42169=CARTESIAN_POINT('',(0.0136640597498046,0.0135791648240051,0.0353351716791691));
#42170=CARTESIAN_POINT('',(0.0136660274088303,0.0136128553332629,0.0352184742547098));
#42171=CARTESIAN_POINT('',(0.0136679631605594,0.0136328748127337,0.0351522974473094));
#42172=CARTESIAN_POINT('',(0.0136804125989053,0.0136615584408772,0.0350948893411197));
#42173=CARTESIAN_POINT('',(0.0136795440116764,0.0135039705136565,0.0356739006950023));
#42174=CARTESIAN_POINT('',(0.0136576885637337,0.0135622930115568,0.0353725345390528));
#42175=CARTESIAN_POINT('',(0.0136620275076353,0.0136194309372824,0.0351792878769671));
#42176=CARTESIAN_POINT('',(0.013680590999552,0.0136619306474012,0.0350941304125763));
#42177=CARTESIAN_POINT('',(0.0136795294309768,0.0135039659523988,0.0356739008696862));
#42178=CARTESIAN_POINT('',(0.013680831805632,0.0136624368944392,0.0350944355572129));
#42179=CARTESIAN_POINT('',(0.0127251061247038,0.0132057278958406,0.0356853119610551));
#42180=CARTESIAN_POINT('',(0.0133472984199313,0.0138340105634861,0.0361523640312129));
#42181=CARTESIAN_POINT('',(0.0133472984199313,0.0138340105634861,0.0361523640312129));
#42182=CARTESIAN_POINT('',(0.0133015007188745,0.0138865737234961,0.0361426658713359));
#42183=CARTESIAN_POINT('',(0.0132134502721952,0.0139965620617856,0.0361230041659299));
#42184=CARTESIAN_POINT('',(0.0130455285504465,0.0141936031357296,0.036086601105706));
#42185=CARTESIAN_POINT('',(0.0130058820419269,0.0143115230386036,0.0360696121138117));
#42186=CARTESIAN_POINT('',(0.0130058820419269,0.0143115230386036,0.0360696121138117));
#42187=CARTESIAN_POINT('',(0.0136804181869855,0.0136615064351884,0.0350947435404781));
#42188=CARTESIAN_POINT('',(0.0136845235441635,0.0136685117358603,0.0351214207542266));
#42189=CARTESIAN_POINT('',(0.0136962282247815,0.0137000990348768,0.0352319296825527));
#42190=CARTESIAN_POINT('',(0.0136867456212001,0.0137598515039631,0.0353955166288276));
#42191=CARTESIAN_POINT('',(0.0136444877520215,0.0138371855745404,0.0355651180311228));
#42192=CARTESIAN_POINT('',(0.0135938073861743,0.0138960677545512,0.0356688188803307));
#42193=CARTESIAN_POINT('',(0.0135566115191702,0.0139338748518138,0.0357288873200465));
#42194=CARTESIAN_POINT('',(0.0135433243902175,0.0139477100689181,0.0357513741953739));
#42195=CARTESIAN_POINT('',(0.0134294743133418,0.0140491444249602,0.0358910536670735));
#42196=CARTESIAN_POINT('',(0.0132581698826406,0.0141702913522595,0.0360077693277889));
#42197=CARTESIAN_POINT('',(0.0131050840320944,0.0142604570193312,0.0360585865159813));
#42198=CARTESIAN_POINT('',(0.0130061230521812,0.0143117701294611,0.0360705462182175));
#42199=CARTESIAN_POINT('',(0.0127820780883721,0.0141004771635773,0.035118051426175));
#42200=CARTESIAN_POINT('',(0.0130571681490899,0.0143724345256651,0.0360411286159117));
#42201=CARTESIAN_POINT('',(0.0131586168026541,0.0143173938115839,0.0360271105881626));
#42202=CARTESIAN_POINT('',(0.0133072254508839,0.0142232987437342,0.0359753879151188));
#42203=CARTESIAN_POINT('',(0.0134710348387075,0.0140916428982257,0.0358532903722309));
#42204=CARTESIAN_POINT('',(0.0135804170390299,0.0139801761974099,0.0357169716746656));
#42205=CARTESIAN_POINT('',(0.0136326038833519,0.0139121394107367,0.0356176123714242));
#42206=CARTESIAN_POINT('',(0.0136832257137762,0.0138229436469999,0.0354673177967897));
#42207=CARTESIAN_POINT('',(0.0137067063451301,0.0137410934370739,0.0353033719092715));
#42208=CARTESIAN_POINT('',(0.0136906404678223,0.0136798085372556,0.0351428401614667));
#42209=CARTESIAN_POINT('',(0.0136813031815613,0.0136633182575446,0.0350940474800154));
#42210=CARTESIAN_POINT('',(0.0130570107031178,0.0143722892292046,0.0360405596727561));
#42211=CARTESIAN_POINT('',(0.0130061230521812,0.0143117701294611,0.0360705462182175));
#42212=CARTESIAN_POINT('',(0.013023153596727,0.0143320069448286,0.0360607990551864));
#42213=CARTESIAN_POINT('',(0.0130401689831634,0.0143522282196738,0.0360509931426053));
#42214=CARTESIAN_POINT('',(0.0130571681490899,0.0143724345256651,0.0360411286159117));
#42215=CARTESIAN_POINT('',(0.0136808846299159,0.0136626724049009,0.0350920767725914));
#42216=CARTESIAN_POINT('',(0.0137210587275886,0.0137327886228891,0.0353000717275669));
#42217=CARTESIAN_POINT('',(0.0136904388863567,0.013851178063408,0.0355407663640888));
#42218=CARTESIAN_POINT('',(0.0134518098416119,0.01412260861273,0.0359035690516185));
#42219=CARTESIAN_POINT('',(0.0132517178337988,0.014266656880963,0.0360136694568607));
#42220=CARTESIAN_POINT('',(0.0130570107031176,0.0143722892292045,0.0360405596727562));
#42221=CARTESIAN_POINT('',(0.0136833127453435,0.0136683630339632,0.0350775860037388));
#42222=CARTESIAN_POINT('',(0.0137578650624181,0.0138044516106767,0.0352453746898784));
#42223=CARTESIAN_POINT('',(0.0137756675930909,0.0139953767732017,0.0354357476721513));
#42224=CARTESIAN_POINT('',(0.0136361532731369,0.014374592085454,0.0357368350948862));
#42225=CARTESIAN_POINT('',(0.0134817097350188,0.0145523279540323,0.035840266790345));
#42226=CARTESIAN_POINT('',(0.013308276944001,0.0146714608170859,0.035880362789578));
#42227=CARTESIAN_POINT('',(0.0136848811056226,0.0136729254478668,0.0350399692792684));
#42228=CARTESIAN_POINT('',(0.0137884825402338,0.0138528162957767,0.0351270500570564));
#42229=CARTESIAN_POINT('',(0.0138412758209031,0.0140905644001273,0.0352265946513145));
#42230=CARTESIAN_POINT('',(0.0137686281604507,0.0145492335926007,0.0353863968047801));
#42231=CARTESIAN_POINT('',(0.0136449518885705,0.0147591260207492,0.0354428150544384));
#42232=CARTESIAN_POINT('',(0.0134907921550379,0.0148982458255525,0.035466872082957));
#42233=CARTESIAN_POINT('',(0.0136834729528892,0.0136743637179171,0.0349598820818488));
#42234=CARTESIAN_POINT('',(0.0137840697280492,0.0138573385894591,0.0348757439524089));
#42235=CARTESIAN_POINT('',(0.0138334867729773,0.0140985532290686,0.0347830222095031));
#42236=CARTESIAN_POINT('',(0.0137555551293985,0.0145626385773065,0.0346424679496524));
#42237=CARTESIAN_POINT('',(0.0136300982234556,0.0147743494085679,0.0345980112820943));
#42238=CARTESIAN_POINT('',(0.0134752693808984,0.0149141454522923,0.0345843997163447));
#42239=CARTESIAN_POINT('',(0.0136805664818357,0.013671129001264,0.0349221271846283));
#42240=CARTESIAN_POINT('',(0.0137492535815907,0.0138131869707248,0.0347567882305654));
#42241=CARTESIAN_POINT('',(0.0137604582150299,0.0140108221137018,0.0345728698062549));
#42242=CARTESIAN_POINT('',(0.0136106422372575,0.0144005004670435,0.0342906828321895));
#42243=CARTESIAN_POINT('',(0.0134527417753365,0.0145817376785579,0.0341992056888346));
#42244=CARTESIAN_POINT('',(0.0132780514912236,0.0147021303845673,0.0341695534475961));
#42245=CARTESIAN_POINT('',(0.0136776403141161,0.0136659840267521,0.0349076015771296));
#42246=CARTESIAN_POINT('',(0.0137105256774238,0.013743550391952,0.0347009641812863));
#42247=CARTESIAN_POINT('',(0.0136715341765596,0.0138704942959491,0.0344658839028819));
#42248=CARTESIAN_POINT('',(0.0134204397438091,0.0141546429885548,0.0341216605741726));
#42249=CARTESIAN_POINT('',(0.013216668455911,0.0143024318724588,0.0340239118433991));
#42250=CARTESIAN_POINT('',(0.0130211889517766,0.0144088376077831,0.0340077073858473));
#42251=CARTESIAN_POINT('',(0.0136780272519456,0.0136667095752855,0.034905581586559));
#42252=CARTESIAN_POINT('',(0.0136964143905424,0.0137108187410915,0.034788422276699));
#42253=CARTESIAN_POINT('',(0.0136871620300887,0.0137953137079372,0.0346141668762517));
#42254=CARTESIAN_POINT('',(0.0136344884354508,0.0139000958670438,0.0344408365435239));
#42255=CARTESIAN_POINT('',(0.0135187620029207,0.0140539445911384,0.0342340356476201));
#42256=CARTESIAN_POINT('',(0.0133752357840903,0.0141802709063995,0.0341154657696032));
#42257=CARTESIAN_POINT('',(0.0131875796217974,0.014312480999393,0.0340340228098608));
#42258=CARTESIAN_POINT('',(0.0130829292098404,0.0143751763364855,0.0340129423431057));
#42259=CARTESIAN_POINT('',(0.0130211600827906,0.0144088013426358,0.0340078173960094));
#42260=CARTESIAN_POINT('',(0.0130211889517765,0.014408837607783,0.0340077073858472));
#42261=CARTESIAN_POINT('',(0.0136774973922645,0.0136658227481176,0.0349051645484567));
#42262=CARTESIAN_POINT('',(0.0136805537788317,0.0136618534337557,0.0350941516620443));
#42263=CARTESIAN_POINT('',(0.0136866691123424,0.0136762766325689,0.0350585201494323));
#42264=CARTESIAN_POINT('',(0.0136846746348222,0.0136785276008497,0.0349410108658378));
#42265=CARTESIAN_POINT('',(0.0136772282532725,0.013665211620951,0.034905449744478));
#42266=CARTESIAN_POINT('',(0.0130570107031176,0.0143722892292045,0.0360405596727562));
#42267=CARTESIAN_POINT('',(0.0133086060896628,0.0146718527161954,0.0358801529400381));
#42268=CARTESIAN_POINT('',(0.0134912320100738,0.0148988005893567,0.0354656660584956));
#42269=CARTESIAN_POINT('',(0.0134829993621013,0.014906225830457,0.0350239020087959));
#42270=CARTESIAN_POINT('',(0.013482999374259,0.0149062258439255,0.0350239020087958));
#42271=CARTESIAN_POINT('',(0.0134829993621013,0.014906225830457,0.0350239020087959));
#42272=CARTESIAN_POINT('',(0.0134747882545363,0.0149136316436989,0.0345832938205633));
#42273=CARTESIAN_POINT('',(0.0132777150147689,0.0147017461863572,0.0341693414377258));
#42274=CARTESIAN_POINT('',(0.0130211889517766,0.0144088376077831,0.0340077073858473));
#42275=CARTESIAN_POINT('',(0.0127792840555328,0.0141049572874922,0.0349295269758739));
#42276=CARTESIAN_POINT('',(0.0129669779043646,0.0143467645108084,0.0339773326375768));
#42277=CARTESIAN_POINT('',(0.0130263712183109,0.0143159396828672,0.0339812121960737));
#42278=CARTESIAN_POINT('',(0.0131233024692379,0.0142619016732827,0.0339979765471674));
#42279=CARTESIAN_POINT('',(0.0133261805475022,0.014133467545687,0.0340761972002906));
#42280=CARTESIAN_POINT('',(0.0135327339226899,0.0139708977511429,0.034245498563561));
#42281=CARTESIAN_POINT('',(0.0136832637964497,0.0137783721189361,0.0345773538662836));
#42282=CARTESIAN_POINT('',(0.0136908619908576,0.0136994685495474,0.0347882996132415));
#42283=CARTESIAN_POINT('',(0.0136770973445796,0.0136648493060317,0.0349048280955806));
#42284=CARTESIAN_POINT('',(0.0129669855780655,0.0143467743968879,0.0339772937079336));
#42285=CARTESIAN_POINT('',(0.0130211600827905,0.0144088013426356,0.0340078173960093));
#42286=CARTESIAN_POINT('',(0.0130032141795775,0.0143887737309074,0.0339965058562739));
#42287=CARTESIAN_POINT('',(0.0129851441896491,0.0143680468565852,0.0339863181194242));
#42288=CARTESIAN_POINT('',(0.0129669779043646,0.0143467645108084,0.0339773326375768));
#42289=CARTESIAN_POINT('',(0.0136559709074652,0.0135274255875118,0.0343187419294822));
#42290=CARTESIAN_POINT('',(0.0136533354668889,0.0135383536079546,0.0343887876498067));
#42291=CARTESIAN_POINT('',(0.0136510727552833,0.0135507726180141,0.0344644536835966));
#42292=CARTESIAN_POINT('',(0.0136514396594344,0.0135793138736788,0.0346078900124016));
#42293=CARTESIAN_POINT('',(0.0136521618108376,0.0135905171703827,0.0346610215461767));
#42294=CARTESIAN_POINT('',(0.0136581861359256,0.0136202052928602,0.0347793667883587));
#42295=CARTESIAN_POINT('',(0.0136624070632991,0.0136379739909101,0.0348466263114605));
#42296=CARTESIAN_POINT('',(0.0136770458879545,0.0136649288717871,0.0349046769298396));
#42297=CARTESIAN_POINT('',(0.0135793479802516,0.0137591529406104,0.0340623518581221));
#42298=CARTESIAN_POINT('',(0.0135840255876753,0.0137955634488069,0.034085439643062));
#42299=CARTESIAN_POINT('',(0.0135966310722218,0.0138333983907062,0.034103367183507));
#42300=CARTESIAN_POINT('',(0.0136375435327623,0.0138821833286537,0.0341070916759763));
#42301=CARTESIAN_POINT('',(0.0136560661394879,0.0138977713670621,0.0341039719527325));
#42302=CARTESIAN_POINT('',(0.0137061521383977,0.0139210308957088,0.0340823310548747));
#42303=CARTESIAN_POINT('',(0.0137390831725555,0.0139285228044378,0.0340624255868605));
#42304=CARTESIAN_POINT('',(0.0137803679828772,0.0139246596653472,0.0340303480415716));
#42305=CARTESIAN_POINT('',(0.0133075405240295,0.0138718879877591,0.0338655879802315));
#42306=CARTESIAN_POINT('',(0.013261936505332,0.0139239282081985,0.0338787180408429));
#42307=CARTESIAN_POINT('',(0.0132132593539372,0.0139802980185987,0.0338928674419205));
#42308=CARTESIAN_POINT('',(0.0131247399461771,0.0140917265396258,0.0339200333078431));
#42309=CARTESIAN_POINT('',(0.0130923728023401,0.0141335928811781,0.0339301491716137));
#42310=CARTESIAN_POINT('',(0.0130245918254165,0.0142313819201084,0.0339529285104976));
#42311=CARTESIAN_POINT('',(0.0129864308401398,0.0142878918202987,0.0339660153368474));
#42312=CARTESIAN_POINT('',(0.0129669855780655,0.0143467743968879,0.0339772937079336));
#42313=CARTESIAN_POINT('',(0.0129669855780655,0.0143467743968879,0.0339772937079336));
#42314=CARTESIAN_POINT('',(0.0130058761022141,0.0142290092437095,0.0339547369657612));
#42315=CARTESIAN_POINT('',(0.0131745865270879,0.014032698672613,0.0339052285351024));
#42316=CARTESIAN_POINT('',(0.013261936505332,0.0139239282081985,0.0338787180408429));
#42317=CARTESIAN_POINT('',(0.0133075405240295,0.0138718879877591,0.0338655879802315));
#42318=CARTESIAN_POINT('',(0.0133075405240295,0.0138718879877591,0.0338655879802315));
#42319=CARTESIAN_POINT('',(0.0127029149047374,0.0132248442373881,0.0343300901276774));
#42320=CARTESIAN_POINT('',(0.0136559709074652,0.0135274255875118,0.0343187419294822));
#42321=CARTESIAN_POINT('',(0.0136772662261439,0.0136652880999797,0.034905471069399));
#42322=CARTESIAN_POINT('',(0.0136556034899632,0.0136256284900497,0.0348199584719417));
#42323=CARTESIAN_POINT('',(0.01364447616907,0.0135751090501954,0.0346243712334455));
#42324=CARTESIAN_POINT('',(0.0136559727524311,0.0135274261730563,0.0343187419075286));
#42325=CARTESIAN_POINT('',(0.0152484657348856,0.0119111184403255,0.0338775863652793));
#42326=CARTESIAN_POINT('',(0.0151858258403965,0.011863360894658,0.0338569113318196));
#42327=CARTESIAN_POINT('',(0.0151277492026445,0.0118233336388945,0.0337656702120796));
#42328=CARTESIAN_POINT('',(0.0151254208358762,0.0118263115356238,0.0336843209195344));
#42329=CARTESIAN_POINT('',(0.0140382448373698,0.0134200696350122,0.0339611627334923));
#42330=CARTESIAN_POINT('',(0.0139873849465785,0.0133719181325723,0.0339320759062046));
#42331=CARTESIAN_POINT('',(0.013946293602799,0.0133349847830113,0.0338490484243907));
#42332=CARTESIAN_POINT('',(0.0139442238483378,0.0133370193734124,0.0337743619960435));
#42333=CARTESIAN_POINT('',(0.012658314481834,0.0147477052200364,0.0339896961860576));
#42334=CARTESIAN_POINT('',(0.0126090750223232,0.0146912370440514,0.0339654793180963));
#42335=CARTESIAN_POINT('',(0.0125657496565872,0.0146441278057015,0.0338778657456314));
#42336=CARTESIAN_POINT('',(0.0125642362393917,0.0146454221589132,0.0337995083619698));
#42337=CARTESIAN_POINT('',(0.00947688983191456,0.0169674284533521,0.0340865237787356));
#42338=CARTESIAN_POINT('',(0.00943997017358526,0.0169025023035178,0.0340621287700834));
#42339=CARTESIAN_POINT('',(0.00940709426201283,0.0168480005019376,0.0339747164540596));
#42340=CARTESIAN_POINT('',(0.0094054067916901,0.016848939004426,0.0338965239761736));
#42341=CARTESIAN_POINT('',(0.00775668729563145,0.0178191849284778,0.0341321851044574));
#42342=CARTESIAN_POINT('',(0.00772625457732441,0.0177506916439944,0.0341079928666602));
#42343=CARTESIAN_POINT('',(0.00769879493364172,0.0176928379308047,0.0340203470976657));
#42344=CARTESIAN_POINT('',(0.0076970813710619,0.0176935893561103,0.0339419630479391));
#42345=CARTESIAN_POINT('',(0.00408418112072838,0.0190005651886774,0.0342268669996844));
#42346=CARTESIAN_POINT('',(0.00406782135904743,0.0189272920959749,0.0342027738260244));
#42347=CARTESIAN_POINT('',(0.00405216994910225,0.0188649907657062,0.0341150197824115));
#42348=CARTESIAN_POINT('',(0.00405023404477903,0.0188654120049874,0.0340365471169725));
#42349=CARTESIAN_POINT('',(0.00216840361041831,0.0193117419450391,0.0342754880779789));
#42350=CARTESIAN_POINT('',(0.00215946952635624,0.0192374761738103,0.0342511839953137));
#42351=CARTESIAN_POINT('',(0.0021501921059827,0.0191743297555034,0.0341636686442656));
#42352=CARTESIAN_POINT('',(0.00214825046287373,0.0191745448583638,0.0340853917257764));
#42353=CARTESIAN_POINT('',(-0.00167360332837079,0.0193610642126229,0.0343700481021553));
#42354=CARTESIAN_POINT('',(-0.00166772909682775,0.019286428417166,0.0343457939093161));
#42355=CARTESIAN_POINT('',(-0.00166433877537794,0.0192225967005017,0.0342582198830898));
#42356=CARTESIAN_POINT('',(-0.00166623630989755,0.0192224297927247,0.0341798947461287));
#42357=CARTESIAN_POINT('',(-0.00361133617940907,0.0190948158684411,0.0344168625248252));
#42358=CARTESIAN_POINT('',(-0.00359794478513623,0.0190209413594288,0.0343927734792581));
#42359=CARTESIAN_POINT('',(-0.00358812593142569,0.0189574520910898,0.0343050135695173));
#42360=CARTESIAN_POINT('',(-0.00359004364584992,0.0189570900562084,0.0342265360377781));
#42361=CARTESIAN_POINT('',(-0.00728829361639954,0.0180142515371123,0.0345124729173908));
#42362=CARTESIAN_POINT('',(-0.00726075726241988,0.0179446383412048,0.0344882166245085));
#42363=CARTESIAN_POINT('',(-0.00723881613136299,0.0178846073086646,0.0344006473284614));
#42364=CARTESIAN_POINT('',(-0.00724064639673391,0.0178838674937992,0.0343223262238402));
#42365=CARTESIAN_POINT('',(-0.00906929804333343,0.0171862126464738,0.034560762512631));
#42366=CARTESIAN_POINT('',(-0.00903491514989842,0.0171197972123796,0.0345364495681483));
#42367=CARTESIAN_POINT('',(-0.00900705233761316,0.0170623997824801,0.034448942961856));
#42368=CARTESIAN_POINT('',(-0.00900874957067781,0.0170615031751766,0.0343706731538278));
#42369=CARTESIAN_POINT('',(-0.0122631905137826,0.0150748786324861,0.0346543869518873));
#42370=CARTESIAN_POINT('',(-0.0122163203849323,0.0150163415921938,0.0346302290363188));
#42371=CARTESIAN_POINT('',(-0.0121775450826729,0.0149652889674267,0.0345425456877034));
#42372=CARTESIAN_POINT('',(-0.0121790274739666,0.0149640819702418,0.0344641308966256));
#42373=CARTESIAN_POINT('',(-0.0137228510447306,0.0137592215827943,0.0347027838593881));
#42374=CARTESIAN_POINT('',(-0.0136703742361262,0.0137057774186251,0.0346785581107913));
#42375=CARTESIAN_POINT('',(-0.0136267651763594,0.0136589664244109,0.0345909540909438));
#42376=CARTESIAN_POINT('',(-0.0136281597039386,0.0136575719060068,0.0345126044943345));
#42377=CARTESIAN_POINT('',(-0.0161549996488971,0.0107998100077384,0.034797946258462));
#42378=CARTESIAN_POINT('',(-0.0160931630832887,0.0107577795404196,0.0347736188837651));
#42379=CARTESIAN_POINT('',(-0.0160413585894283,0.0107205833515088,0.0346861292106204));
#42380=CARTESIAN_POINT('',(-0.0160424287014922,0.0107189779662681,0.0346078733006445));
#42381=CARTESIAN_POINT('',(-0.0171612867006073,0.00911837226548826,0.0348448845895495));
#42382=CARTESIAN_POINT('',(-0.0170953462354564,0.00908269155364083,0.0348207145277423));
#42383=CARTESIAN_POINT('',(-0.0170397742567095,0.00905078118993255,0.0347330443100082));
#42384=CARTESIAN_POINT('',(-0.0170406643333398,0.00904911376884754,0.0346546402390712));
#42385=CARTESIAN_POINT('',(-0.018618876747511,0.00556775154408273,0.0349392970584412));
#42386=CARTESIAN_POINT('',(-0.0185471385013646,0.00554568163233485,0.0349151903208354));
#42387=CARTESIAN_POINT('',(-0.0184862866589607,0.00552519255369288,0.0348274513429876));
#42388=CARTESIAN_POINT('',(-0.0184868552108964,0.00552330384230827,0.0347489910210362));
#42389=CARTESIAN_POINT('',(-0.01908252879493,0.00367700453617041,0.0349880241107599));
#42390=CARTESIAN_POINT('',(-0.0190091993532158,0.00366227237929489,0.0349637137267457));
#42391=CARTESIAN_POINT('',(-0.0189469864824965,0.00364807081817205,0.0348762056218833));
#42392=CARTESIAN_POINT('',(-0.0189473534850118,0.00364615087558417,0.0347979346472256));
#42393=CARTESIAN_POINT('',(-0.0194330429780207,-0.000159071216011557,0.0350828838010445));
#42394=CARTESIAN_POINT('',(-0.0193581952805587,-0.000159034107970636,0.0350586138052778));
#42395=CARTESIAN_POINT('',(-0.0192943233846616,-0.000160631300607095,0.0349710578392802));
#42396=CARTESIAN_POINT('',(-0.0192943049086593,-0.000162537334766749,0.034892747516314));
#42397=CARTESIAN_POINT('',(-0.019323220858512,-0.00208279330176897,0.0351290854614679));
#42398=CARTESIAN_POINT('',(-0.0192485540725893,-0.00207532108809656,0.0351049608609899));
#42399=CARTESIAN_POINT('',(-0.0191845482294334,-0.00207058909152159,0.0350172412926273));
#42400=CARTESIAN_POINT('',(-0.0191843388777613,-0.00207253258253173,0.0349387968701855));
#42401=CARTESIAN_POINT('',(-0.018526423896832,-0.00587164369870195,0.035225609788055));
#42402=CARTESIAN_POINT('',(-0.0184549150235699,-0.00584958997299527,0.0352013255107728));
#42403=CARTESIAN_POINT('',(-0.0183934136736763,-0.00583237202561983,0.0351137878656332));
#42404=CARTESIAN_POINT('',(-0.0183928195717425,-0.0058342469680116,0.0350354927017894));
#42405=CARTESIAN_POINT('',(-0.0178587922177036,-0.00766578380247021,0.0352724553485967));
#42406=CARTESIAN_POINT('',(-0.017789822465766,-0.00763681873606203,0.0352481492370294));
#42407=CARTESIAN_POINT('',(-0.0177303624302418,-0.0076136257508411,0.0351606344733825));
#42408=CARTESIAN_POINT('',(-0.0177296077983877,-0.00761538266113453,0.0350823579657423));
#42409=CARTESIAN_POINT('',(-0.0159857063641824,-0.0110535861634857,0.0353669496908954));
#42410=CARTESIAN_POINT('',(-0.0159236482423738,-0.0110113827549873,0.0353428313428075));
#42411=CARTESIAN_POINT('',(-0.0158696595078198,-0.0109766550493149,0.0352551031157736));
#42412=CARTESIAN_POINT('',(-0.0158685715064848,-0.010978227730547,0.0351766515074452));
#42413=CARTESIAN_POINT('',(-0.0148111911879068,-0.0125819195993878,0.0354145067676068));
#42414=CARTESIAN_POINT('',(-0.0147537039270021,-0.0125338506107053,0.0353903052149494));
#42415=CARTESIAN_POINT('',(-0.0147035220233913,-0.0124940841885928,0.0353026737935011));
#42416=CARTESIAN_POINT('',(-0.0147022403647437,-0.0124955888864539,0.0352243017315574));
#42417=CARTESIAN_POINT('',(-0.0120387344173888,-0.0152554388784305,0.0355103574544654));
#42418=CARTESIAN_POINT('',(-0.0119919676073606,-0.0151971041221094,0.0354860257152941));
#42419=CARTESIAN_POINT('',(-0.0119508100978304,-0.0151483938894718,0.0353985411397392));
#42420=CARTESIAN_POINT('',(-0.0119492905153562,-0.0151495897482933,0.0353202894208755));
#42421=CARTESIAN_POINT('',(-0.010451420680373,-0.0163834982989298,0.0355570836717863));
#42422=CARTESIAN_POINT('',(-0.0104106338065928,-0.0163206205454677,0.0355328929543693));
#42423=CARTESIAN_POINT('',(-0.010374434674129,-0.0162677917784069,0.0354452462963411));
#42424=CARTESIAN_POINT('',(-0.0103728406094323,-0.0162688127609957,0.0353668615585341));
#42425=CARTESIAN_POINT('',(-0.00702795570842145,-0.0181180930152355,0.0356515539846757));
#42426=CARTESIAN_POINT('',(-0.00700027756530127,-0.0180483744095495,0.0356274130424822));
#42427=CARTESIAN_POINT('',(-0.00697504988780368,-0.0179894030893777,0.0355397127643222));
#42428=CARTESIAN_POINT('',(-0.00697321301761058,-0.017990119265087,0.0354612841950215));
#42429=CARTESIAN_POINT('',(-0.00516713643770654,-0.0187328837046514,0.0357004746702459));
#42430=CARTESIAN_POINT('',(-0.00514668355624036,-0.0186609611650446,0.035676151543525));
#42431=CARTESIAN_POINT('',(-0.00512764139888409,-0.0186000854485199,0.0355886577116004));
#42432=CARTESIAN_POINT('',(-0.00512576324307812,-0.0186006006840196,0.0355103984279492));
#42433=CARTESIAN_POINT('',(-0.00139218102196667,-0.0193827829215529,0.0357945730344739));
#42434=CARTESIAN_POINT('',(-0.00138624224911403,-0.0193081403307028,0.0357703296806507));
#42435=CARTESIAN_POINT('',(-0.00137954992248072,-0.0192445505752173,0.0356827431915192));
#42436=CARTESIAN_POINT('',(-0.0013776523864038,-0.0192446841629754,0.0356044078293643));
#42437=CARTESIAN_POINT('',(0.000572588218934399,-0.0194246737866148,0.035841714022483));
#42438=CARTESIAN_POINT('',(0.000570947370553278,-0.019349620051212,0.0358176203178043));
#42439=CARTESIAN_POINT('',(0.000571210769109811,-0.0192853859213364,0.0357298658608833));
#42440=CARTESIAN_POINT('',(0.000573167396785734,-0.0192853284395788,0.0356513928178601));
#42441=CARTESIAN_POINT('',(0.00436973798898508,-0.018934846936721,0.0359372961428186));
#42442=CARTESIAN_POINT('',(0.00435347581480306,-0.0188617958776991,0.0359130232916096));
#42443=CARTESIAN_POINT('',(0.00434123413948511,-0.0187990977995665,0.0358254727273128));
#42444=CARTESIAN_POINT('',(0.0043431547027079,-0.0187986547687731,0.0357471669804605));
#42445=CARTESIAN_POINT('',(0.00625864225674502,-0.018397160611825,0.0359854747050194));
#42446=CARTESIAN_POINT('',(0.00623511134760215,-0.0183261678087875,0.0359611636278828));
#42447=CARTESIAN_POINT('',(0.00621660098285804,-0.0182651048018455,0.0358736547360438));
#42448=CARTESIAN_POINT('',(0.00621841450216693,-0.0182644872522259,0.03579538304732));
#42449=CARTESIAN_POINT('',(0.00974796227618663,-0.016811426961068,0.0360791583163149));
#42450=CARTESIAN_POINT('',(0.00971084419310295,-0.0167462530048705,0.0360550101091685));
#42451=CARTESIAN_POINT('',(0.00968054611933654,-0.0166897336117225,0.0359673158108602));
#42452=CARTESIAN_POINT('',(0.00968220133754792,-0.0166887731953749,0.0358888920411454));
#42453=CARTESIAN_POINT('',(0.0113882717487478,-0.0157468141669751,0.0361274222318138));
#42454=CARTESIAN_POINT('',(0.0113448598901736,-0.0156857881408525,0.0361031878926111));
#42455=CARTESIAN_POINT('',(0.0113091654394432,-0.0156327125443483,0.0360155936464992));
#42456=CARTESIAN_POINT('',(0.0113107615506835,-0.0156315548533139,0.0359372520648063));
#42457=CARTESIAN_POINT('',(0.0142638915192683,-0.0131979063047583,0.0362228199557271));
#42458=CARTESIAN_POINT('',(0.0142093998765725,-0.0131467035594434,0.0361984945903921));
#42459=CARTESIAN_POINT('',(0.0141640569778619,-0.0131018477396012,0.0361110025320489));
#42460=CARTESIAN_POINT('',(0.0141653634357823,-0.0131004317761201,0.0360327446597237));
#42461=CARTESIAN_POINT('',(0.0155099871775632,-0.011710480490977,0.0362692166595979));
#42462=CARTESIAN_POINT('',(0.0154504782693005,-0.0116648392026414,0.036245060107269));
#42463=CARTESIAN_POINT('',(0.0154006067027975,-0.0116245513559714,0.0361573745561721));
#42464=CARTESIAN_POINT('',(0.015401748510621,-0.0116230458123332,0.0360789579026339));
#42465=CARTESIAN_POINT('',(0.0175178637361487,-0.00841573059787445,0.0363642600524374));
#42466=CARTESIAN_POINT('',(0.0174504761001674,-0.00838269957389024,0.0363401437162083));
#42467=CARTESIAN_POINT('',(0.0173936016377699,-0.00835293382421085,0.0362524158765654));
#42468=CARTESIAN_POINT('',(0.0173944625462095,-0.00835115105051529,0.0361739647082496));
#42469=CARTESIAN_POINT('',(0.0182624515796345,-0.006648377091405,0.0364122382904254));
#42470=CARTESIAN_POINT('',(0.0181923746561503,-0.00662223604375927,0.036387923067016));
#42471=CARTESIAN_POINT('',(0.0181331939085809,-0.00659837938135913,0.0363004203966629));
#42472=CARTESIAN_POINT('',(0.0181338591348402,-0.0065965437312554,0.0362221538738593));
#42473=CARTESIAN_POINT('',(0.0192194486591489,-0.00288751225102433,0.0365077284567637));
#42474=CARTESIAN_POINT('',(0.01914550312317,-0.00287582042360165,0.0364834668324474));
#42475=CARTESIAN_POINT('',(0.0190826491640174,-0.00286423331881863,0.0363959012744127));
#42476=CARTESIAN_POINT('',(0.0190829294130007,-0.00286234891985882,0.0363175830830445));
#42477=CARTESIAN_POINT('',(0.0194098491272683,-0.000982580873600955,0.036553695077945));
#42478=CARTESIAN_POINT('',(0.0193349437255172,-0.000978214703617675,0.0365295661903181));
#42479=CARTESIAN_POINT('',(0.0192710001663832,-0.000972817108818172,0.0364418515882359));
#42480=CARTESIAN_POINT('',(0.0192710989915557,-0.000970861653981333,0.0363634112480515));
#42481=CARTESIAN_POINT('',(0.0192202056017125,0.00287588470824289,0.0366500242217906));
#42482=CARTESIAN_POINT('',(0.0191461244303748,0.00286538714458625,0.0366257326413781));
#42483=CARTESIAN_POINT('',(0.0190826930320087,0.00285808453264583,0.0365382032286708));
#42484=CARTESIAN_POINT('',(0.0190824022057189,0.00286002705453847,0.0364599148108454));
#42485=CARTESIAN_POINT('',(0.0188379106547843,0.0047734665138793,0.0366973166700389));
#42486=CARTESIAN_POINT('',(0.018765251017742,0.00475566014909327,0.036673017774804));
#42487=CARTESIAN_POINT('',(0.0187028830749146,0.00474206184380905,0.0365854946832061));
#42488=CARTESIAN_POINT('',(0.0187024138420233,0.00474391283128575,0.0365072113414088));
#42489=CARTESIAN_POINT('',(0.0175295655931796,0.00838993396492618,0.0367911918806325));
#42490=CARTESIAN_POINT('',(0.0174616178458993,0.00835805890798054,0.0367670802579245));
#42491=CARTESIAN_POINT('',(0.0174028132235672,0.00833229126715749,0.036679344518385));
#42492=CARTESIAN_POINT('',(0.0174019863583542,0.008334018433673,0.0366008867507613));
#42493=CARTESIAN_POINT('',(0.0165984266245079,0.0101061561823627,0.0368394726457053));
#42494=CARTESIAN_POINT('',(0.0165341336245753,0.0100676948925726,0.0368152604792397));
#42495=CARTESIAN_POINT('',(0.0164783622620697,0.0100362923655943,0.0367276411189044));
#42496=CARTESIAN_POINT('',(0.0164773324201164,0.0100379785673599,0.036649278948126));
#42497=CARTESIAN_POINT('',(0.0142905353273534,0.0131684358682503,0.0369348355464337));
#42498=CARTESIAN_POINT('',(0.0142351661563029,0.0131181958780369,0.0369105048728009));
#42499=CARTESIAN_POINT('',(0.0141868524427726,0.0130765746613298,0.0368230189991468));
#42500=CARTESIAN_POINT('',(0.0141855420207472,0.0130779927733353,0.0367447662090692));
#42501=CARTESIAN_POINT('',(0.0128895188291006,0.0145429059113914,0.0369818752438031));
#42502=CARTESIAN_POINT('',(0.0128393736391177,0.0144871840945391,0.0369576976771935));
#42503=CARTESIAN_POINT('',(0.0127953290097661,0.0144406609758556,0.0368700360789205));
#42504=CARTESIAN_POINT('',(0.0127939152942572,0.0144419190605648,0.0367916390825784));
#42505=CARTESIAN_POINT('',(0.00978786991559796,0.0167879924321533,0.0370762585418591));
#42506=CARTESIAN_POINT('',(0.00974958535440995,0.0167235036723632,0.0370521074471736));
#42507=CARTESIAN_POINT('',(0.0097154094364033,0.016669251743918,0.0369644189414872));
#42508=CARTESIAN_POINT('',(0.00971370211163489,0.0166702515276451,0.0368860000449194));
#42509=CARTESIAN_POINT('',(0.00804166596354184,0.0176903828787484,0.0371252845413655));
#42510=CARTESIAN_POINT('',(0.00801018587904991,0.0176225629513854,0.0371009582456875));
#42511=CARTESIAN_POINT('',(0.00798183457162373,0.0175654329761448,0.0370134679189905));
#42512=CARTESIAN_POINT('',(0.00798006309091339,0.0175662353813498,0.0369352115046535));
#42513=CARTESIAN_POINT('',(0.0044163194260252,0.0189242184549924,0.0372192839751649));
#42514=CARTESIAN_POINT('',(0.00439873869692677,0.0188514198959119,0.0371950506017007));
#42515=CARTESIAN_POINT('',(0.0043821463774674,0.0187896490582238,0.0371074527101591));
#42516=CARTESIAN_POINT('',(0.00438029403874385,0.0187900786731213,0.0370291079952339));
#42517=CARTESIAN_POINT('',(0.00248610588398672,0.0192737620343253,0.0372664223567425));
#42518=CARTESIAN_POINT('',(0.00247593541563535,0.0191993875068387,0.0372423237815989));
#42519=CARTESIAN_POINT('',(0.00246558189748319,0.0191360009975268,0.0371545749507012));
#42520=CARTESIAN_POINT('',(0.00246363690390784,0.0191362517585942,0.0370761065326615));
#42521=CARTESIAN_POINT('',(-0.00134787560567592,0.0193860391546447,0.0373622032590154));
#42522=CARTESIAN_POINT('',(-0.00134326448971298,0.01931135295845,0.0373379210285972));
#42523=CARTESIAN_POINT('',(-0.00134099918203681,0.0192475283997314,0.0372503810494137));
#42524=CARTESIAN_POINT('',(-0.00134296270095129,0.0192473917543767,0.0371720839782732));
#42525=CARTESIAN_POINT('',(-0.00328486942927988,0.019153728202705,0.0374099693667313));
#42526=CARTESIAN_POINT('',(-0.00327280431272498,0.0190799067467614,0.0373856637145816));
#42527=CARTESIAN_POINT('',(-0.00326413183658672,0.0190166788604113,0.0372981485277988));
#42528=CARTESIAN_POINT('',(-0.00326601750557292,0.0190163551594814,0.0372198716721568));
#42529=CARTESIAN_POINT('',(-0.00699439582431333,0.0181316033959343,0.0375040151627022));
#42530=CARTESIAN_POINT('',(-0.00696794173589825,0.018061407895021,0.0374798741828622));
#42531=CARTESIAN_POINT('',(-0.0069468685444334,0.018000823563801,0.0373921717860003));
#42532=CARTESIAN_POINT('',(-0.00694865640299855,0.0180001335575965,0.037313741377107));
#42533=CARTESIAN_POINT('',(-0.00876107696796061,0.0173476846701873,0.0375518061498425));
#42534=CARTESIAN_POINT('',(-0.00872784348875839,0.0172805784608766,0.0375275629593083));
#42535=CARTESIAN_POINT('',(-0.00870097863415649,0.0172225469740549,0.0374399787779819));
#42536=CARTESIAN_POINT('',(-0.00870273685794072,0.0172216558340193,0.0373616454492075));
#42537=CARTESIAN_POINT('',(-0.0120213318765713,0.0152701046479567,0.0376477120444383));
#42538=CARTESIAN_POINT('',(-0.0119755279397664,0.0152109928382331,0.0376233891251002));
#42539=CARTESIAN_POINT('',(-0.0119377636830074,0.0151595828288496,0.0375358941828318));
#42540=CARTESIAN_POINT('',(-0.0119392736272278,0.0151583905391748,0.0374576339393092));
#42541=CARTESIAN_POINT('',(-0.0134661942258329,0.0140140920121328,0.0376934022305724));
#42542=CARTESIAN_POINT('',(-0.0134146259061713,0.0139596103567137,0.0376692590059635));
#42543=CARTESIAN_POINT('',(-0.0133717221338478,0.0139119318098514,0.0375815583359552));
#42544=CARTESIAN_POINT('',(-0.0133730874184949,0.0139106261003993,0.037503129276001));
#42545=CARTESIAN_POINT('',(-0.0159800261710854,0.0110622696501474,0.0377890510435331));
#42546=CARTESIAN_POINT('',(-0.0159186701493929,0.0110190736210227,0.0377649234054599));
#42547=CARTESIAN_POINT('',(-0.0158671939734713,0.0109807538574401,0.0376772086356948));
#42548=CARTESIAN_POINT('',(-0.0158683286817252,0.0109791224811712,0.0375987682063429));
#42549=CARTESIAN_POINT('',(-0.0169927014477256,0.00942964358742211,0.0378370711676181));
#42550=CARTESIAN_POINT('',(-0.0169275999860674,0.00939284044147255,0.0378127520470631));
#42551=CARTESIAN_POINT('',(-0.0168729023629467,0.00936000506277512,0.0377252537200097));
#42552=CARTESIAN_POINT('',(-0.0168738459564173,0.00935829903214214,0.0376469907536258));
#42553=CARTESIAN_POINT('',(-0.0185202330766905,0.00588892750320043,0.0379318849520895));
#42554=CARTESIAN_POINT('',(-0.0184490597344988,0.00586569177572236,0.0379076315446938));
#42555=CARTESIAN_POINT('',(-0.0183888161595843,0.00584431082219037,0.03782005659223));
#42556=CARTESIAN_POINT('',(-0.0183893906474437,0.00584249516487678,0.0377417306953401));
#42557=CARTESIAN_POINT('',(-0.0190152816034714,0.00401040540637397,0.0379786358366598));
#42558=CARTESIAN_POINT('',(-0.0189419961223453,0.00399436197687571,0.0379545013168636));
#42559=CARTESIAN_POINT('',(-0.0188797021261493,0.0039790153132323,0.0378667932018171));
#42560=CARTESIAN_POINT('',(-0.0188801063331463,0.00397709655791713,0.0377883581908105));
#42561=CARTESIAN_POINT('',(-0.0194321009153758,0.000192138599558602,0.0380744231692379));
#42562=CARTESIAN_POINT('',(-0.0193573042177216,0.000190819056578032,0.0380501249191978));
#42563=CARTESIAN_POINT('',(-0.0192935315844883,0.000188027198034302,0.0379626030162209));
#42564=CARTESIAN_POINT('',(-0.0192935505188315,0.000186066007663494,0.0378843207510498));
#42565=CARTESIAN_POINT('',(-0.01935245436779,-0.00176338950479553,0.0381221642309786));
#42566=CARTESIAN_POINT('',(-0.0192778947935724,-0.00175718375645641,0.0380978732683488));
#42567=CARTESIAN_POINT('',(-0.0192141536943148,-0.0017535195261046,0.0380103410376233));
#42568=CARTESIAN_POINT('',(-0.0192139807220376,-0.00175541870492419,0.0379320501962032));
#42569=CARTESIAN_POINT('',(-0.0186307898171988,-0.00552669110195807,0.0382157044502257));
#42570=CARTESIAN_POINT('',(-0.0185586670123005,-0.00550590460021261,0.038191599349049));
#42571=CARTESIAN_POINT('',(-0.0184965293375801,-0.00548971177913334,0.0381038563465176));
#42572=CARTESIAN_POINT('',(-0.0184959839749268,-0.00549155049286511,0.0380253926248339));
#42573=CARTESIAN_POINT('',(-0.0179766003326881,-0.00737942712623029,0.0382643900908638));
#42574=CARTESIAN_POINT('',(-0.0179070883556642,-0.00735152506121528,0.0382401675413537));
#42575=CARTESIAN_POINT('',(-0.0178471053992343,-0.00732926072206128,0.0381525599762558));
#42576=CARTESIAN_POINT('',(-0.017846352858866,-0.00733108658494678,0.0380742074777779));
#42577=CARTESIAN_POINT('',(-0.0161849938678833,-0.0107539093268891,0.0383593363237856));
#42578=CARTESIAN_POINT('',(-0.0161224057707,-0.0107130134365234,0.0383350073881844));
#42579=CARTESIAN_POINT('',(-0.0160681417269081,-0.0106795156784479,0.0382475194490954));
#42580=CARTESIAN_POINT('',(-0.0160670723710059,-0.0106811200865827,0.0381692649588679));
#42581=CARTESIAN_POINT('',(-0.0150241786357296,-0.0123287368515955,0.0384061484184165));
#42582=CARTESIAN_POINT('',(-0.0149658519529488,-0.0122816050792086,0.0383819847308958));
#42583=CARTESIAN_POINT('',(-0.0149149959562187,-0.0122425879942847,0.03829430730965));
#42584=CARTESIAN_POINT('',(-0.0149138001047669,-0.0122440523050679,0.0382158973270259));
#42585=CARTESIAN_POINT('',(-0.0122807280456702,-0.0150634424110327,0.0385017879912471));
#42586=CARTESIAN_POINT('',(-0.0122328851481888,-0.0150056988755769,0.0384776241054119));
#42587=CARTESIAN_POINT('',(-0.0121906942167475,-0.0149574409602581,0.0383899504553218));
#42588=CARTESIAN_POINT('',(-0.0121891559707154,-0.014958700716832,0.0383115437663749));
#42589=CARTESIAN_POINT('',(-0.0107387574079005,-0.016197932406738,0.0385494815949886));
#42590=CARTESIAN_POINT('',(-0.0106969473711148,-0.0161359401607028,0.0385251524019803));
#42591=CARTESIAN_POINT('',(-0.0106599200181777,-0.0160840104127377,0.0384376652763639));
#42592=CARTESIAN_POINT('',(-0.0106582997137264,-0.0160850815777654,0.0383594114826556));
#42593=CARTESIAN_POINT('',(-0.00731727827992635,-0.0180045813174106,0.0386443821218688));
#42594=CARTESIAN_POINT('',(-0.00728853974211108,-0.0179354004473274,0.0386201592294896));
#42595=CARTESIAN_POINT('',(-0.00726249647480254,-0.0178769524956158,0.0385325493700246));
#42596=CARTESIAN_POINT('',(-0.00726073440225153,-0.0178776659016483,0.0384541948382906));
#42597=CARTESIAN_POINT('',(-0.00549562993204591,-0.0186409126876467,0.0386908155039891));
#42598=CARTESIAN_POINT('',(-0.0054738544920556,-0.0185690779957131,0.0386667116487949));
#42599=CARTESIAN_POINT('',(-0.00545363064055279,-0.0185081268843176,0.0385789688906636));
#42600=CARTESIAN_POINT('',(-0.00545174652657209,-0.0185086819285558,0.03850050546279));
#42601=CARTESIAN_POINT('',(-0.00171297789558108,-0.0193578808109938,0.0387869685227048));
#42602=CARTESIAN_POINT('',(-0.00170580575094533,-0.0192834050608197,0.0387626779532545));
#42603=CARTESIAN_POINT('',(-0.00169802546614798,-0.0192200301102672,0.0386751473835489));
#42604=CARTESIAN_POINT('',(-0.00169606742719998,-0.0192202029699177,0.0385968580236358));
#42605=CARTESIAN_POINT('',(0.000234326520478524,-0.0194314445656357,0.0388345938678207));
#42606=CARTESIAN_POINT('',(0.000234010164348733,-0.0193566380194836,0.0388102946104787));
#42607=CARTESIAN_POINT('',(0.000235377831076791,-0.0192928221301491,0.0387227720368678));
#42608=CARTESIAN_POINT('',(0.000237288513941407,-0.0192927990424999,0.0386444891190078));
#42609=CARTESIAN_POINT('',(0.00404787155173841,-0.0190071440116824,0.0389283814240497));
#42610=CARTESIAN_POINT('',(0.00403281600376,-0.0189336501553832,0.0389042461039105));
#42611=CARTESIAN_POINT('',(0.00402156009123918,-0.0188704913271033,0.0388165373983829));
#42612=CARTESIAN_POINT('',(0.00402343712348825,-0.0188700915325411,0.0387381018186629));
#42613=CARTESIAN_POINT('',(0.00594205675945055,-0.018501902080374,0.038976946540659));
#42614=CARTESIAN_POINT('',(0.00591972441584579,-0.0184304448473425,0.038952694041197));
#42615=CARTESIAN_POINT('',(0.00590226500799304,-0.0183689513755182,0.0388651204286461));
#42616=CARTESIAN_POINT('',(0.00590413947814813,-0.0183683463522363,0.0387867957647425));
#42617=CARTESIAN_POINT('',(0.00945543378881706,-0.0169768884659516,0.0390718896815281));
#42618=CARTESIAN_POINT('',(0.00941955105645558,-0.0169112809125558,0.0390475705383369));
#42619=CARTESIAN_POINT('',(0.00939038642398818,-0.016854546848796,0.0389600712082809));
#42620=CARTESIAN_POINT('',(0.00939206362974605,-0.0168536094492528,0.0388818073612772));
#42621=CARTESIAN_POINT('',(0.0111223087685258,-0.0159353585344843,0.0391187890482724));
#42622=CARTESIAN_POINT('',(0.0110798312243679,-0.0158735148232922,0.0390946605182411));
#42623=CARTESIAN_POINT('',(0.0110448505119366,-0.0158197280398541,0.0390069433294018));
#42624=CARTESIAN_POINT('',(0.0110464049211253,-0.0158186485540586,0.0389285007223895));
#42625=CARTESIAN_POINT('',(0.0140306587396472,-0.0134454521687635,0.0392134074489147));
#42626=CARTESIAN_POINT('',(0.0139769149734139,-0.013393127998949,0.0391892651849783));
#42627=CARTESIAN_POINT('',(0.0139321645237592,-0.0133471836038336,0.0391015671499933));
#42628=CARTESIAN_POINT('',(0.0139335456449393,-0.0133457487432768,0.0390231404614087));
#42629=CARTESIAN_POINT('',(0.0153155581303857,-0.0119607522408212,0.0392624168290426));
#42630=CARTESIAN_POINT('',(0.0152569911307815,-0.0119142632470286,0.0392380940571982));
#42631=CARTESIAN_POINT('',(0.015208082986905,-0.0118733172212726,0.0391505997737426));
#42632=CARTESIAN_POINT('',(0.0152092788797299,-0.011871781703946,0.0390723401171548));
#42633=CARTESIAN_POINT('',(0.0173657491105147,-0.00872162810886881,0.0393565917639802));
#42634=CARTESIAN_POINT('',(0.0172990962157357,-0.00868750783861493,0.0393323481039219));
#42635=CARTESIAN_POINT('',(0.017242940434333,-0.00865693103776873,0.0392447620183172));
#42636=CARTESIAN_POINT('',(0.017243792561054,-0.00865522864971671,0.039166426990155));
#42637=CARTESIAN_POINT('',(0.0181547615587285,-0.0069335040110206,0.039403733158809));
#42638=CARTESIAN_POINT('',(0.0180848927866211,-0.00690620417209522,0.0393795919178693));
#42639=CARTESIAN_POINT('',(0.0180257763837351,-0.00688131022021618,0.0392918915243171));
#42640=CARTESIAN_POINT('',(0.0180264763251293,-0.00687947534514428,0.0392134628550138));
#42641=CARTESIAN_POINT('',(0.0191637763706284,-0.00322453562887558,0.0394995926897395));
#42642=CARTESIAN_POINT('',(0.0190901121570296,-0.00321155341112151,0.0394752871793574));
#42643=CARTESIAN_POINT('',(0.0190275708723674,-0.00319884217617825,0.0393877734491774));
#42644=CARTESIAN_POINT('',(0.0190278950280094,-0.00319691109165435,0.0393094978793444));
#42645=CARTESIAN_POINT('',(0.019390584562046,-0.00129919113440175,0.0395467820100426));
#42646=CARTESIAN_POINT('',(0.0193159596168944,-0.00129360518917694,0.0395224993996629));
#42647=CARTESIAN_POINT('',(0.0192524133638981,-0.00128721042390899,0.0394349575490327));
#42648=CARTESIAN_POINT('',(0.0192525410891745,-0.00128531010501602,0.0393566588132005));
#42649=CARTESIAN_POINT('',(0.0192654480728298,0.00255902747664352,0.0396410321703988));
#42650=CARTESIAN_POINT('',(0.0191909539952961,0.00254972160441421,0.0396169341992129));
#42651=CARTESIAN_POINT('',(0.0191270342322012,0.00254340177096497,0.0395291832721127));
#42652=CARTESIAN_POINT('',(0.0191267815750555,0.00254530686490345,0.0394507130547643));
#42653=CARTESIAN_POINT('',(0.018920683437361,0.00444305374675822,0.0396885804156549));
#42654=CARTESIAN_POINT('',(0.0188476331628076,0.00442650180934002,0.0396643480409234));
#42655=CARTESIAN_POINT('',(0.0187848919764505,0.00441401055138857,0.0395767516461146));
#42656=CARTESIAN_POINT('',(0.0187844377200531,0.00441593205747535,0.0394984083074891));
#42657=CARTESIAN_POINT('',(0.0176595364392572,0.00811552306226673,0.0397849985133176));
#42658=CARTESIAN_POINT('',(0.0175913513792114,0.00808482042028178,0.0397606712460022));
#42659=CARTESIAN_POINT('',(0.0175325381227602,0.00806013414993144,0.0396731812985189));
#42660=CARTESIAN_POINT('',(0.0175317315447527,0.0080618822515282,0.0395949251539854));
#42661=CARTESIAN_POINT('',(0.0167748459587384,0.00981354181841796,0.0398307170263652));
#42662=CARTESIAN_POINT('',(0.0167098246400574,0.00977615831575187,0.0398065649037819));
#42663=CARTESIAN_POINT('',(0.0166534462708234,0.00974561518644464,0.0397188746507484));
#42664=CARTESIAN_POINT('',(0.0166524910438048,0.00974725586583842,0.0396404541567125));
#42665=CARTESIAN_POINT('',(0.0145036323846716,0.0129360948209068,0.039926190043373));
#42666=CARTESIAN_POINT('',(0.0144472907815484,0.012886636570823,0.0399020137013212));
#42667=CARTESIAN_POINT('',(0.01439803453912,0.0128456564564349,0.0398143541368571));
#42668=CARTESIAN_POINT('',(0.0143967148926182,0.0128471419070078,0.0397359590016802));
#42669=CARTESIAN_POINT('',(0.0131425537235162,0.0143150190215106,0.0399743936492381));
#42670=CARTESIAN_POINT('',(0.0130915539773512,0.01426034540911,0.0399500631806892));
#42671=CARTESIAN_POINT('',(0.0130468557902625,0.0142148597033713,0.0398625773915283));
#42672=CARTESIAN_POINT('',(0.0130454255977014,0.0142161695140225,0.0397843246887073));
#42673=CARTESIAN_POINT('',(0.0100673829200725,0.0166225526528062,0.0400686266341829));
#42674=CARTESIAN_POINT('',(0.0100280785092642,0.0165587699208662,0.0400444133545312));
#42675=CARTESIAN_POINT('',(0.00999312597703867,0.0165051542085715,0.039956792543069));
#42676=CARTESIAN_POINT('',(0.00999149890733325,0.0165061368666732,0.0398784290286423));
#42677=CARTESIAN_POINT('',(0.00834737832249906,0.017549210372631,0.0401157595299874));
#42678=CARTESIAN_POINT('',(0.0083146237018335,0.0174816849729387,0.0400916485526069));
#42679=CARTESIAN_POINT('',(0.00828510636698564,0.0174246703944439,0.040003913952241));
#42680=CARTESIAN_POINT('',(0.00828332989840086,0.0174255146209965,0.0399254572243831));
#42681=CARTESIAN_POINT('',(0.00473953259241176,0.0188458640380989,0.040211512069501));
#42682=CARTESIAN_POINT('',(0.0047207264931358,0.0187734587187308,0.0401872142418862));
#42683=CARTESIAN_POINT('',(0.00470307137359621,0.018712114939268,0.0400996918515199));
#42684=CARTESIAN_POINT('',(0.00470116778765926,0.0187125929642203,0.0400214091930436));
#42685=CARTESIAN_POINT('',(0.00281385362484171,0.0192276739823713,0.0402594115432935));
#42686=CARTESIAN_POINT('',(0.00280244216170432,0.0191537339652338,0.0402351197714317));
#42687=CARTESIAN_POINT('',(0.00279109103467653,0.0190909074196349,0.0401475885704477));
#42688=CARTESIAN_POINT('',(0.00278920281488217,0.019091183988523,0.0400692985725725));
#42689=CARTESIAN_POINT('',(-0.00101085160756184,0.0194066985670039,0.0403530112899306));
#42690=CARTESIAN_POINT('',(-0.00100753201763225,0.0193317466932373,0.0403288812557846));
#42691=CARTESIAN_POINT('',(-0.00100634339435394,0.0192675947719003,0.0402411666875001));
#42692=CARTESIAN_POINT('',(-0.0010082631995002,0.0192674950044555,0.0401627263035939));
#42693=CARTESIAN_POINT('',(-0.00296586699536353,0.0192049596230593,0.0404017829715575));
#42694=CARTESIAN_POINT('',(-0.00295502402753038,0.019130895206498,0.0403775214550599));
#42695=CARTESIAN_POINT('',(-0.00294743051497526,0.0190674417552862,0.040289958079941));
#42696=CARTESIAN_POINT('',(-0.00294937536344791,0.0190671384373783,0.0402116418088512));
#42697=CARTESIAN_POINT('',(-0.00667478459254796,0.0182501325704563,0.0404966423224674));
#42698=CARTESIAN_POINT('',(-0.0066496376241613,0.0181797025697532,0.0404723274623812));
#42699=CARTESIAN_POINT('',(-0.00662973097637039,0.018119087966066,0.0403848231561246));
#42700=CARTESIAN_POINT('',(-0.0066315320520576,0.0181184261421127,0.0403065552228863));
#42701=CARTESIAN_POINT('',(-0.00848057591989537,0.0174853536409583,0.0405433851196045));
#42702=CARTESIAN_POINT('',(-0.00844833575227234,0.0174175882114456,0.0405192688181649));
#42703=CARTESIAN_POINT('',(-0.0084222354928671,0.0173589471688255,0.0404315380802686));
#42704=CARTESIAN_POINT('',(-0.00842394764778655,0.0173581211968173,0.0403530843731059));
#42705=CARTESIAN_POINT('',(-0.0117501648030116,0.0154785718893798,0.0406383502013855));
#42706=CARTESIAN_POINT('',(-0.0117052950541378,0.0154184856025082,0.0406141935740401));
#42707=CARTESIAN_POINT('',(-0.0116683116154951,0.0153661186350555,0.0405265117750975));
#42708=CARTESIAN_POINT('',(-0.0116698995197312,0.0153649181792621,0.0404480984064987));
#42709=CARTESIAN_POINT('',(-0.0132419645360361,0.01422343802526,0.0406869447264834));
#42710=CARTESIAN_POINT('',(-0.0131914477879221,0.0141683084749517,0.0406626190329021));
#42711=CARTESIAN_POINT('',(-0.0131495970747723,0.0141201765420058,0.0405751279738163));
#42712=CARTESIAN_POINT('',(-0.0131510178975401,0.0141188503836186,0.0404968709562312));
#42713=CARTESIAN_POINT('',(-0.0157858403880931,0.011334670738937,0.0407814369533176));
#42714=CARTESIAN_POINT('',(-0.0157253427703919,0.0112905215962408,0.0407572027913683));
#42715=CARTESIAN_POINT('',(-0.0156746531259851,0.0112515127002032,0.0406696058633485));
#42716=CARTESIAN_POINT('',(-0.0156757612826429,0.0112499651602134,0.0405912619422651));
#42717=CARTESIAN_POINT('',(-0.0168337225819455,0.0097128872234943,0.0408280824322182));
#42718=CARTESIAN_POINT('',(-0.0167690424369808,0.00967490186409546,0.0408039349928322));
#42719=CARTESIAN_POINT('',(-0.0167146050123985,0.00964099036924619,0.0407162417069933));
#42720=CARTESIAN_POINT('',(-0.0167155867809466,0.00963928678279519,0.0406378188741549));
#42721=CARTESIAN_POINT('',(-0.018423271651614,0.00618680701624641,0.0409245341856734));
#42722=CARTESIAN_POINT('',(-0.0183525530717912,0.006162448432523,0.0409002225940088));
#42723=CARTESIAN_POINT('',(-0.0182927812174779,0.0061401035270347,0.0408127157048635));
#42724=CARTESIAN_POINT('',(-0.0182934027154407,0.0061382496041647,0.0407344457386575));
#42725=CARTESIAN_POINT('',(-0.0189430547325762,0.0043443461353158,0.0409710362127245));
#42726=CARTESIAN_POINT('',(-0.0188702341171792,0.00432704686481311,0.0409467617589281));
#42727=CARTESIAN_POINT('',(-0.0188084758538503,0.00431069829717667,0.0408592105361161));
#42728=CARTESIAN_POINT('',(-0.0188089018133566,0.00430884403332253,0.0407809041095408));
#42729=CARTESIAN_POINT('',(-0.0194289986128713,0.000499713531233832,0.0410656760686004));
#42730=CARTESIAN_POINT('',(-0.0193539583666749,0.000497198497755513,0.0410415831174496));
#42731=CARTESIAN_POINT('',(-0.0192898275617786,0.000493392807686237,0.0409538266520444));
#42732=CARTESIAN_POINT('',(-0.0192898777469486,0.000491468041456822,0.040875351896354));
#42733=CARTESIAN_POINT('',(-0.0193817406628462,-0.00142299211126438,0.0411135075422031));
#42734=CARTESIAN_POINT('',(-0.0193070170772642,-0.00141809444964756,0.0410892654598308));
#42735=CARTESIAN_POINT('',(-0.019243117359171,-0.00141559108917121,0.0410016800819513));
#42736=CARTESIAN_POINT('',(-0.0192429699175204,-0.00141755853501489,0.040923345775823));
#42737=CARTESIAN_POINT('',(-0.0187193942117811,-0.00522021721159691,0.0412091471935832));
#42738=CARTESIAN_POINT('',(-0.0186472127981405,-0.0052006845494549,0.0411848232168061));
#42739=CARTESIAN_POINT('',(-0.0185852342022787,-0.0051856082833503,0.0410973294412903));
#42740=CARTESIAN_POINT('',(-0.0185847148569473,-0.00518745960300022,0.0410190701522683));
#42741=CARTESIAN_POINT('',(-0.0181039359117161,-0.00706460040595502,0.0412555665134694));
#42742=CARTESIAN_POINT('',(-0.0180338532992189,-0.00703785993463442,0.0412314243596961));
#42743=CARTESIAN_POINT('',(-0.0179733690213254,-0.00701652438380678,0.0411437230827132));
#42744=CARTESIAN_POINT('',(-0.0179726792551525,-0.00701830153821873,0.0410652935604343));
#42745=CARTESIAN_POINT('',(-0.0163613828719178,-0.0104861909729681,0.0413506434124658));
#42746=CARTESIAN_POINT('',(-0.0162979641669806,-0.0104462472372041,0.0413264544004279));
#42747=CARTESIAN_POINT('',(-0.0162428869540188,-0.0104135600110401,0.0412388091539726));
#42748=CARTESIAN_POINT('',(-0.0162418185736249,-0.0104152333392688,0.0411604257625291));
#42749=CARTESIAN_POINT('',(-0.0152223786671565,-0.0120789136020188,0.0413992881003474));
#42750=CARTESIAN_POINT('',(-0.0151634461213869,-0.0120329066992753,0.0413749569533594));
#42751=CARTESIAN_POINT('',(-0.0151121781877566,-0.0119949854999305,0.0412874718141746));
#42752=CARTESIAN_POINT('',(-0.0151109728566117,-0.0119965009218216,0.0412092196393451));
#42753=CARTESIAN_POINT('',(-0.0125568686401054,-0.0148311281959786,0.0414931318161541));
#42754=CARTESIAN_POINT('',(-0.012508011411256,-0.0147743157003177,0.0414689287321229));
#42755=CARTESIAN_POINT('',(-0.0124650463432653,-0.0147268539152569,0.0413812963157667));
#42756=CARTESIAN_POINT('',(-0.0124635942482089,-0.0147280804403202,0.0413029232831929));
#42757=CARTESIAN_POINT('',(-0.010995231801385,-0.0160233379181721,0.0415406428119252));
#42758=CARTESIAN_POINT('',(-0.0109523014847925,-0.0159617922274038,0.0415165240644872));
#42759=CARTESIAN_POINT('',(-0.0109142176058814,-0.0159101249346095,0.0414287983483162));
#42760=CARTESIAN_POINT('',(-0.0109125933109026,-0.0159112383674669,0.0413503489155356));
#42761=CARTESIAN_POINT('',(-0.00764011994476365,-0.0178674958607134,0.0416362600396937));
#42762=CARTESIAN_POINT('',(-0.00761018133565773,-0.017798951100108,0.0416119553101224));
#42763=CARTESIAN_POINT('',(-0.00758312062253375,-0.0177411528083686,0.0415244406939323));
#42764=CARTESIAN_POINT('',(-0.00758131839265829,-0.0177419224038618,0.0414461644041004));
#42765=CARTESIAN_POINT('',(-0.00579698462809434,-0.0185478388243877,0.0416841102526258));
#42766=CARTESIAN_POINT('',(-0.00577410687134877,-0.01847659559011,0.0416598265164387));
#42767=CARTESIAN_POINT('',(-0.00575303316508779,-0.0184163131855544,0.04157228606953));
#42768=CARTESIAN_POINT('',(-0.0057512140507308,-0.0184168822966398,0.0414939884842142));
#42769=CARTESIAN_POINT('',(-0.00204511726705045,-0.0193252414217171,0.0417777971524379));
#42770=CARTESIAN_POINT('',(-0.00203664008434553,-0.0192506900880234,0.0417536717205969));
#42771=CARTESIAN_POINT('',(-0.00202774868857115,-0.019187136766194,0.0416659520810417));
#42772=CARTESIAN_POINT('',(-0.00202583336017481,-0.019187339987148,0.0415875075428947));
#42773=CARTESIAN_POINT('',(-9.05804658936935E-5,-0.0194329094892977,0.0418264478471602));
#42774=CARTESIAN_POINT('',(-8.9642911205528E-5,-0.0193580705522084,0.0418021777740408));
#42775=CARTESIAN_POINT('',(-8.71656546924683E-5,-0.019294227531414,0.0417146241096909));
#42776=CARTESIAN_POINT('',(-8.51986897315877E-5,-0.0192942337059858,0.0416363157991664));
#42777=CARTESIAN_POINT('',(0.00373284185397302,-0.0190711043162353,0.0419214916564631));
#42778=CARTESIAN_POINT('',(0.00371903948671961,-0.0189975958351805,0.0418971816093208));
#42779=CARTESIAN_POINT('',(0.00370887284137344,-0.018934599967898,0.0418096717232319));
#42780=CARTESIAN_POINT('',(0.00371075297471115,-0.0189342289380529,0.0417313992090289));
#42781=CARTESIAN_POINT('',(0.0056195348488219,-0.0186041914397168,0.041967771073828));
#42782=CARTESIAN_POINT('',(0.00559837174197131,-0.0185321764440214,0.0419436646493534));
#42783=CARTESIAN_POINT('',(0.0055818376167325,-0.0184701315167897,0.0418559229912704));
#42784=CARTESIAN_POINT('',(0.00558366573546322,-0.0184695830661741,0.041777460339377));
#42785=CARTESIAN_POINT('',(0.00918111747785819,-0.0171287475784746,0.0420633382769924));
#42786=CARTESIAN_POINT('',(0.00914621849626832,-0.0170623881114195,0.0420391678140263));
#42787=CARTESIAN_POINT('',(0.00911790208787631,-0.0170048972731719,0.0419515016544082));
#42788=CARTESIAN_POINT('',(0.00911965739953659,-0.0170039604386378,0.0418731011158541));
#42789=CARTESIAN_POINT('',(0.0108287157855478,-0.0161383651826623,0.0421111871737686));
#42790=CARTESIAN_POINT('',(0.0107875443681479,-0.0160759437721169,0.0420868590299796));
#42791=CARTESIAN_POINT('',(0.0107538243240508,-0.0160218044754006,0.0419993706635951));
#42792=CARTESIAN_POINT('',(0.0107554348807014,-0.0160207209592401,0.041921115849482));
#42793=CARTESIAN_POINT('',(0.0138163523926375,-0.0136685566777615,0.0422062857606146));
#42794=CARTESIAN_POINT('',(0.0137635062306705,-0.0136154636695298,0.0421820602826808));
#42795=CARTESIAN_POINT('',(0.0137195386676774,-0.0135689798753639,0.0420944534535886));
#42796=CARTESIAN_POINT('',(0.0137208756379874,-0.0135676251147251,0.0420161014120124));
#42797=CARTESIAN_POINT('',(0.0150937991990989,-0.0122429033161526,0.0422526218686467));
#42798=CARTESIAN_POINT('',(0.0150359189264516,-0.0121952115724331,0.0422284654018838));
#42799=CARTESIAN_POINT('',(0.0149875171517796,-0.0121531589775004,0.0421407824163082));
#42800=CARTESIAN_POINT('',(0.0149887556291129,-0.012151630069666,0.0420623680363629));
#42801=CARTESIAN_POINT('',(0.0172184502353371,-0.009012020296029,0.0423490045947479));
#42802=CARTESIAN_POINT('',(0.0171524539800783,-0.00897682604798362,0.042324691488919));
#42803=CARTESIAN_POINT('',(0.0170969498824196,-0.00894534784936932,0.0422371862082005));
#42804=CARTESIAN_POINT('',(0.0170978537102632,-0.0089436182365821,0.0421589175519357));
#42805=CARTESIAN_POINT('',(0.0180274816378425,-0.00725761467570689,0.0423958372533736));
#42806=CARTESIAN_POINT('',(0.0179582537787476,-0.00722911756875251,0.0423715794694566));
#42807=CARTESIAN_POINT('',(0.0178997912496169,-0.00720328948227317,0.0422840092016225));
#42808=CARTESIAN_POINT('',(0.0179005019669257,-0.00720152699125071,0.0422056871496299));
#42809=CARTESIAN_POINT('',(0.0191046950454922,-0.00356301633164709,0.0424898936854717));
#42810=CARTESIAN_POINT('',(0.0190309951402892,-0.00354867574103588,0.0424658045978915));
#42811=CARTESIAN_POINT('',(0.0189682692840251,-0.00353477957180662,0.0423780440089436));
#42812=CARTESIAN_POINT('',(0.0189686243930409,-0.0035328813041711,0.0422995658792278));
#42813=CARTESIAN_POINT('',(0.0193644544292967,-0.00163030860279191,0.0425384839417672));
#42814=CARTESIAN_POINT('',(0.0192899038645396,-0.00162344189871589,0.0425142307870624));
#42815=CARTESIAN_POINT('',(0.0192264252594773,-0.00161590860419999,0.0424266579222541));
#42816=CARTESIAN_POINT('',(0.0192265874470749,-0.0016139458694519,0.0423483338702482));
#42817=CARTESIAN_POINT('',(0.0193072408081446,0.00220542823088705,0.0426334895036402));
#42818=CARTESIAN_POINT('',(0.01923286195712,0.00219751006854614,0.0426091846427798));
#42819=CARTESIAN_POINT('',(0.019169247600259,0.0021923811499423,0.0425216688740683));
#42820=CARTESIAN_POINT('',(0.0191690269526096,0.00219428617542683,0.0424433915393039));
#42821=CARTESIAN_POINT('',(0.0189869068886521,0.00414048987402366,0.0426802037297687));
#42822=CARTESIAN_POINT('',(0.01891345262312,0.00412504746132331,0.0426561010076335));
#42823=CARTESIAN_POINT('',(0.0188502989803406,0.00411343336493398,0.0425683550470634));
#42824=CARTESIAN_POINT('',(0.0188498968568833,0.00411529619648721,0.0424898888595828));
#42825=CARTESIAN_POINT('',(0.0178060736540218,0.0077833268932127,0.0427752115903381));
#42826=CARTESIAN_POINT('',(0.0177371541792912,0.00775384712325843,0.0427510318674556));
#42827=CARTESIAN_POINT('',(0.017677604400204,0.00773022695108189,0.0426633764366052));
#42828=CARTESIAN_POINT('',(0.0176768086339158,0.00773205734716713,0.0425849847137418));
#42829=CARTESIAN_POINT('',(0.0169282222197374,0.00954199709281463,0.0428242133111679));
#42830=CARTESIAN_POINT('',(0.0168628218514916,0.00950581417344825,0.0427998657441485));
#42831=CARTESIAN_POINT('',(0.0168062687037002,0.00947642024545496,0.0427123993667165));
#42832=CARTESIAN_POINT('',(0.0168053156255896,0.0094781059476651,0.0426341625770041));
#42833=CARTESIAN_POINT('',(0.0152787301216398,0.0118928357701172,0.0428944730874302));
#42834=CARTESIAN_POINT('',(0.0152195044455773,0.0118474598128942,0.0428702336640911));
#42835=CARTESIAN_POINT('',(0.0151679575922512,0.0118100113144053,0.0427826428309556));
#42836=CARTESIAN_POINT('',(0.0151667907386638,0.0118115087985106,0.0427043039122707));
#42837=CARTESIAN_POINT('',(0.0146717483068224,0.0126350518476812,0.0429176501654895));
#42838=CARTESIAN_POINT('',(0.0146147700280014,0.0125867335795153,0.0428934842250373));
#42839=CARTESIAN_POINT('',(0.0145650311406933,0.0125466826050009,0.0428058098733814));
#42840=CARTESIAN_POINT('',(0.0145637933589508,0.0125481208887642,0.0427274024400431));
#42841=CARTESIAN_POINT('',(0.0133400624183863,0.0140340131728593,0.0429650606966497));
#42842=CARTESIAN_POINT('',(0.0132881303661509,0.0139802216821325,0.0429409428302006));
#42843=CARTESIAN_POINT('',(0.0132425288710425,0.0139353796424642,0.0428532155792548));
#42844=CARTESIAN_POINT('',(0.013241122291298,0.0139367175227223,0.0427747648303184));
#42845=CARTESIAN_POINT('',(0.0126150983580388,0.0146866171639263,0.042989652595112));
#42846=CARTESIAN_POINT('',(0.0125664024074084,0.0146304267516039,0.0429647923161076));
#42847=CARTESIAN_POINT('',(0.0125248389268988,0.0145834093453335,0.0428775280838563));
#42848=CARTESIAN_POINT('',(0.0125244674148037,0.0145837132205409,0.042799403358162));
#42849=CARTESIAN_POINT('',(0.0118641087128433,0.0152851839160009,0.0429958229345714));
#42850=CARTESIAN_POINT('',(0.0118157461105819,0.0152229742289092,0.0429751567186458));
#42851=CARTESIAN_POINT('',(0.0117723227925367,0.0151674788982722,0.0428837874796227));
#42852=CARTESIAN_POINT('',(0.0117721272428104,0.015167630671238,0.04280232572374));
#42853=CARTESIAN_POINT('',(0.0136941102546716,0.013457761490415,0.0337585246215808));
#42854=CARTESIAN_POINT('',(0.0135895474492647,0.013564160655447,0.0337622503149065));
#42855=CARTESIAN_POINT('',(0.01334654683062,0.0138064699816532,0.0337708464888983));
#42856=CARTESIAN_POINT('',(0.0128765937054183,0.0142481009367531,0.0337870668407993));
#42857=CARTESIAN_POINT('',(0.0123812852719009,0.0146790102787035,0.0338036262209131));
#42858=CARTESIAN_POINT('',(0.011936906974365,0.0150409981913683,0.0338181036860316));
#42859=CARTESIAN_POINT('',(0.0115301573081769,0.0153545232374545,0.0338310925608864));
#42860=CARTESIAN_POINT('',(0.0112446290788422,0.015564003170425,0.0338400407264213));
#42861=CARTESIAN_POINT('',(0.0108253784832943,0.0158609026048407,0.0338529843428364));
#42862=CARTESIAN_POINT('',(0.010324636018273,0.0161929424871847,0.0338680560525854));
#42863=CARTESIAN_POINT('',(0.00972406948175458,0.0165597766514572,0.0338856035628603));
#42864=CARTESIAN_POINT('',(0.0091724403886533,0.0168718086851734,0.0339012951499738));
#42865=CARTESIAN_POINT('',(0.00852858148303964,0.0172069826354789,0.0339191663943377));
#42866=CARTESIAN_POINT('',(0.00789371996930137,0.0175068391635713,0.0339363895649794));
#42867=CARTESIAN_POINT('',(0.007353800789958,0.017738735947024,0.0339507482859093));
#42868=CARTESIAN_POINT('',(0.00696670183591407,0.0178920847815684,0.0339608928198493));
#42869=CARTESIAN_POINT('',(0.00675326239252082,0.0179734876172019,0.033966451706429));
#42870=CARTESIAN_POINT('',(0.00656721188965184,0.0180421563621817,0.0339712701462319));
#42871=CARTESIAN_POINT('',(0.00647774007262375,0.018074345239179,0.0339735851140953));
#42872=CARTESIAN_POINT('',(0.00631178123728991,0.0181332991798986,0.0339778913305606));
#42873=CARTESIAN_POINT('',(0.00601080715784662,0.0182365193187258,0.0339857151080177));
#42874=CARTESIAN_POINT('',(0.00549520048212785,0.0184015890871872,0.0339991324785569));
#42875=CARTESIAN_POINT('',(0.00486734732829062,0.01857623817052,0.0340154149159029));
#42876=CARTESIAN_POINT('',(0.00431522273416663,0.018710900877931,0.0340296727710237));
#42877=CARTESIAN_POINT('',(0.00382175659852987,0.0188175153011505,0.0340423767830938));
#42878=CARTESIAN_POINT('',(0.00347079643802958,0.0188847748277211,0.034051372586562));
#42879=CARTESIAN_POINT('',(0.00295799950639641,0.018973974806623,0.0340644528912556));
#42880=CARTESIAN_POINT('',(0.00209444891561219,0.0190965256364289,0.0340863242877525));
#42881=CARTESIAN_POINT('',(0.00088264967494292,0.0191971690537947,0.0341166697948567));
#42882=CARTESIAN_POINT('',(-0.000265183527458678,0.0192075069895004,0.0341451369917628));
#42883=CARTESIAN_POINT('',(-0.00104676910514645,0.019173434339615,0.0341644461903466));
#42884=CARTESIAN_POINT('',(-0.00146947003827434,0.0191447694438164,0.0341748775932301));
#42885=CARTESIAN_POINT('',(-0.00182217380906955,0.0191140171311492,0.0341835724100592));
#42886=CARTESIAN_POINT('',(-0.00201525877505204,0.0190942941612785,0.0341883416702004));
#42887=CARTESIAN_POINT('',(-0.00235530901830927,0.0190564618912583,0.0341967754294064));
#42888=CARTESIAN_POINT('',(-0.00297748392721909,0.0189740593513065,0.0342122985383287));
#42889=CARTESIAN_POINT('',(-0.00403678940420134,0.0187887784475889,0.034239022591207));
#42890=CARTESIAN_POINT('',(-0.0052889441035157,0.0184721107348805,0.0342712683636976));
#42891=CARTESIAN_POINT('',(-0.00625355214601337,0.0181576172995491,0.0342966798883434));
#42892=CARTESIAN_POINT('',(-0.00676271658551289,0.0179706639211776,0.0343102840321073));
#42893=CARTESIAN_POINT('',(-0.00704946142295342,0.0178596671197241,0.0343179998365711));
#42894=CARTESIAN_POINT('',(-0.00729501792534726,0.0177605771205138,0.0343246478509529));
#42895=CARTESIAN_POINT('',(-0.00743702325795866,0.0177013632470171,0.0343285094384181));
#42896=CARTESIAN_POINT('',(-0.00766141934138433,0.0176059659993698,0.0343346234804498));
#42897=CARTESIAN_POINT('',(-0.00803514983488992,0.0174404794253086,0.0343448579947234));
#42898=CARTESIAN_POINT('',(-0.0087850330542926,0.0170838852172053,0.0343655931162305));
#42899=CARTESIAN_POINT('',(-0.00961358323222665,0.0166315511648749,0.0343890271514878));
#42900=CARTESIAN_POINT('',(-0.010417114523336,0.0161335564903514,0.0344123822255873));
#42901=CARTESIAN_POINT('',(-0.0109074208000341,0.015803970647621,0.0344269254265874));
#42902=CARTESIAN_POINT('',(-0.0112919160733621,0.0155298062326985,0.0344385204583214));
#42903=CARTESIAN_POINT('',(-0.0115772453337043,0.0153182329300907,0.0344472264029292));
#42904=CARTESIAN_POINT('',(-0.0118091588638532,0.0151396810220304,0.0344543871753119));
#42905=CARTESIAN_POINT('',(-0.0119747865130799,0.0150083073640502,0.0344595520977263));
#42906=CARTESIAN_POINT('',(-0.0120610264990449,0.0149390577059178,0.0344622528669767));
#42907=CARTESIAN_POINT('',(-0.0121476861584109,0.0148686064259165,0.0344649779294458));
#42908=CARTESIAN_POINT('',(-0.0121490871942248,0.0148673937526884,0.0344650244436881));
#42909=CARTESIAN_POINT('',(-0.012185961924089,0.0148372383407356,0.0344661941039101));
#42910=CARTESIAN_POINT('',(-0.0122470677776355,0.0147869320183904,0.0344681504822471));
#42911=CARTESIAN_POINT('',(-0.0124227600987986,0.0146407236228182,0.0344738288083486));
#42912=CARTESIAN_POINT('',(-0.012715495880542,0.0143895546814955,0.0344834696544062));
#42913=CARTESIAN_POINT('',(-0.0130990369149521,0.014039692277915,0.0344964829696457));
#42914=CARTESIAN_POINT('',(-0.0134260848981876,0.013728183831799,0.0345078184723691));
#42915=CARTESIAN_POINT('',(-0.0137360546234464,0.0134168816015701,0.0345188546161402));
#42916=CARTESIAN_POINT('',(-0.0139882906799606,0.0131530959686775,0.0345280281181907));
#42917=CARTESIAN_POINT('',(-0.0142201817272134,0.0129015418221073,0.034536631612315));
#42918=CARTESIAN_POINT('',(-0.0143266064427612,0.0127826328112155,0.0345406433614217));
#42919=CARTESIAN_POINT('',(-0.0145066481029053,0.0125790201543027,0.0345474706117571));
#42920=CARTESIAN_POINT('',(-0.0147902746456681,0.0122471231614338,0.0345584219683724));
#42921=CARTESIAN_POINT('',(-0.015174778428772,0.0117700082232991,0.034573750880059));
#42922=CARTESIAN_POINT('',(-0.0155127292111199,0.0113174191605092,0.0345878245341603));
#42923=CARTESIAN_POINT('',(-0.0157362681348944,0.0110011849494621,0.0345974416553844));
#42924=CARTESIAN_POINT('',(-0.0158496869700815,0.0108369266575419,0.0346023906521781));
#42925=CARTESIAN_POINT('',(-0.0159571868772797,0.0106777061651138,0.0346071463999587));
#42926=CARTESIAN_POINT('',(-0.0159663462936758,0.0106637422864074,0.0346075577231221));
#42927=CARTESIAN_POINT('',(-0.0160276561327147,0.0105717118602376,0.0346102871836528));
#42928=CARTESIAN_POINT('',(-0.0161476069176707,0.0103888001327877,0.0346156758069228));
#42929=CARTESIAN_POINT('',(-0.0163581974103101,0.0100574369270042,0.0346253353556078));
#42930=CARTESIAN_POINT('',(-0.0166217923490061,0.00961328317443536,0.0346380332767143));
#42931=CARTESIAN_POINT('',(-0.0168446227175717,0.00921819835684225,0.0346491817224154));
#42932=CARTESIAN_POINT('',(-0.0170456288458299,0.00884020300519206,0.0346597012247684));
#42933=CARTESIAN_POINT('',(-0.0171960295178942,0.00854112137700337,0.0346679264580525));
#42934=CARTESIAN_POINT('',(-0.0172790049411183,0.00837171883319988,0.0346725610105133));
#42935=CARTESIAN_POINT('',(-0.0173547950476286,0.00821319909425432,0.0346768775789744));
#42936=CARTESIAN_POINT('',(-0.0173820928307441,0.00815499207037812,0.0346784576900277));
#42937=CARTESIAN_POINT('',(-0.0174348258340047,0.00804203806109061,0.0346815237131564));
#42938=CARTESIAN_POINT('',(-0.0175180723128191,0.00785997902884154,0.0346864537280027));
#42939=CARTESIAN_POINT('',(-0.0176376136993543,0.00758925941223894,0.0346937581407388));
#42940=CARTESIAN_POINT('',(-0.0177736098997301,0.00726500599075267,0.0347024643405804));
#42941=CARTESIAN_POINT('',(-0.0179481211417278,0.00682648423236474,0.0347141867892852));
#42942=CARTESIAN_POINT('',(-0.0181095832063446,0.00638655283579656,0.0347258777552459));
#42943=CARTESIAN_POINT('',(-0.0182627011614772,0.00592868581523455,0.0347379790976535));
#42944=CARTESIAN_POINT('',(-0.0183620783579825,0.00561489817091336,0.0347462570227646));
#42945=CARTESIAN_POINT('',(-0.0184911675089137,0.00517537833237663,0.0347577897996903));
#42946=CARTESIAN_POINT('',(-0.018633074967421,0.00464483147881868,0.034771595644462));
#42947=CARTESIAN_POINT('',(-0.0188493565307284,0.00372059112093591,0.0347954200936349));
#42948=CARTESIAN_POINT('',(-0.0190550954247574,0.00249158709200293,0.0348265651563859));
#42949=CARTESIAN_POINT('',(-0.0191790575163336,0.00115543871336813,0.0348599221754414));
#42950=CARTESIAN_POINT('',(-0.0192,0.000367624981005561,0.0348793718366157));
#42951=CARTESIAN_POINT('',(-0.0192,0.,0.0348884087721565));
#42952=CARTESIAN_POINT('',(0.0136941126101477,0.0134577620508462,0.0337585747238691));
#42953=CARTESIAN_POINT('',(-0.0192,1.85786059226098E-19,0.0348884087721565));
#42954=CARTESIAN_POINT('',(0.0136941154444571,0.0134577621240347,0.0337586248089782));
#42955=CARTESIAN_POINT('',(0.0136826371269313,0.0134694418914976,0.0337617141202682));
#42956=CARTESIAN_POINT('',(0.0136430578016153,0.013509394949222,0.0337721504615356));
#42957=CARTESIAN_POINT('',(0.0134399334786531,0.0137221538478718,0.0338277048930865));
#42958=CARTESIAN_POINT('',(0.0133538196812112,0.0138190636682607,0.0338522664919164));
#42959=CARTESIAN_POINT('',(0.0133075373500049,0.0138718845916857,0.0338655904181358));
#42960=CARTESIAN_POINT('',(0.0129669874288091,0.0143467767916369,0.0339772843973612));
#42961=CARTESIAN_POINT('',(0.0115713800653362,0.0156079658614213,0.0340242546179052));
#42962=CARTESIAN_POINT('',(0.00917172797759027,0.0172065231735504,0.0340957211296002));
#42963=CARTESIAN_POINT('',(0.00565700559390481,0.0185655378803378,0.0341863739834551));
#42964=CARTESIAN_POINT('',(0.00286356960593685,0.0191945939613825,0.0342580305967084));
#42965=CARTESIAN_POINT('',(6.00390298951636E-5,0.0194071967834707,0.0343276084462218));
#42966=CARTESIAN_POINT('',(-0.00280547377715355,0.0192040953034031,0.0343972796574007));
#42967=CARTESIAN_POINT('',(-0.00555104901130441,0.0185964846565865,0.0344666190124259));
#42968=CARTESIAN_POINT('',(-0.00911660442038569,0.0172386681088485,0.0345620081421828));
#42969=CARTESIAN_POINT('',(-0.0122793980430035,0.0151500481911074,0.0346526132888181));
#42970=CARTESIAN_POINT('',(-0.0149232917304808,0.0124063671395135,0.0347478780396232));
#42971=CARTESIAN_POINT('',(-0.0165616126372687,0.0101175449752386,0.0348171161399589));
#42972=CARTESIAN_POINT('',(-0.0178737227091099,0.00756282226843125,0.0348866382876858));
#42973=CARTESIAN_POINT('',(-0.0187779015622702,0.00490239274816994,0.0349565395549962));
#42974=CARTESIAN_POINT('',(-0.0192952846344691,0.00208222391132934,0.035027924969667));
#42975=CARTESIAN_POINT('',(-0.0194268294272506,-0.00167922858791242,0.0351192514716495));
#42976=CARTESIAN_POINT('',(-0.0187196013062885,-0.00545527351177937,0.0352143794552229));
#42977=CARTESIAN_POINT('',(-0.0172399183781032,-0.00891304084397672,0.0353065595114178));
#42978=CARTESIAN_POINT('',(-0.0157375834854316,-0.0113573828877688,0.0353761580765403));
#42979=CARTESIAN_POINT('',(-0.0139325142252646,-0.0135103121249464,0.0354464263275229));
#42980=CARTESIAN_POINT('',(-0.0117870130508438,-0.0154180328418685,0.0355175145555988));
#42981=CARTESIAN_POINT('',(-0.00943081487800948,-0.0169618553426991,0.0355857575287973));
#42982=CARTESIAN_POINT('',(-0.0059780389972534,-0.0185615634550717,0.0356801290647163));
#42983=CARTESIAN_POINT('',(-0.00227155551396098,-0.0193687118024069,0.0357728320835663));
#42984=CARTESIAN_POINT('',(0.00154447697031841,-0.0193459848972831,0.0358658407634035));
#42985=CARTESIAN_POINT('',(0.0043234624990737,-0.0189197123559901,0.0359362675419697));
#42986=CARTESIAN_POINT('',(0.0070686233449079,-0.0180743485664414,0.0360069893486505));
#42987=CARTESIAN_POINT('',(0.00960729763734257,-0.0168625579867165,0.0360751939385716));
#42988=CARTESIAN_POINT('',(0.0119817385251178,-0.0152679901260296,0.036146398333989));
#42989=CARTESIAN_POINT('',(0.0140751032296404,-0.0133602052681052,0.0362165935557949));
#42990=CARTESIAN_POINT('',(0.0158720725358971,-0.0111697360825902,0.0362853008234503));
#42991=CARTESIAN_POINT('',(0.017339924630644,-0.00871616399730907,0.0363556492418429));
#42992=CARTESIAN_POINT('',(0.01841839670659,-0.00611632933404608,0.0364260662584277));
#42993=CARTESIAN_POINT('',(0.0191193204551073,-0.00333208225338983,0.0364963626431574));
#42994=CARTESIAN_POINT('',(0.0194001577826843,-0.000534679403752089,0.0365647528474457));
#42995=CARTESIAN_POINT('',(0.0192236717854676,0.00327853672896307,0.0366602725835808));
#42996=CARTESIAN_POINT('',(0.018224829179944,0.00693697048911509,0.0367513080216613));
#42997=CARTESIAN_POINT('',(0.0164475669963537,0.0103015758611845,0.0368454846683361));
#42998=CARTESIAN_POINT('',(0.0147828163275645,0.0125743553559636,0.0369157664930877));
#42999=CARTESIAN_POINT('',(0.0127662795816731,0.0146175804468894,0.036985696406264));
#43000=CARTESIAN_POINT('',(0.010521926670691,0.0163078537119878,0.0370544310064815));
#43001=CARTESIAN_POINT('',(0.00800300191271364,0.0176804927319421,0.0371262210936272));
#43002=CARTESIAN_POINT('',(0.00447259200101117,0.0189788791549912,0.0372181259863815));
#43003=CARTESIAN_POINT('',(0.000664909643921832,0.0194877876118655,0.0373117878618414));
#43004=CARTESIAN_POINT('',(-0.00308456505535271,0.0191606283485715,0.0374054362510788));
#43005=CARTESIAN_POINT('',(-0.00587409426056678,0.0184972029882785,0.0374750047751963));
#43006=CARTESIAN_POINT('',(-0.00848360455853172,0.0174551515786284,0.0375442942774273));
#43007=CARTESIAN_POINT('',(-0.0109666974490278,0.0160118766280472,0.0376159401009681));
#43008=CARTESIAN_POINT('',(-0.0131672264635854,0.0142568604798726,0.0376845401175858));
#43009=CARTESIAN_POINT('',(-0.0157688169313013,0.0114739692250601,0.0377774471690446));
#43010=CARTESIAN_POINT('',(-0.0176905845230479,0.00820506762897047,0.0378720135163756));
#43011=CARTESIAN_POINT('',(-0.0188604585521843,0.00457496739751311,0.0379643254507625));
#43012=CARTESIAN_POINT('',(-0.0193238678886162,0.00180099601517996,0.038034217719475));
#43013=CARTESIAN_POINT('',(-0.0193776974386726,-0.00107110904910607,0.0381055592469513));
#43014=CARTESIAN_POINT('',(-0.0190194600004675,-0.0038596155043962,0.0381738069591164));
#43015=CARTESIAN_POINT('',(-0.0182460090102748,-0.00661678492586967,0.0382440393960188));
#43016=CARTESIAN_POINT('',(-0.017087926902402,-0.00919618802446331,0.0383148490752953));
#43017=CARTESIAN_POINT('',(-0.0155783506063201,-0.0115757708632551,0.0383839682823852));
#43018=CARTESIAN_POINT('',(-0.0130632358203733,-0.0144816519499531,0.0384773950900149));
#43019=CARTESIAN_POINT('',(-0.010025782979492,-0.0167255305076173,0.0385715559135774));
#43020=CARTESIAN_POINT('',(-0.00653620922525659,-0.0182738357125707,0.038663894601552));
#43021=CARTESIAN_POINT('',(-0.00382731274404074,-0.0190266288203552,0.0387334537957832));
#43022=CARTESIAN_POINT('',(-0.000976733981174734,-0.0193826570182263,0.0388051700031889));
#43023=CARTESIAN_POINT('',(0.00183431259761074,-0.0193202229377954,0.0388737808129606));
#43024=CARTESIAN_POINT('',(0.00465688500635297,-0.0188410216106093,0.0389436412511739));
#43025=CARTESIAN_POINT('',(0.00824013858898105,-0.0176721532478986,0.0390380543124924));
#43026=CARTESIAN_POINT('',(0.0115444908180822,-0.0157139654073397,0.0391299297625707));
#43027=CARTESIAN_POINT('',(0.014282567866367,-0.0131403805311297,0.0392233974621493));
#43028=CARTESIAN_POINT('',(0.0160642150400973,-0.0108892151776004,0.0392947924092649));
#43029=CARTESIAN_POINT('',(0.0174689157689923,-0.00845486378107598,0.0393630514512943));
#43030=CARTESIAN_POINT('',(0.0185240980053153,-0.00579015455245212,0.0394335621023632));
#43031=CARTESIAN_POINT('',(0.0191668143900673,-0.00304030331008378,0.039504060297298));
#43032=CARTESIAN_POINT('',(0.0194070059599408,-0.00020585768527927,0.0395735746428004));
#43033=CARTESIAN_POINT('',(0.0192272197225004,0.00263703515499631,0.0396428116900019));
#43034=CARTESIAN_POINT('',(0.018642647445271,0.00539604189027514,0.0397133466396609));
#43035=CARTESIAN_POINT('',(0.0176426254569399,0.00808509465012985,0.0397842936399775));
#43036=CARTESIAN_POINT('',(0.016290883612116,0.0105484058535663,0.0398523810041133));
#43037=CARTESIAN_POINT('',(0.0145569267682256,0.0128356891429286,0.0399235328516493));
#43038=CARTESIAN_POINT('',(0.0118723213903701,0.0154668195912942,0.0400169915385569));
#43039=CARTESIAN_POINT('',(0.00861024551575036,0.0174959563819991,0.040108902747744));
#43040=CARTESIAN_POINT('',(0.00505465403671454,0.0187375722405681,0.0402032500102804));
#43041=CARTESIAN_POINT('',(0.0022406078308495,0.0192773142856526,0.0402736766567547));
#43042=CARTESIAN_POINT('',(-0.000567815702499361,0.0193996097737672,0.0403419104891806));
#43043=CARTESIAN_POINT('',(-0.00342343385126204,0.019103229646225,0.040413410340871));
#43044=CARTESIAN_POINT('',(-0.00615038409441286,0.0184065111805356,0.0404831263946253));
#43045=CARTESIAN_POINT('',(-0.0096686184475022,0.0169361375016966,0.0405754200348359));
#43046=CARTESIAN_POINT('',(-0.0127612579722979,0.014745466048664,0.0406696667323146));
#43047=CARTESIAN_POINT('',(-0.0153174985528208,0.0119167439622277,0.0407630226618228));
#43048=CARTESIAN_POINT('',(-0.0168803478268236,0.00957730141101147,0.0408314952578956));
#43049=CARTESIAN_POINT('',(-0.0181084201448125,0.00698073191123133,0.040903316503968));
#43050=CARTESIAN_POINT('',(-0.0189264976843559,0.00429183545878377,0.040972517770357));
#43051=CARTESIAN_POINT('',(-0.0193532395078142,0.00145820300039777,0.0410418486064576));
#43052=CARTESIAN_POINT('',(-0.0193620320611151,-0.00230749915773812,0.0411356242159793));
#43053=CARTESIAN_POINT('',(-0.0185332483892014,-0.00605879754200571,0.0412293706720468));
#43054=CARTESIAN_POINT('',(-0.016943283271981,-0.00946543418309202,0.0413213013145344));
#43055=CARTESIAN_POINT('',(-0.015361383898717,-0.011860165190698,0.0413930810113919));
#43056=CARTESIAN_POINT('',(-0.0134878684246655,-0.0139539968664765,0.041461859993234));
#43057=CARTESIAN_POINT('',(-0.011283505722983,-0.0157915277757609,0.041531474060057));
#43058=CARTESIAN_POINT('',(-0.00887573630878226,-0.0172579423885106,0.0416019244936904));
#43059=CARTESIAN_POINT('',(-0.00625374805766054,-0.0183727273844134,0.0416725169175158));
#43060=CARTESIAN_POINT('',(-0.0035009432514515,-0.0190884916581397,0.0417415286098294));
#43061=CARTESIAN_POINT('',(-0.000694024097694391,-0.0193957179364182,0.041811277677145));
#43062=CARTESIAN_POINT('',(0.00217039459611988,-0.0192850364083003,0.0418827211420678));
#43063=CARTESIAN_POINT('',(0.00493306079849546,-0.0187701014847105,0.0419511700517889));
#43064=CARTESIAN_POINT('',(0.00764936514413544,-0.017837231574939,0.0420211945202578));
#43065=CARTESIAN_POINT('',(0.0101479004136944,-0.016541940153591,0.0420917118837952));
#43066=CARTESIAN_POINT('',(0.0124680747395051,-0.0148733882123723,0.0421621302592813));
#43067=CARTESIAN_POINT('',(0.0145011247329489,-0.012897360404977,0.0422308513194342));
#43068=CARTESIAN_POINT('',(0.0162238523411861,-0.0106518911739671,0.0423012625647974));
#43069=CARTESIAN_POINT('',(0.0176125742791933,-0.00814946075124356,0.0423722297397302));
#43070=CARTESIAN_POINT('',(0.0186067193865136,-0.00551875898010681,0.042440438355834));
#43071=CARTESIAN_POINT('',(0.0192174809116328,-0.00271201785770265,0.0425110817790405));
#43072=CARTESIAN_POINT('',(0.0194065096006142,9.34149747220036E-5,0.0425814604532221));
#43073=CARTESIAN_POINT('',(0.0191081892507249,0.00389774562463771,0.0426745473591831));
#43074=CARTESIAN_POINT('',(0.0179919903563871,0.007520895965826,0.042767400870812));
#43075=CARTESIAN_POINT('',(0.0161048328482777,0.0108289039411657,0.0428618782301824));
#43076=CARTESIAN_POINT('',(0.0149474287891037,0.0123060965833487,0.0429072185458034));
#43077=CARTESIAN_POINT('',(0.0143115152723113,0.0130059180970762,0.0429303525689935));
#43078=CARTESIAN_POINT('',(0.0138344501175927,0.013346906106166,0.0428477190027887));
#43079=CARTESIAN_POINT('',(0.0137810933123524,0.0133933759157219,0.0428378817273722));
#43080=CARTESIAN_POINT('',(0.0136815110794371,0.0134813833724383,0.0428194391764527));
#43081=CARTESIAN_POINT('',(0.0134677269994354,0.0136841748462814,0.0427787288709304));
#43082=CARTESIAN_POINT('',(0.0134262957679323,0.0137249207015359,0.0427708801730808));
#43083=CARTESIAN_POINT('',(0.0134137957134195,0.0137371265036079,0.0427684701217644));
#43084=CARTESIAN_POINT('',(0.0134138302057369,0.01373715900257,0.0427684304783987));
#43085=CARTESIAN_POINT('',(0.0192,6.20369116582113E-17,0.0423886526967672));
#43086=CARTESIAN_POINT('',(0.0192,8.41105296097433E-5,0.0423907560454785));
#43087=CARTESIAN_POINT('',(0.0191993101561165,0.000354898460622047,0.0423974844836466));
#43088=CARTESIAN_POINT('',(0.0191766387333424,0.00106850340612669,0.042415143749824));
#43089=CARTESIAN_POINT('',(0.0191112650346421,0.00191748446063122,0.0424361618456873));
#43090=CARTESIAN_POINT('',(0.019019580056546,0.00264245869365634,0.0424541897576075));
#43091=CARTESIAN_POINT('',(0.0189503569894495,0.00309282029534998,0.0424654289275442));
#43092=CARTESIAN_POINT('',(0.0188887797036297,0.00344944824861375,0.0424743542717575));
#43093=CARTESIAN_POINT('',(0.0188293966922826,0.00375842442754358,0.0424821124849691));
#43094=CARTESIAN_POINT('',(0.0187745744306113,0.00402076367859953,0.0424887206147141));
#43095=CARTESIAN_POINT('',(0.0187412404233969,0.00417342550003737,0.0424925731883303));
#43096=CARTESIAN_POINT('',(0.0187050520437726,0.00433168203525138,0.0424965755168272));
#43097=CARTESIAN_POINT('',(0.018696728057649,0.0043671315616813,0.0424974734143471));
#43098=CARTESIAN_POINT('',(0.0186766311706155,0.00445296219600791,0.0424996493623985));
#43099=CARTESIAN_POINT('',(0.0186366467243465,0.00461866745151867,0.0425038653622425));
#43100=CARTESIAN_POINT('',(0.0185680752589999,0.00488971898546871,0.0425108015077658));
#43101=CARTESIAN_POINT('',(0.0184688432623808,0.00525306123742752,0.0425201772806294));
#43102=CARTESIAN_POINT('',(0.0183491800792793,0.00565803440009305,0.042530716283468));
#43103=CARTESIAN_POINT('',(0.0181591486606039,0.00625031568604568,0.0425462733093148));
#43104=CARTESIAN_POINT('',(0.0179166470931237,0.00692068257031733,0.0425641419122045));
#43105=CARTESIAN_POINT('',(0.0176486931774257,0.00756587072340413,0.0425816911154129));
#43106=CARTESIAN_POINT('',(0.0174753152043798,0.00795521723283759,0.0425924075624996));
#43107=CARTESIAN_POINT('',(0.0173638688662241,0.00819524077046688,0.0425990644098585));
#43108=CARTESIAN_POINT('',(0.0172585053153977,0.00841378634159452,0.0426051703025579));
#43109=CARTESIAN_POINT('',(0.0171905663695672,0.00855179612008063,0.0426090415422495));
#43110=CARTESIAN_POINT('',(0.0170630931485617,0.0088055843917611,0.0426161809727479));
#43111=CARTESIAN_POINT('',(0.0168032065498494,0.00929884274092558,0.0426301691842053));
#43112=CARTESIAN_POINT('',(0.0164032373516879,0.00999415034658874,0.0426502129902482));
#43113=CARTESIAN_POINT('',(0.0157098656135333,0.0110705284649427,0.0426820419855479));
#43114=CARTESIAN_POINT('',(0.0147433274768177,0.0123493775949883,0.0427215469906524));
#43115=CARTESIAN_POINT('',(0.0138719316916315,0.0132898260649551,0.0427528145663577));
#43116=CARTESIAN_POINT('',(0.013413822225715,0.013737153027353,0.04276836728379));
#43117=CARTESIAN_POINT('',(0.0192,2.94926899266343E-17,0.0423886526967672));
#43118=CARTESIAN_POINT('',(-0.0192,8.05624845824862E-17,0.0408877752241749));
#43119=CARTESIAN_POINT('',(-0.0192,-0.000790229530708466,0.0409075953257136));
#43120=CARTESIAN_POINT('',(-0.0191024902357828,-0.00228924689105798,0.0409451529412056));
#43121=CARTESIAN_POINT('',(-0.0187518434727255,-0.00426572061081252,0.0409951852764988));
#43122=CARTESIAN_POINT('',(-0.0183528464081777,-0.00568448980504592,0.0410317662955944));
#43123=CARTESIAN_POINT('',(-0.0180088712099482,-0.00667252564303641,0.0410576537661434));
#43124=CARTESIAN_POINT('',(-0.0177787547011939,-0.00725516830706239,0.041073083335469));
#43125=CARTESIAN_POINT('',(-0.0176157987395533,-0.00763941139942041,0.0410833716631891));
#43126=CARTESIAN_POINT('',(-0.0174129376544513,-0.00809625754586341,0.0410957602633943));
#43127=CARTESIAN_POINT('',(-0.0171024529019984,-0.00874270830779054,0.0411136159336686));
#43128=CARTESIAN_POINT('',(-0.0166971635643165,-0.00949179650613317,0.0411349193872462));
#43129=CARTESIAN_POINT('',(-0.0163498797803306,-0.0100690098818459,0.0411518194785876));
#43130=CARTESIAN_POINT('',(-0.0161395567634752,-0.0104015023515241,0.0411617007389796));
#43131=CARTESIAN_POINT('',(-0.0159536165111858,-0.0106840701655911,0.041170204502041));
#43132=CARTESIAN_POINT('',(-0.0158288589915724,-0.010867525782549,0.0411757802417608));
#43133=CARTESIAN_POINT('',(-0.0156381862076702,-0.0111417113858313,0.0411841617472069));
#43134=CARTESIAN_POINT('',(-0.0153088209143396,-0.0115955027701945,0.0411982061191146));
#43135=CARTESIAN_POINT('',(-0.0149156448029552,-0.0120969775242192,0.041214101827745));
#43136=CARTESIAN_POINT('',(-0.0145132329713727,-0.0125728662887122,0.0412295875973739));
#43137=CARTESIAN_POINT('',(-0.0142075465558633,-0.0129173407929886,0.0412409994982153));
#43138=CARTESIAN_POINT('',(-0.0139460919157739,-0.0131978402099629,0.0412504731750429));
#43139=CARTESIAN_POINT('',(-0.0137678276758751,-0.0133828035863834,0.0412568064688921));
#43140=CARTESIAN_POINT('',(-0.0136555424293172,-0.0134969516717746,0.0412607492974457));
#43141=CARTESIAN_POINT('',(-0.0135992418411063,-0.0135539684744944,0.0412627210283634));
#43142=CARTESIAN_POINT('',(-0.0134352302934178,-0.0137168263728138,0.0412684062842928));
#43143=CARTESIAN_POINT('',(-0.0132579373716275,-0.0138885323308974,0.0412744781844828));
#43144=CARTESIAN_POINT('',(-0.0129382859541697,-0.0141897428025687,0.0412852846022242));
#43145=CARTESIAN_POINT('',(-0.0125174989864431,-0.0145631192702491,0.0412991295585662));
#43146=CARTESIAN_POINT('',(-0.0120576161914113,-0.0149451644540537,0.0413138536796516));
#43147=CARTESIAN_POINT('',(-0.0115178594071772,-0.0153674208124418,0.0413307452470723));
#43148=CARTESIAN_POINT('',(-0.0110975504615446,-0.0156700975264825,0.0413435336219379));
#43149=CARTESIAN_POINT('',(-0.0108386028116304,-0.0158484284729733,0.0413513286388253));
#43150=CARTESIAN_POINT('',(-0.0107453006271399,-0.0159116649237077,0.0413541314074882));
#43151=CARTESIAN_POINT('',(-0.0106893122950504,-0.0159492375281496,0.0413558140584502));
#43152=CARTESIAN_POINT('',(-0.0106829773279673,-0.0159535901620855,0.0413560053224019));
#43153=CARTESIAN_POINT('',(-0.0105608308634261,-0.0160348201908378,0.0413596787486931));
#43154=CARTESIAN_POINT('',(-0.0104376987303638,-0.0161153027447725,0.0413633632280166));
#43155=CARTESIAN_POINT('',(-0.0102020901654385,-0.0162666296622881,0.0413703793371311));
#43156=CARTESIAN_POINT('',(-0.00987146528891982,-0.0164701572903933,0.0413801137315337));
#43157=CARTESIAN_POINT('',(-0.00946462300536958,-0.0167073407298974,0.0413919325677006));
#43158=CARTESIAN_POINT('',(-0.00905315557312621,-0.016933798059228,0.0414037310715287));
#43159=CARTESIAN_POINT('',(-0.0086362788082987,-0.0171501887172174,0.0414155414712359));
#43160=CARTESIAN_POINT('',(-0.00821314098066917,-0.0173567373186424,0.0414273927491726));
#43161=CARTESIAN_POINT('',(-0.00786004973653656,-0.0175187131933612,0.0414371794146286));
#43162=CARTESIAN_POINT('',(-0.00760371557950614,-0.0176304334168209,0.0414442297417697));
#43163=CARTESIAN_POINT('',(-0.00746780894372702,-0.0176883667470539,0.0414479558176956));
#43164=CARTESIAN_POINT('',(-0.00733422672753375,-0.0177440740139076,0.0414516077630015));
#43165=CARTESIAN_POINT('',(-0.00732029263468191,-0.0177497329616383,0.0414519857541695));
#43166=CARTESIAN_POINT('',(-0.00725241481445632,-0.0177776665645231,0.041453829820565));
#43167=CARTESIAN_POINT('',(-0.00713795877204129,-0.0178241126689765,0.0414569192176163));
#43168=CARTESIAN_POINT('',(-0.00683112228250598,-0.0179457285808909,0.041465138017541));
#43169=CARTESIAN_POINT('',(-0.00633866199453227,-0.0181284176211699,0.0414781382628205));
#43170=CARTESIAN_POINT('',(-0.00569108838309847,-0.0183399452812841,0.0414949514488509));
#43171=CARTESIAN_POINT('',(-0.00512558263153796,-0.0185066345675347,0.041509481554257));
#43172=CARTESIAN_POINT('',(-0.00459315438703795,-0.018645292370458,0.0415230262911801));
#43173=CARTESIAN_POINT('',(-0.00417429553018401,-0.0187413310068665,0.0415335997738542));
#43174=CARTESIAN_POINT('',(-0.00394144610689307,-0.0187915288929255,0.0415394593793895));
#43175=CARTESIAN_POINT('',(-0.00371467452763229,-0.0188374569165726,0.0415451495876443));
#43176=CARTESIAN_POINT('',(-0.00366253993579643,-0.0188474385517718,0.0415464559038186));
#43177=CARTESIAN_POINT('',(-0.00352911882355083,-0.0188731229249262,0.0415498025895469));
#43178=CARTESIAN_POINT('',(-0.00331806670210132,-0.0189117969030331,0.0415550971105512));
#43179=CARTESIAN_POINT('',(-0.00298368362996883,-0.0189683135558426,0.0415634879824173));
#43180=CARTESIAN_POINT('',(-0.00256021784043124,-0.0190302474353696,0.0415741144451643));
#43181=CARTESIAN_POINT('',(-0.0019545748860709,-0.0191046696787996,0.0415893112575738));
#43182=CARTESIAN_POINT('',(-0.00129443594121435,-0.0191621433397765,0.0416058729550482));
#43183=CARTESIAN_POINT('',(-0.000660783499350027,-0.0191900885905044,0.0416217826982338));
#43184=CARTESIAN_POINT('',(-0.00029379549353288,-0.0191985486823184,0.0416310035722329));
#43185=CARTESIAN_POINT('',(1.40969858954864E-5,-0.0192006090827728,0.0416387469016346));
#43186=CARTESIAN_POINT('',(0.000230767535956538,-0.0191990147952285,0.0416441958506577));
#43187=CARTESIAN_POINT('',(0.000551430994764053,-0.0191932906497573,0.0416522519772854));
#43188=CARTESIAN_POINT('',(0.00109754635716764,-0.0191730128969162,0.0416659594214273));
#43189=CARTESIAN_POINT('',(0.00219831591572031,-0.0190920329812718,0.0416935604210137));
#43190=CARTESIAN_POINT('',(0.00344269095661963,-0.0189071248749801,0.0417248119050316));
#43191=CARTESIAN_POINT('',(0.00467056968104334,-0.0186312321044329,0.0417559255019949));
#43192=CARTESIAN_POINT('',(0.00542835809864762,-0.0184213500639201,0.041775291034865));
#43193=CARTESIAN_POINT('',(0.00602803088987008,-0.018231204772277,0.0417907434711645));
#43194=CARTESIAN_POINT('',(0.00639947443283039,-0.0181033265332761,0.0418003742150108));
#43195=CARTESIAN_POINT('',(0.00669540002907382,-0.017995266731838,0.0418080867822258));
#43196=CARTESIAN_POINT('',(0.00691435280541358,-0.0179123329850677,0.0418138133375932));
#43197=CARTESIAN_POINT('',(0.00710224597756983,-0.0178383401471856,0.0418187471727468));
#43198=CARTESIAN_POINT('',(0.00723788769643847,-0.0177836975605415,0.041822318358613));
#43199=CARTESIAN_POINT('',(0.00737796793752131,-0.0177259326582208,0.0418260148286403));
#43200=CARTESIAN_POINT('',(0.0073703491011212,-0.017728999212047,0.0418258185554632));
#43201=CARTESIAN_POINT('',(0.00743026231646231,-0.0177040593575576,0.0418274239460156));
#43202=CARTESIAN_POINT('',(0.00754768102226501,-0.0176545807589192,0.041830607865276));
#43203=CARTESIAN_POINT('',(0.00783884407870035,-0.0175289244893563,0.0418385612409421));
#43204=CARTESIAN_POINT('',(0.0082639897540754,-0.0173331423334386,0.0418503368030392));
#43205=CARTESIAN_POINT('',(0.00863903075263067,-0.0171473802473699,0.0418608782810132));
#43206=CARTESIAN_POINT('',(0.00886440003866057,-0.017031697285228,0.0418672614475087));
#43207=CARTESIAN_POINT('',(0.00906697043761888,-0.0169245981571955,0.0418730369652154));
#43208=CARTESIAN_POINT('',(0.00918762193876269,-0.016859220837623,0.0418764956962864));
#43209=CARTESIAN_POINT('',(0.00936854790080353,-0.0167597604756134,0.0418816979611583));
#43210=CARTESIAN_POINT('',(0.00965533299718655,-0.0165973437622871,0.0418899987202618));
#43211=CARTESIAN_POINT('',(0.0100214704002119,-0.0163794430472246,0.0419007186943628));
#43212=CARTESIAN_POINT('',(0.0103877158294851,-0.0161487428082167,0.0419115893350397));
#43213=CARTESIAN_POINT('',(0.0106637416343302,-0.0159673771450731,0.041919864041294));
#43214=CARTESIAN_POINT('',(0.0109375808148649,-0.0157813619886028,0.0419281253609799));
#43215=CARTESIAN_POINT('',(0.0113503752868312,-0.0154896219760115,0.0419406986626162));
#43216=CARTESIAN_POINT('',(0.0118123120155717,-0.0151422408651364,0.04195501523734));
#43217=CARTESIAN_POINT('',(0.012321491356983,-0.0147277402482593,0.0419712326504712));
#43218=CARTESIAN_POINT('',(0.0127219740779942,-0.0143838846105524,0.0419842492362208));
#43219=CARTESIAN_POINT('',(0.0130767671369701,-0.0140604932018218,0.0419960700187888));
#43220=CARTESIAN_POINT('',(0.013355291689487,-0.0137954574858325,0.0420055296132992));
#43221=CARTESIAN_POINT('',(0.0136034679287909,-0.013550264566355,0.0420141060557007));
#43222=CARTESIAN_POINT('',(0.0137183204603457,-0.0134333925954473,0.0420181372468344));
#43223=CARTESIAN_POINT('',(0.0139202883167972,-0.0132251853682298,0.0420252874232371));
#43224=CARTESIAN_POINT('',(0.0142560638446756,-0.0128664058736527,0.042037432434279));
#43225=CARTESIAN_POINT('',(0.0147580408957158,-0.0122936740432925,0.0420563435082996));
#43226=CARTESIAN_POINT('',(0.0153593761017835,-0.0115358160474499,0.0420804895382233));
#43227=CARTESIAN_POINT('',(0.0161783030162588,-0.0103826008409574,0.0421160151729955));
#43228=CARTESIAN_POINT('',(0.0168705072963708,-0.00920355864864432,0.0421502634638184));
#43229=CARTESIAN_POINT('',(0.0173388672004359,-0.00825584890076573,0.0421765361369678));
#43230=CARTESIAN_POINT('',(0.0175802225602196,-0.00772204446789762,0.0421910420818898));
#43231=CARTESIAN_POINT('',(0.0177351449178442,-0.00736001958369804,0.0422007585431764));
#43232=CARTESIAN_POINT('',(0.01791839444369,-0.00690302681829382,0.042212887415959));
#43233=CARTESIAN_POINT('',(0.0181347032683639,-0.00631970574701028,0.0422282156781225));
#43234=CARTESIAN_POINT('',(0.0184813777085925,-0.00527075533504568,0.0422554367547435));
#43235=CARTESIAN_POINT('',(0.0188626401710491,-0.00374447320016042,0.0422940505032));
#43236=CARTESIAN_POINT('',(0.0191384476936898,-0.00188190996108592,0.0423407335796704));
#43237=CARTESIAN_POINT('',(0.0192,-0.000627225603661956,0.0423725857024158));
#43238=CARTESIAN_POINT('',(0.0192,6.20369116582113E-17,0.0423886526967672));
#43239=CARTESIAN_POINT('',(-0.0192,-4.87313518597996E-17,0.0408877752241749));
#43240=CARTESIAN_POINT('',(0.0192,6.20369116582113E-17,0.0393882658116679));
#43241=CARTESIAN_POINT('',(0.0192,0.000628663193716255,0.0394036918705302));
#43242=CARTESIAN_POINT('',(0.0191536423955705,0.0015716580957445,0.0394269245338009));
#43243=CARTESIAN_POINT('',(0.0189995988018166,0.00281988974234687,0.0394580882726883));
#43244=CARTESIAN_POINT('',(0.0188382414158924,0.0037492807809807,0.0394815550949727));
#43245=CARTESIAN_POINT('',(0.0186314785348052,0.00466956151336681,0.0395051135719536));
#43246=CARTESIAN_POINT('',(0.0184216424502334,0.00542728908450856,0.0395248294007126));
#43247=CARTESIAN_POINT('',(0.0182318091544692,0.00602626968437309,0.0395406357785295));
#43248=CARTESIAN_POINT('',(0.0180778993213337,0.0064731679978757,0.0395525495916115));
#43249=CARTESIAN_POINT('',(0.0179422772508365,0.00683820558017339,0.0395623838627851));
#43250=CARTESIAN_POINT('',(0.0178392386001615,0.00710000322913891,0.0395695006067997));
#43251=CARTESIAN_POINT('',(0.0177842888139774,0.00723642379621665,0.0395732227865096));
#43252=CARTESIAN_POINT('',(0.0177275516131133,0.00737407443096096,0.0395769946656179));
#43253=CARTESIAN_POINT('',(0.0177269279017841,0.00737533546334951,0.0395770266010384));
#43254=CARTESIAN_POINT('',(0.0176992843382282,0.00744166518141708,0.0395788274065915));
#43255=CARTESIAN_POINT('',(0.0176452703809674,0.00756948390581538,0.0395822756645362));
#43256=CARTESIAN_POINT('',(0.017517855835472,0.00786387574531342,0.0395902105782316));
#43257=CARTESIAN_POINT('',(0.017321086347921,0.00828838647033772,0.0396017401937472));
#43258=CARTESIAN_POINT('',(0.0171201982418748,0.00869426237509275,0.0396128858976038));
#43259=CARTESIAN_POINT('',(0.0168655170512065,0.00918235348971352,0.039626424154774));
#43260=CARTESIAN_POINT('',(0.0166105763192255,0.00963499190879102,0.0396391957627629));
#43261=CARTESIAN_POINT('',(0.0163311842889985,0.0100998698300814,0.0396525411880442));
#43262=CARTESIAN_POINT('',(0.0161191538370153,0.010433383372431,0.0396622723989714));
#43263=CARTESIAN_POINT('',(0.0159700558475872,0.0106584357566633,0.039668931065234));
#43264=CARTESIAN_POINT('',(0.0159357098178215,0.0107095327692222,0.0396704576416785));
#43265=CARTESIAN_POINT('',(0.0158650123930345,0.0108143449383736,0.0396736008722819));
#43266=CARTESIAN_POINT('',(0.0157044098910281,0.0110484126310998,0.0396806832073905));
#43267=CARTESIAN_POINT('',(0.0154068004321202,0.0114651914171696,0.0396934916850739));
#43268=CARTESIAN_POINT('',(0.0149838701362527,0.0120095870647659,0.0397107595447022));
#43269=CARTESIAN_POINT('',(0.0145960079631043,0.0124793728908199,0.0397260280724261));
#43270=CARTESIAN_POINT('',(0.0142137041808713,0.0129122412610384,0.0397405073037401));
#43271=CARTESIAN_POINT('',(0.0139027461904543,0.013243082345973,0.0397518953020944));
#43272=CARTESIAN_POINT('',(0.0137258318462371,0.013426086445793,0.0397582801568527));
#43273=CARTESIAN_POINT('',(0.0135552914776017,0.0135979434580184,0.0397643542839402));
#43274=CARTESIAN_POINT('',(0.0135029522520794,0.013649591158744,0.0397661981766909));
#43275=CARTESIAN_POINT('',(0.0133905476680313,0.013760289378962,0.0397701517285016));
#43276=CARTESIAN_POINT('',(0.0132102734430134,0.0139342468568727,0.0397764216682764));
#43277=CARTESIAN_POINT('',(0.0129342562559308,0.0141920912041413,0.039785854447427));
#43278=CARTESIAN_POINT('',(0.0125936292504082,0.0144951868826209,0.0397972070581682));
#43279=CARTESIAN_POINT('',(0.0121198149179599,0.0148970802968096,0.0398126338858884));
#43280=CARTESIAN_POINT('',(0.0116161623327904,0.0152933219081227,0.0398284776193318));
#43281=CARTESIAN_POINT('',(0.0111553360265177,0.0156285127776966,0.0398425153838518));
#43282=CARTESIAN_POINT('',(0.0108767891599144,0.0158225340169491,0.0398508631983172));
#43283=CARTESIAN_POINT('',(0.0106865851100706,0.0159519407358001,0.0398565124117519));
#43284=CARTESIAN_POINT('',(0.0104072495475043,0.0161358272498322,0.0398647230396787));
#43285=CARTESIAN_POINT('',(0.0100754118146885,0.0163459399928608,0.0398743760764964));
#43286=CARTESIAN_POINT('',(0.00950035678502807,0.0166922082094278,0.0398908926449025));
#43287=CARTESIAN_POINT('',(0.00875384603134648,0.0170968957843418,0.039911845817925));
#43288=CARTESIAN_POINT('',(0.0081020794439293,0.0174100301198974,0.0399297884925825));
#43289=CARTESIAN_POINT('',(0.00770950994118586,0.0175849253891927,0.0399405133593165));
#43290=CARTESIAN_POINT('',(0.00749339191535072,0.0176775567923482,0.0399464022709833));
#43291=CARTESIAN_POINT('',(0.00736437907546044,0.0177318263720311,0.0399499177644167));
#43292=CARTESIAN_POINT('',(0.0071505137327307,0.0178193106408842,0.0399557283252957));
#43293=CARTESIAN_POINT('',(0.00689113359732511,0.0179216425000948,0.0399627320417996));
#43294=CARTESIAN_POINT('',(0.0064158681706289,0.0181004635162985,0.039975474323709));
#43295=CARTESIAN_POINT('',(0.00572142024949732,0.0183349322075204,0.0399938233931462));
#43296=CARTESIAN_POINT('',(0.00484975661297025,0.018584983346868,0.0400164652467346));
#43297=CARTESIAN_POINT('',(0.00394456205902514,0.0187982938011497,0.0400396261985757));
#43298=CARTESIAN_POINT('',(0.003006227135957,0.0189714005540031,0.040063332061757));
#43299=CARTESIAN_POINT('',(0.00219800533447482,0.0190787682971744,0.0400835415569089));
#43300=CARTESIAN_POINT('',(0.00153726200154088,0.0191405638311173,0.0400999677726655));
#43301=CARTESIAN_POINT('',(0.00103334736169756,0.019174358785584,0.0401124554130579));
#43302=CARTESIAN_POINT('',(0.000612060895325595,0.0191916623121909,0.0401228699838319));
#43303=CARTESIAN_POINT('',(0.000306057472550829,0.0191978340427517,0.0401304243073443));
#43304=CARTESIAN_POINT('',(0.000143407820939696,0.019199668352477,0.0401344378939259));
#43305=CARTESIAN_POINT('',(-1.55348747597567E-5,0.0192000906241528,0.0401383581666904));
#43306=CARTESIAN_POINT('',(-3.50474507310864E-5,0.0191999598784769,0.0401388403847884));
#43307=CARTESIAN_POINT('',(-0.000117118793954894,0.0191997380722673,0.040140870006623));
#43308=CARTESIAN_POINT('',(-0.000252801557641752,0.0191986224620844,0.0401442349505813));
#43309=CARTESIAN_POINT('',(-0.000502949885347162,0.0191943818004722,0.0401504580233786));
#43310=CARTESIAN_POINT('',(-0.000868273907348215,0.0191817450963066,0.0401595785306492));
#43311=CARTESIAN_POINT('',(-0.00130522815659472,0.0191575157563828,0.0401705187836643));
#43312=CARTESIAN_POINT('',(-0.00181110824690881,0.0191169756635091,0.0401832238751875));
#43313=CARTESIAN_POINT('',(-0.00238718143541817,0.0190542461966417,0.0401977465083337));
#43314=CARTESIAN_POINT('',(-0.00291965608528364,0.0189792585649219,0.0402112333996222));
#43315=CARTESIAN_POINT('',(-0.003328880733356,0.0189097999105468,0.0402216509659764));
#43316=CARTESIAN_POINT('',(-0.00355883570920757,0.018867675527702,0.0402275196565659));
#43317=CARTESIAN_POINT('',(-0.0037690470698942,0.0188266518728038,0.0402328975287772));
#43318=CARTESIAN_POINT('',(-0.00385425562783366,0.0188092215396048,0.0402350806262347));
#43319=CARTESIAN_POINT('',(-0.00401163409480545,0.0187765591117627,0.0402391123289397));
#43320=CARTESIAN_POINT('',(-0.00426703497988582,0.0187208549725118,0.0402456615128404));
#43321=CARTESIAN_POINT('',(-0.00464336103854244,0.0186320121818119,0.0402553284273964));
#43322=CARTESIAN_POINT('',(-0.00509133262757738,0.0185145999405918,0.0402668729231654));
#43323=CARTESIAN_POINT('',(-0.00569142929801448,0.0183417067157091,0.0402823966614816));
#43324=CARTESIAN_POINT('',(-0.00643953417939225,0.0180964887623544,0.0403018892620983));
#43325=CARTESIAN_POINT('',(-0.00764861293056902,0.0176311781153509,0.0403337429361392));
#43326=CARTESIAN_POINT('',(-0.00877194968886215,0.0170989890752868,0.0403643029732516));
#43327=CARTESIAN_POINT('',(-0.00986916205567748,0.0164784446199987,0.0403955414276563));
#43328=CARTESIAN_POINT('',(-0.0106659087537477,0.0159741691064759,0.0404189859021889));
#43329=CARTESIAN_POINT('',(-0.0114375703211447,0.0154311005462077,0.0404425334656104));
#43330=CARTESIAN_POINT('',(-0.0120574296139266,0.0149476262149671,0.0404622204711009));
#43331=CARTESIAN_POINT('',(-0.0125387719179605,0.014542803094461,0.0404780172609407));
#43332=CARTESIAN_POINT('',(-0.0128330350716999,0.014282749792635,0.0404878980331269));
#43333=CARTESIAN_POINT('',(-0.0130651746463766,0.0140697956508291,0.0404958352900833));
#43334=CARTESIAN_POINT('',(-0.0132356200633878,0.0139096531159513,0.0405017329760987));
#43335=CARTESIAN_POINT('',(-0.0133813667192793,0.0137690609604139,0.0405068445971381));
#43336=CARTESIAN_POINT('',(-0.0134849038273407,0.013667644115147,0.0405105047798711));
#43337=CARTESIAN_POINT('',(-0.0135949724049001,0.0135580215410906,0.040514430961611));
#43338=CARTESIAN_POINT('',(-0.0135788562738796,0.0135740196044398,0.0405138554096467));
#43339=CARTESIAN_POINT('',(-0.013609156462397,0.0135437116544659,0.0405149294725554));
#43340=CARTESIAN_POINT('',(-0.0136570287270167,0.013495503255589,0.0405166155567645));
#43341=CARTESIAN_POINT('',(-0.0137821312605483,0.0133684574799683,0.0405210328193024));
#43342=CARTESIAN_POINT('',(-0.0139980125105175,0.0131430334155296,0.0405287431765659));
#43343=CARTESIAN_POINT('',(-0.0142819294060527,0.0128351046817623,0.0405390791679773));
#43344=CARTESIAN_POINT('',(-0.0146270316308284,0.0124418613087138,0.0405519808968963));
#43345=CARTESIAN_POINT('',(-0.0149605400689078,0.0120380099651769,0.0405648901144448));
#43346=CARTESIAN_POINT('',(-0.0152502893023969,0.0116667906790124,0.0405764949136099));
#43347=CARTESIAN_POINT('',(-0.0154787029801495,0.0113622029530943,0.0405858757901543));
#43348=CARTESIAN_POINT('',(-0.0156742762892487,0.0110902740411778,0.0405941279021359));
#43349=CARTESIAN_POINT('',(-0.0158190296671483,0.0108814243134223,0.0406003880676495));
#43350=CARTESIAN_POINT('',(-0.0158955177767126,0.0107693260506697,0.0406037312400238));
#43351=CARTESIAN_POINT('',(-0.015973223957531,0.0106535845062456,0.0406071653818326));
#43352=CARTESIAN_POINT('',(-0.0159750842603848,0.0106506429498373,0.0406072513485023));
#43353=CARTESIAN_POINT('',(-0.016004737302427,0.0106061332989109,0.0406085702173757));
#43354=CARTESIAN_POINT('',(-0.0160457097484964,0.0105440997393347,0.0406104062489303));
#43355=CARTESIAN_POINT('',(-0.0161148626127109,0.0104383749009219,0.0406135316770759));
#43356=CARTESIAN_POINT('',(-0.0162014277246918,0.0103035414653994,0.0406175054280723));
#43357=CARTESIAN_POINT('',(-0.0163259042259946,0.0101059387085917,0.0406233082728591));
#43358=CARTESIAN_POINT('',(-0.0164954813766009,0.00982841814386152,0.0406314083422509));
#43359=CARTESIAN_POINT('',(-0.0167940372935135,0.00931475059235479,0.0406462432390558));
#43360=CARTESIAN_POINT('',(-0.0171243037635479,0.00869933678641187,0.0406637235619664));
#43361=CARTESIAN_POINT('',(-0.0174326121245624,0.00805075025151385,0.0406817399808592));
#43362=CARTESIAN_POINT('',(-0.0176037375735768,0.00766769660920411,0.040692273678032));
#43363=CARTESIAN_POINT('',(-0.0177512447249361,0.00731870166664532,0.0407017937408365));
#43364=CARTESIAN_POINT('',(-0.0178257021606035,0.00713418591542377,0.0407067907165703));
#43365=CARTESIAN_POINT('',(-0.0179457861347056,0.00682926329932022,0.0407150093377251));
#43366=CARTESIAN_POINT('',(-0.0180804566090405,0.00646589981592569,0.0407247063574043));
#43367=CARTESIAN_POINT('',(-0.0182344250697825,0.00601837778077936,0.0407365179454826));
#43368=CARTESIAN_POINT('',(-0.0183761369999105,0.00557053872483966,0.0407482083695427));
#43369=CARTESIAN_POINT('',(-0.018506876712944,0.00511941055385669,0.0407598657682243));
#43370=CARTESIAN_POINT('',(-0.0186260344845876,0.00466745886331707,0.0407714339154503));
#43371=CARTESIAN_POINT('',(-0.0187166031178119,0.00428585199186025,0.0407811136333159));
#43372=CARTESIAN_POINT('',(-0.0187737468316163,0.00402480727004834,0.0407876954822791));
#43373=CARTESIAN_POINT('',(-0.0188070377234321,0.00386494732693353,0.0407917129301286));
#43374=CARTESIAN_POINT('',(-0.0188255327189833,0.00377460196925392,0.0407939801464488));
#43375=CARTESIAN_POINT('',(-0.0188653714524608,0.00357091425566207,0.0407990812380753));
#43376=CARTESIAN_POINT('',(-0.0189069061487365,0.00334517738421681,0.0408047240798885));
#43377=CARTESIAN_POINT('',(-0.0189753331557474,0.00294439963429444,0.0408147220664482));
#43378=CARTESIAN_POINT('',(-0.0190499661576845,0.00242043706186934,0.0408277441621779));
#43379=CARTESIAN_POINT('',(-0.019113129789702,0.00185089177339893,0.040841859237278));
#43380=CARTESIAN_POINT('',(-0.0191684223934121,0.00117913314761158,0.0408584844592615));
#43381=CARTESIAN_POINT('',(-0.0191973269841242,0.00050253555781279,0.0408752334091669));
#43382=CARTESIAN_POINT('',(-0.0192,0.00013801990587612,0.0408843134849681));
#43383=CARTESIAN_POINT('',(-0.0192,0.,0.0408877752241749));
#43384=CARTESIAN_POINT('',(0.0192,2.03021822078784E-17,0.0393882658116679));
#43385=CARTESIAN_POINT('',(-0.0192,8.05624845824862E-17,0.0378887293230132));
#43386=CARTESIAN_POINT('',(-0.0192,-0.00022193889075637,0.0378942721115581));
#43387=CARTESIAN_POINT('',(-0.0191924320556616,-0.000711426082709432,0.0379064517956354));
#43388=CARTESIAN_POINT('',(-0.0191421970582481,-0.00158317381499541,0.037928054835619));
#43389=CARTESIAN_POINT('',(-0.0190535124946304,-0.0024167203864713,0.0379487073148984));
#43390=CARTESIAN_POINT('',(-0.0189554945574285,-0.00306401165003696,0.0379648016378798));
#43391=CARTESIAN_POINT('',(-0.0188907175093251,-0.00343731284693225,0.0379741079256706));
#43392=CARTESIAN_POINT('',(-0.0188290752177871,-0.00375905421228844,0.0379821470681816));
#43393=CARTESIAN_POINT('',(-0.0187880008954488,-0.00395782378144535,0.0379871310075943));
#43394=CARTESIAN_POINT('',(-0.0187212406658431,-0.00426626724610465,0.0379948956222375));
#43395=CARTESIAN_POINT('',(-0.0185978997077452,-0.00478734166477267,0.038008106411531));
#43396=CARTESIAN_POINT('',(-0.0183088332462928,-0.00584298996768977,0.0380352271895157));
#43397=CARTESIAN_POINT('',(-0.0177620834674924,-0.00737366341407103,0.0380759865548395));
#43398=CARTESIAN_POINT('',(-0.0170941518681076,-0.00878135287379402,0.0381151560081176));
#43399=CARTESIAN_POINT('',(-0.0164736157016148,-0.00987719356066384,0.0381465879808454));
#43400=CARTESIAN_POINT('',(-0.0159690984896644,-0.0106734882760038,0.0381700383824134));
#43401=CARTESIAN_POINT('',(-0.0154259711799453,-0.0114444880981995,0.0381934093609142));
#43402=CARTESIAN_POINT('',(-0.0149422694824126,-0.0120640331314217,0.0382128149599319));
#43403=CARTESIAN_POINT('',(-0.0145377336262114,-0.0125446797662033,0.0382282849050756));
#43404=CARTESIAN_POINT('',(-0.0142246821957469,-0.0128984848324273,0.0382398960222624));
#43405=CARTESIAN_POINT('',(-0.0139594876570885,-0.0131840329444294,0.0382494563292828));
#43406=CARTESIAN_POINT('',(-0.0137646375498219,-0.0133859425920867,0.0382563300866765));
#43407=CARTESIAN_POINT('',(-0.0136609215342739,-0.0134916929024351,0.0382599567853406));
#43408=CARTESIAN_POINT('',(-0.0135582188102546,-0.0135947690861585,0.0382635161110624));
#43409=CARTESIAN_POINT('',(-0.0135482786278759,-0.0136045543424977,0.038263860599836));
#43410=CARTESIAN_POINT('',(-0.0134907445988545,-0.0136617534019531,0.0382658629222794));
#43411=CARTESIAN_POINT('',(-0.0133811059120139,-0.0137695767183726,0.0382696851256903));
#43412=CARTESIAN_POINT('',(-0.013143861328283,-0.0139983997136955,0.0382779202854849));
#43413=CARTESIAN_POINT('',(-0.0128035734119893,-0.0143102267404934,0.0382895007109755));
#43414=CARTESIAN_POINT('',(-0.0124719007318678,-0.0145992794240946,0.0383005570957964));
#43415=CARTESIAN_POINT('',(-0.0120678051379103,-0.0149372183515959,0.0383138096678115));
#43416=CARTESIAN_POINT('',(-0.0116643371150943,-0.0152540441969734,0.0383267146451698));
#43417=CARTESIAN_POINT('',(-0.011234855509977,-0.0155722024727821,0.0383401487233681));
#43418=CARTESIAN_POINT('',(-0.0109586912674793,-0.0157661723475873,0.0383486214441619));
#43419=CARTESIAN_POINT('',(-0.0107718438041718,-0.0158937935027922,0.0383542934085894));
#43420=CARTESIAN_POINT('',(-0.0106822323133276,-0.015954248644862,0.0383570000856446));
#43421=CARTESIAN_POINT('',(-0.0105115727459199,-0.0160673909813946,0.0383621161608581));
#43422=CARTESIAN_POINT('',(-0.0103011824439216,-0.0162034830854251,0.0383683646498227));
#43423=CARTESIAN_POINT('',(-0.00989711393134361,-0.0164566986763136,0.0383802284704803));
#43424=CARTESIAN_POINT('',(-0.00925876527977091,-0.0168290521393271,0.0383985326419782));
#43425=CARTESIAN_POINT('',(-0.00851434895537478,-0.0172148696100751,0.0384192037589066));
#43426=CARTESIAN_POINT('',(-0.00787277575534994,-0.017514944145597,0.0384366231604828));
#43427=CARTESIAN_POINT('',(-0.00732122560114219,-0.0177521031293637,0.03845135591687));
#43428=CARTESIAN_POINT('',(-0.00688808195711684,-0.0179238650748241,0.0384627985294625));
#43429=CARTESIAN_POINT('',(-0.00627170063586758,-0.0181520498765417,0.0384789986618317));
#43430=CARTESIAN_POINT('',(-0.00552184479124476,-0.0183967910996496,0.0384985269826806));
#43431=CARTESIAN_POINT('',(-0.00477249712507726,-0.0186015961593812,0.0385178912002506));
#43432=CARTESIAN_POINT('',(-0.00426399640441388,-0.018721709547373,0.0385309854245854));
#43433=CARTESIAN_POINT('',(-0.00396222747631565,-0.0187870343587279,0.0385387451876652));
#43434=CARTESIAN_POINT('',(-0.00377408530146284,-0.0188260665630228,0.0385435837484251));
#43435=CARTESIAN_POINT('',(-0.00344526112599039,-0.018889306769233,0.0385520214470724));
#43436=CARTESIAN_POINT('',(-0.00306918572988036,-0.0189546724649684,0.0385616310948113));
#43437=CARTESIAN_POINT('',(-0.00241500810887963,-0.0190538501414187,0.0385782724945357));
#43438=CARTESIAN_POINT('',(-0.00157722589308354,-0.0191428040566018,0.0385994059960559));
#43439=CARTESIAN_POINT('',(-0.000846127191215844,-0.0191844243705943,0.0386177049419109));
#43440=CARTESIAN_POINT('',(-0.000404458241607011,-0.0191964896371516,0.0386287047575351));
#43441=CARTESIAN_POINT('',(-0.000158060393806309,-0.0191995331018626,0.0386348240862482));
#43442=CARTESIAN_POINT('',(-1.50190681013459E-5,-0.0192003620780359,0.0386383701305568));
#43443=CARTESIAN_POINT('',(0.000244723469544005,-0.0191990155180333,0.0386448002721589));
#43444=CARTESIAN_POINT('',(0.000550291329664181,-0.0191931325629526,0.0386523616897328));
#43445=CARTESIAN_POINT('',(0.00110375867659713,-0.0191728691077525,0.0386660513662283));
#43446=CARTESIAN_POINT('',(0.00188303616742212,-0.0191150910945949,0.0386853227006194));
#43447=CARTESIAN_POINT('',(0.00281814553053024,-0.018999839334807,0.0387085138769124));
#43448=CARTESIAN_POINT('',(0.00374445115215519,-0.0188391721881906,0.0387315538826043));
#43449=CARTESIAN_POINT('',(0.00466542500010175,-0.0186325272534402,0.0387547875710639));
#43450=CARTESIAN_POINT('',(0.00542285114301209,-0.0184229471939061,0.0387743875269876));
#43451=CARTESIAN_POINT('',(0.00602185387965969,-0.0182332651742008,0.0387901842335238));
#43452=CARTESIAN_POINT('',(0.00646854041601569,-0.0180795624022548,0.0388021279840688));
#43453=CARTESIAN_POINT('',(0.00683407280218434,-0.0179438377921012,0.0388120392734974));
#43454=CARTESIAN_POINT('',(0.007094917691237,-0.0178412714741173,0.0388191948946996));
#43455=CARTESIAN_POINT('',(0.00723282418127284,-0.0177857444077235,0.038822996836939));
#43456=CARTESIAN_POINT('',(0.00736587173888015,-0.0177309618253466,0.0388266838892492));
#43457=CARTESIAN_POINT('',(0.0073843861896102,-0.0177231669849029,0.0388271966167576));
#43458=CARTESIAN_POINT('',(0.00745604326299315,-0.0176932376117725,0.0388291735852158));
#43459=CARTESIAN_POINT('',(0.00757674482354925,-0.0176420940691219,0.0388324878733712));
#43460=CARTESIAN_POINT('',(0.00788956992636278,-0.0175063459502744,0.0388410446583097));
#43461=CARTESIAN_POINT('',(0.0083708008458124,-0.0172843204463115,0.0388542055739615));
#43462=CARTESIAN_POINT('',(0.00897491977693818,-0.0169761806590531,0.0388709566428017));
#43463=CARTESIAN_POINT('',(0.00948599593134554,-0.0166967382374707,0.0388853067707876));
#43464=CARTESIAN_POINT('',(0.00995430881721385,-0.0164210055546526,0.0388986682361985));
#43465=CARTESIAN_POINT('',(0.0103086527523722,-0.0161986113824786,0.0389089420525471));
#43466=CARTESIAN_POINT('',(0.0105092558920236,-0.0160689024824901,0.0389148057763633));
#43467=CARTESIAN_POINT('',(0.0106842952236901,-0.0159529058029027,0.0389199577600312));
#43468=CARTESIAN_POINT('',(0.0107789322017483,-0.0158889481787481,0.0389227606204501));
#43469=CARTESIAN_POINT('',(0.0109307821699586,-0.0157852344189826,0.0389272762278964));
#43470=CARTESIAN_POINT('',(0.0111788075288396,-0.0156116926899071,0.0389347168123635));
#43471=CARTESIAN_POINT('',(0.0116644283329899,-0.0152572781880804,0.038949522325062));
#43472=CARTESIAN_POINT('',(0.0122999567309008,-0.0147526441473697,0.0389695900374676));
#43473=CARTESIAN_POINT('',(0.0128656892406923,-0.0142571188912635,0.0389883073357696));
#43474=CARTESIAN_POINT('',(0.0132332312914574,-0.0139122800421054,0.0390009248073013));
#43475=CARTESIAN_POINT('',(0.0134250463387246,-0.0137268244149825,0.0390076227416391));
#43476=CARTESIAN_POINT('',(0.0135893314577,-0.0135639102791304,0.039013446818175));
#43477=CARTESIAN_POINT('',(0.0136534342910137,-0.0134991239603666,0.0390157417561474));
#43478=CARTESIAN_POINT('',(0.0137815513931907,-0.0133688156365421,0.0390203345378987));
#43479=CARTESIAN_POINT('',(0.0140042813904065,-0.0131370514035129,0.0390283972628939));
#43480=CARTESIAN_POINT('',(0.0143735057578032,-0.0127362066135043,0.0390420251019215));
#43481=CARTESIAN_POINT('',(0.014870950316987,-0.012154021192521,0.0390611145754916));
#43482=CARTESIAN_POINT('',(0.0154161360185727,-0.0114576829812737,0.0390831115195838));
#43483=CARTESIAN_POINT('',(0.0159938597301856,-0.0106400137371051,0.039107969709061));
#43484=CARTESIAN_POINT('',(0.0164889532961113,-0.00985023681927002,0.0391310804854158));
#43485=CARTESIAN_POINT('',(0.0168834212994582,-0.00914971785465512,0.0391510025966153));
#43486=CARTESIAN_POINT('',(0.0171270921483327,-0.00868241353400955,0.0391640558797881));
#43487=CARTESIAN_POINT('',(0.0173187007840868,-0.0082909231800945,0.0391748488202584));
#43488=CARTESIAN_POINT('',(0.0174607893482642,-0.00798736678856053,0.0391831464550681));
#43489=CARTESIAN_POINT('',(0.0175760751256471,-0.00772958500855156,0.0391901360047796));
#43490=CARTESIAN_POINT('',(0.0176578178690573,-0.0075396375228582,0.0391952537705549));
#43491=CARTESIAN_POINT('',(0.0177006367356661,-0.00743849845576918,0.0391979717800081));
#43492=CARTESIAN_POINT('',(0.0177564184460363,-0.00730445903356114,0.0392015643443123));
#43493=CARTESIAN_POINT('',(0.0177309029613751,-0.00736575644533109,0.039199922157795));
#43494=CARTESIAN_POINT('',(0.0177479902368498,-0.00732461983040761,0.0392010291412403));
#43495=CARTESIAN_POINT('',(0.0177576742445014,-0.00730107002858475,0.0392016708340031));
#43496=CARTESIAN_POINT('',(0.0177881389222152,-0.00722669586283352,0.0392036829298165));
#43497=CARTESIAN_POINT('',(0.0178400515667169,-0.00709805311807092,0.0392071590793552));
#43498=CARTESIAN_POINT('',(0.0179312400113604,-0.00686674521496964,0.0392133889812832));
#43499=CARTESIAN_POINT('',(0.0180758020447088,-0.00647910650840098,0.0392237562464804));
#43500=CARTESIAN_POINT('',(0.0182488639014487,-0.00597777556167481,0.039237046499586));
#43501=CARTESIAN_POINT('',(0.0184090657290274,-0.00546301808203981,0.0392505556512843));
#43502=CARTESIAN_POINT('',(0.0185409846123923,-0.00499208265195435,0.0392628120525489));
#43503=CARTESIAN_POINT('',(0.0186403729145296,-0.00460775037080017,0.0392727607731072));
#43504=CARTESIAN_POINT('',(0.0187212541907411,-0.00426555219765061,0.0392815728714641));
#43505=CARTESIAN_POINT('',(0.0187776536559985,-0.00400599730873853,0.0392882297681019));
#43506=CARTESIAN_POINT('',(0.0188072882778651,-0.00386419551343452,0.039291860457865));
#43507=CARTESIAN_POINT('',(0.0188349231018114,-0.00372676217679712,0.0392953739293965));
#43508=CARTESIAN_POINT('',(0.0188403362303185,-0.00369887407573525,0.039296085710669));
#43509=CARTESIAN_POINT('',(0.0188551437332107,-0.00362307015227261,0.0392980203865328));
#43510=CARTESIAN_POINT('',(0.0188771176710835,-0.00350740461657399,0.0393009673583189));
#43511=CARTESIAN_POINT('',(0.0189093718726891,-0.00333040862608833,0.0393054655665473));
#43512=CARTESIAN_POINT('',(0.0189455248915272,-0.00311812090203791,0.0393108409863942));
#43513=CARTESIAN_POINT('',(0.0189915174784813,-0.0028285052248755,0.0393181500561142));
#43514=CARTESIAN_POINT('',(0.0190439300027691,-0.0024572895851176,0.0393274732938753));
#43515=CARTESIAN_POINT('',(0.0191158601377365,-0.00184258518610987,0.0393428220638243));
#43516=CARTESIAN_POINT('',(0.019180683030258,-0.00103622452335621,0.0393628021022237));
#43517=CARTESIAN_POINT('',(0.0192,-0.000351678025297538,0.0393796363802441));
#43518=CARTESIAN_POINT('',(0.0192,6.20369116582113E-17,0.0393882658116679));
#43519=CARTESIAN_POINT('',(-0.0192,-7.15606202600399E-16,0.0378887293230132));
#43520=CARTESIAN_POINT('',(0.0192,-4.02812422912431E-17,0.0363879628538316));
#43521=CARTESIAN_POINT('',(0.0192,0.0025132741228718,0.0364504947900475));
#43522=CARTESIAN_POINT('',(0.0182002919343753,0.00753865073535335,0.0365755586624793));
#43523=CARTESIAN_POINT('',(0.0139299003749868,0.0139299426504137,0.0367631544711271));
#43524=CARTESIAN_POINT('',(0.00753880775836791,0.0182002798556818,0.0369507502797747));
#43525=CARTESIAN_POINT('',(2.09173148415435E-17,0.0196998600721591,0.0371383460884224));
#43526=CARTESIAN_POINT('',(-0.00753880775836788,0.0182002798556819,0.0373259418970701));
#43527=CARTESIAN_POINT('',(-0.0139299003749868,0.0139299426504138,0.0375135377057178));
#43528=CARTESIAN_POINT('',(-0.0182002919343753,0.00753865073535338,0.0377011335143655));
#43529=CARTESIAN_POINT('',(-0.0192,0.00251327412287184,0.0378261973867973));
#43530=CARTESIAN_POINT('',(-0.0192,0.,0.0378887293230132));
#43531=CARTESIAN_POINT('',(0.0192,-1.66086175294244E-17,0.0363879628538316));
#43532=CARTESIAN_POINT('',(-0.0192,8.05624845824862E-17,0.0348884087721565));
#43533=CARTESIAN_POINT('',(-0.0192,-0.00251327412287176,0.0349508901922263));
#43534=CARTESIAN_POINT('',(-0.0182002919343753,-0.00753865073535332,0.0350758530323659));
#43535=CARTESIAN_POINT('',(-0.0139299003749868,-0.0139299426504137,0.0352632972925753));
#43536=CARTESIAN_POINT('',(-0.00753880775836796,-0.0182002798556818,0.0354507415527847));
#43537=CARTESIAN_POINT('',(-6.58895417508622E-17,-0.0196998600721591,0.0356381858129941));
#43538=CARTESIAN_POINT('',(0.00753880775836784,-0.0182002798556819,0.0358256300732035));
#43539=CARTESIAN_POINT('',(0.0139299003749867,-0.0139299426504138,0.0360130743334129));
#43540=CARTESIAN_POINT('',(0.0182002919343753,-0.00753865073535341,0.0362005185936222));
#43541=CARTESIAN_POINT('',(0.0192,-0.00251327412287188,0.0363254814337619));
#43542=CARTESIAN_POINT('',(0.0192,-4.02812422912431E-17,0.0363879628538316));
#43543=CARTESIAN_POINT('',(0.0135622971600913,0.0138716519279114,0.0432540773782661));
#43544=CARTESIAN_POINT('',(0.0135274210106397,0.0136559761133728,0.0446813017670343));
#43545=CARTESIAN_POINT('',(0.0135093917909034,0.0136603263905846,0.0447968672191863));
#43546=CARTESIAN_POINT('',(0.0134827517892629,0.0136695662613628,0.0449835750428777));
#43547=CARTESIAN_POINT('',(0.013457778662072,0.0136941188033885,0.0452414242721579));
#43548=CARTESIAN_POINT('',(0.0134577620230351,0.0136941126402747,0.0452414232474944));
#43549=CARTESIAN_POINT('',(0.0134577729136188,0.013694124453173,0.0452414232598564));
#43550=CARTESIAN_POINT('',(0.0134431358506774,0.013708481346275,0.0444170923559122));
#43551=CARTESIAN_POINT('',(0.0134284989859897,0.0137228384410837,0.0435927614519608));
#43552=CARTESIAN_POINT('',(0.0134138623189673,0.0137371957381755,0.0427684305480228));
#43553=CARTESIAN_POINT('',(0.0134138694653129,0.0137371887554162,0.0427684291163815));
#43554=CARTESIAN_POINT('',(0.0134483181858801,0.0137035122742865,0.0430257467298376));
#43555=CARTESIAN_POINT('',(0.0134818447172915,0.0136878125844233,0.0432118318925806));
#43556=CARTESIAN_POINT('',(0.0135040830062574,0.0136794957015745,0.0433266841502101));
#43557=CARTESIAN_POINT('',(0.0138452187948272,0.013589183021651,0.0342442501353452));
#43558=CARTESIAN_POINT('',(0.013694112126519,0.0134577608686323,0.0337585747113245));
#43559=CARTESIAN_POINT('',(0.0137084811428348,0.0134431356876894,0.0345829056064801));
#43560=CARTESIAN_POINT('',(0.0137228503168215,0.0134285106616982,0.0354072365016364));
#43561=CARTESIAN_POINT('',(0.0137372196488776,0.0134138857902519,0.0362315673967792));
#43562=CARTESIAN_POINT('',(0.0137371716111379,0.0134138422538494,0.0362315674617482));
#43563=CARTESIAN_POINT('',(0.0137372123221964,0.0134138932845458,0.0362315689613074));
#43564=CARTESIAN_POINT('',(0.0137035340125068,0.0134483202299136,0.0359743257853847));
#43565=CARTESIAN_POINT('',(0.013687850265109,0.0134818048026976,0.0357884360374105));
#43566=CARTESIAN_POINT('',(0.01367954401169,0.0135039705136105,0.0356739006949439));
#43567=CARTESIAN_POINT('',(0.0136559727524296,0.0135274261730626,0.0343187419075685));
#43568=CARTESIAN_POINT('',(0.0136603243690877,0.0135093775412914,0.0342030569645028));
#43569=CARTESIAN_POINT('',(0.013669568440656,0.0134827363571335,0.0340163339693225));
#43570=CARTESIAN_POINT('',(0.0136941065780828,0.0134577665146654,0.0337585737172107));
#43571=CARTESIAN_POINT('',(0.0119111171034194,0.0152484668621677,0.0451224137724094));
#43572=CARTESIAN_POINT('',(0.0118633605503285,0.0151858282583754,0.0451430883500229));
#43573=CARTESIAN_POINT('',(0.0118233321519909,0.0151277503647984,0.0452343265114968));
#43574=CARTESIAN_POINT('',(0.0118263099903143,0.0151254220441274,0.0453156741150844));
#43575=CARTESIAN_POINT('',(0.0134200668536559,0.0140382472338094,0.0450388374046298));
#43576=CARTESIAN_POINT('',(0.013371916547268,0.0139873876325758,0.0450679237332757));
#43577=CARTESIAN_POINT('',(0.0133349840844563,0.0139462943878066,0.0451509479553486));
#43578=CARTESIAN_POINT('',(0.0133370200672889,0.0139442235544884,0.0452256332373079));
#43579=CARTESIAN_POINT('',(0.0147477564958791,0.0126583308748199,0.0450103900077387));
#43580=CARTESIAN_POINT('',(0.0146912735976177,0.0126090804528248,0.0450345912790446));
#43581=CARTESIAN_POINT('',(0.0146441359577131,0.0125657399351169,0.0451222194837998));
#43582=CARTESIAN_POINT('',(0.0146454248516105,0.01256423370876,0.0452005895299071));
#43583=CARTESIAN_POINT('',(0.0169675628741187,0.00947696062870603,0.0449137425318125));
#43584=CARTESIAN_POINT('',(0.0169025856234469,0.00944001123116975,0.0449380908423935));
#43585=CARTESIAN_POINT('',(0.016848005170986,0.00940708560671004,0.0450255531783573));
#43586=CARTESIAN_POINT('',(0.0168489449892251,0.00940539688277867,0.0451037872947182));
#43587=CARTESIAN_POINT('',(0.0178192095346987,0.00775672168733615,0.0448678738535445));
#43588=CARTESIAN_POINT('',(0.0177507059561247,0.00772628217992625,0.044892055106076));
#43589=CARTESIAN_POINT('',(0.0176928356180264,0.00769880283204781,0.0449797095415211));
#43590=CARTESIAN_POINT('',(0.01769359091967,0.00769707801660105,0.0450581013158372));
#43591=CARTESIAN_POINT('',(0.0190005468345018,0.0040841515008905,0.0447730868019316));
#43592=CARTESIAN_POINT('',(0.0189272846560822,0.00406779723084781,0.044797187650629));
#43593=CARTESIAN_POINT('',(0.0188649943920347,0.00405215796587943,0.0448849298806516));
#43594=CARTESIAN_POINT('',(0.0188654132776149,0.00405022857269431,0.0449633935072848));
#43595=CARTESIAN_POINT('',(0.0193117423498795,0.00216840122592053,0.0447245118621838));
#43596=CARTESIAN_POINT('',(0.0192374781351968,0.00215946733845291,0.0447488154351232));
#43597=CARTESIAN_POINT('',(0.0191743301485486,0.00215018981994738,0.0448363280115777));
#43598=CARTESIAN_POINT('',(0.0191745452466472,0.00214824821757985,0.0449146032877846));
#43599=CARTESIAN_POINT('',(0.0193610639046287,-0.00167360848793416,0.0446299517719903));
#43600=CARTESIAN_POINT('',(0.0192864296756519,-0.00166773435971748,0.0446542054557712));
#43601=CARTESIAN_POINT('',(0.0192225964002094,-0.00166434381837124,0.044741776704796));
#43602=CARTESIAN_POINT('',(0.019222429495433,-0.00166624131300508,0.0448201001988356));
#43603=CARTESIAN_POINT('',(0.0190948154609097,-0.00361133873910463,0.0445831374115228));
#43604=CARTESIAN_POINT('',(0.0190209425032217,-0.00359794761588151,0.0446072259517545));
#43605=CARTESIAN_POINT('',(0.0189574517013896,-0.00358812839235511,0.0446949830741052));
#43606=CARTESIAN_POINT('',(0.0189570896738194,-0.00359004606659571,0.0447734589594669));
#43607=CARTESIAN_POINT('',(0.0180142500641535,-0.00728829745566222,0.0444875269798807));
#43608=CARTESIAN_POINT('',(0.0179446383345139,-0.00726076166462538,0.0445117827641695));
#43609=CARTESIAN_POINT('',(0.0178846058775381,-0.00723881986642369,0.0445993492826507));
#43610=CARTESIAN_POINT('',(0.0178838660778194,-0.00724065009319846,0.0446776687439555));
#43611=CARTESIAN_POINT('',(0.0171862112204154,-0.00906930077004769,0.0444392374123103));
#43612=CARTESIAN_POINT('',(0.0171197971849369,-0.00903491858731672,0.0444635498466536));
#43613=CARTESIAN_POINT('',(0.0170623984036047,-0.00900705497327935,0.0445510536791123));
#43614=CARTESIAN_POINT('',(0.0170615018148729,-0.00900875217054671,0.0446293218452303));
#43615=CARTESIAN_POINT('',(0.0150748765585205,-0.0122631930816844,0.0443456129679493));
#43616=CARTESIAN_POINT('',(0.015016340754005,-0.0122163239260077,0.044369770376547));
#43617=CARTESIAN_POINT('',(0.0149652869581169,-0.0121775475694233,0.0444574509420824));
#43618=CARTESIAN_POINT('',(0.0149640799859765,-0.0121790299294539,0.0445358640882813));
#43619=CARTESIAN_POINT('',(0.0137592188484159,-0.0137228537103216,0.0442972160453779));
#43620=CARTESIAN_POINT('',(0.0137057758160768,-0.0136703779924722,0.0443214412859766));
#43621=CARTESIAN_POINT('',(0.0136589637681864,-0.0136267677645398,0.0444090425264624));
#43622=CARTESIAN_POINT('',(0.0136575692787798,-0.0136281622625707,0.0444873904791982));
#43623=CARTESIAN_POINT('',(0.0107998076932649,-0.0161550011326311,0.0442020536744408));
#43624=CARTESIAN_POINT('',(0.0107577781165153,-0.0160931658584387,0.0442263805387302));
#43625=CARTESIAN_POINT('',(0.0107205811206235,-0.016041360017213,0.0443138674388793));
#43626=CARTESIAN_POINT('',(0.0107189757689592,-0.0160424301065671,0.0443921217071986));
#43627=CARTESIAN_POINT('',(0.00911836794955619,-0.0171612888614804,0.044155115293634));
#43628=CARTESIAN_POINT('',(0.00908268800265674,-0.0170953497707791,0.044179284848013));
#43629=CARTESIAN_POINT('',(0.00905077697408364,-0.0170397763631208,0.044266952283579));
#43630=CARTESIAN_POINT('',(0.00904910958776107,-0.0170406664206737,0.044345354710046));
#43631=CARTESIAN_POINT('',(0.00556774916588638,-0.018618877334691,0.0440607028803731));
#43632=CARTESIAN_POINT('',(0.00554567972638056,-0.0185471405914764,0.0440848091125059));
#43633=CARTESIAN_POINT('',(0.00552519027181333,-0.0184862872185166,0.0441725453038299));
#43634=CARTESIAN_POINT('',(0.00552330159985229,-0.0184868557583233,0.044251003979556));
#43635=CARTESIAN_POINT('',(0.0036769985003576,-0.0190825297688914,0.0440119757378991));
#43636=CARTESIAN_POINT('',(0.00366226667577984,-0.0190092018617648,0.0440362856120546));
#43637=CARTESIAN_POINT('',(0.00364806490597945,-0.0189469874336672,0.0441237909427346));
#43638=CARTESIAN_POINT('',(0.00364614500367027,-0.0189473544278605,0.0442020602752495));
#43639=CARTESIAN_POINT('',(-0.000159073605862996,-0.0194330427739331,0.0439171161419455));
#43640=CARTESIAN_POINT('',(-0.000159036489398663,-0.0193581966471054,0.0439413856283332));
#43641=CARTESIAN_POINT('',(-0.000160633593426761,-0.0192943231817672,0.0440289388180418));
#43642=CARTESIAN_POINT('',(-0.000162539587570898,-0.0192943047059287,0.0441072474983732));
#43643=CARTESIAN_POINT('',(-0.00208280092412028,-0.0193232197787198,0.0438709143474731));
#43644=CARTESIAN_POINT('',(-0.00207532883784003,-0.0192485545634404,0.0438950384420773));
#43645=CARTESIAN_POINT('',(-0.00207059657791085,-0.0191845471658223,0.0439827552249456));
#43646=CARTESIAN_POINT('',(-0.00207254002817534,-0.0191843378177612,0.0440611980015088));
#43647=CARTESIAN_POINT('',(-0.00587164608183915,-0.0185264228724639,0.0437743901481076));
#43648=CARTESIAN_POINT('',(-0.00584959280964872,-0.0184549155034643,0.0437986739161329));
#43649=CARTESIAN_POINT('',(-0.00583237431302894,-0.0183934126817911,0.043886208785472));
#43650=CARTESIAN_POINT('',(-0.00583424921587975,-0.0183928185920857,0.0439645023066169));
#43651=CARTESIAN_POINT('',(-0.00766578626947044,-0.0178587914359639,0.0437275445893659));
#43652=CARTESIAN_POINT('',(-0.00763682180113842,-0.0177898231337236,0.043751850190935));
#43653=CARTESIAN_POINT('',(-0.00761362812625151,-0.0177303616851066,0.0438393621803527));
#43654=CARTESIAN_POINT('',(-0.00761538499953849,-0.0177296070688981,0.043917637045953));
#43655=CARTESIAN_POINT('',(-0.0110535926085533,-0.0159857022185186,0.0436330501225642));
#43656=CARTESIAN_POINT('',(-0.0110113900601718,-0.0159236454139806,0.0436571679642768));
#43657=CARTESIAN_POINT('',(-0.0109766613811024,-0.0158696554354374,0.0437448934060955));
#43658=CARTESIAN_POINT('',(-0.0109782340290061,-0.0158685674562356,0.0438233433689821));
#43659=CARTESIAN_POINT('',(-0.012581921556096,-0.0148111897659011,0.0435854931721957));
#43660=CARTESIAN_POINT('',(-0.0125338535684551,-0.0147537037166466,0.0436096942173712));
#43661=CARTESIAN_POINT('',(-0.0124940860684927,-0.0147035206656104,0.0436973228579851));
#43662=CARTESIAN_POINT('',(-0.0124955907346439,-0.0147022390336426,0.0437756932755677));
#43663=CARTESIAN_POINT('',(-0.0152554428038941,-0.0120387297395458,0.0434896423948305));
#43664=CARTESIAN_POINT('',(-0.015197109256151,-0.0119919639285616,0.0435139736236071));
#43665=CARTESIAN_POINT('',(-0.0151483977361707,-0.0119508055167351,0.0436014554263285));
#43666=CARTESIAN_POINT('',(-0.0151495935693689,-0.0119492859658235,0.0436797055035351));
#43667=CARTESIAN_POINT('',(-0.0163834997393635,-0.0104514186411031,0.0434429162689194));
#43668=CARTESIAN_POINT('',(-0.0163206232990258,-0.0104106326306365,0.0434671064785535));
#43669=CARTESIAN_POINT('',(-0.0162677931645333,-0.0103744327157288,0.0435547503556089));
#43670=CARTESIAN_POINT('',(-0.0162688141254918,-0.0103728386843743,0.043633133449291));
#43671=CARTESIAN_POINT('',(-0.0181180948755052,-0.00702795123329128,0.0433484458948482));
#43672=CARTESIAN_POINT('',(-0.018048377725369,-0.00700027368810441,0.0433725863307973));
#43673=CARTESIAN_POINT('',(-0.0179894049063615,-0.00697504552157947,0.0434602838245048));
#43674=CARTESIAN_POINT('',(-0.0179901210666772,-0.00697320868955981,0.043538710748284));
#43675=CARTESIAN_POINT('',(-0.0187328845045549,-0.00516713373106079,0.0432995252600545));
#43676=CARTESIAN_POINT('',(-0.0186609634707438,-0.0051466812890816,0.0433238478766118));
#43677=CARTESIAN_POINT('',(-0.0186000862209964,-0.0051276387903171,0.0434113389351564));
#43678=CARTESIAN_POINT('',(-0.0186006014453895,-0.00512576067388384,0.0434895965769441));
#43679=CARTESIAN_POINT('',(-0.0193827832507852,-0.00139217716998413,0.0432054268717574));
#43680=CARTESIAN_POINT('',(-0.0193081422241517,-0.00138623853652184,0.0432296697167476));
#43681=CARTESIAN_POINT('',(-0.0192445508952148,-0.00137954617751035,0.0433172534279926));
#43682=CARTESIAN_POINT('',(-0.0192446844798051,-0.00137764868123542,0.0433955871469998));
#43683=CARTESIAN_POINT('',(-0.019424673673698,0.000572591618044089,0.0431582858933068));
#43684=CARTESIAN_POINT('',(-0.0193496215132889,0.000570950790978695,0.0431823790926352));
#43685=CARTESIAN_POINT('',(-0.019285385811491,0.000571214061864182,0.0432701307623699));
#43686=CARTESIAN_POINT('',(-0.0192853283305864,0.000573170648562909,0.0433486021590327));
#43687=CARTESIAN_POINT('',(-0.0189348462154845,0.0043697410562523,0.0430627037786195));
#43688=CARTESIAN_POINT('',(-0.0188617966919163,0.00435347921143666,0.0430869761208192));
#43689=CARTESIAN_POINT('',(-0.0187990971022846,0.0043412371042362,0.0431745239086082));
#43690=CARTESIAN_POINT('',(-0.0187986540804816,0.00434315762703661,0.0432528280125303));
#43691=CARTESIAN_POINT('',(-0.0183971591744498,0.00625864624530665,0.0430145251915811));
#43692=CARTESIAN_POINT('',(-0.0183261678659743,0.00623511581432621,0.0430388357585548));
#43693=CARTESIAN_POINT('',(-0.0182651033996267,0.00621660486642616,0.0431263418765282));
#43694=CARTESIAN_POINT('',(-0.0182644858625964,0.00621841834748833,0.0432046119233684));
#43695=CARTESIAN_POINT('',(-0.0168114255453012,0.00974796456580604,0.0429208416185235));
#43696=CARTESIAN_POINT('',(-0.0167462529616046,0.00971084725244702,0.0429449893189298));
#43697=CARTESIAN_POINT('',(-0.0166897322456514,0.00968054832275472,0.0430326808335318));
#43698=CARTESIAN_POINT('',(-0.0166887718492012,0.00968220350615855,0.0431111029581461));
#43699=CARTESIAN_POINT('',(-0.015746810917611,0.0113882759971328,0.042872577634837));
#43700=CARTESIAN_POINT('',(-0.0156857861843996,0.0113448650330417,0.0428968114659125));
#43701=CARTESIAN_POINT('',(-0.0156327093668857,0.0113091695906071,0.0429844029331076));
#43702=CARTESIAN_POINT('',(-0.0156315516997354,0.0113107656680076,0.0430627428710397));
#43703=CARTESIAN_POINT('',(-0.0131979043879043,0.014263893099291,0.0427771799842653));
#43704=CARTESIAN_POINT('',(-0.0131467027239952,0.014209402593538,0.0428015048391955));
#43705=CARTESIAN_POINT('',(-0.0131018458953999,0.0141640584913093,0.0428889941244775));
#43706=CARTESIAN_POINT('',(-0.0131004299615031,0.0141653649215906,0.0429672503551503));
#43707=CARTESIAN_POINT('',(-0.0117104749854287,0.0155099910721682,0.0427307831768934));
#43708=CARTESIAN_POINT('',(-0.0116648346754129,0.0154504833966338,0.0427549392219934));
#43709=CARTESIAN_POINT('',(-0.0116245459516405,0.0154006105196224,0.0428426219902237));
#43710=CARTESIAN_POINT('',(-0.0116230404391685,0.0154017523029656,0.0429210369991081));
#43711=CARTESIAN_POINT('',(-0.0084157282397445,0.0175178646338017,0.0426357398842286));
#43712=CARTESIAN_POINT('',(-0.00838269791797529,0.0174504784084052,0.0426598557148911));
#43713=CARTESIAN_POINT('',(-0.00835293155804294,0.017393602493656,0.0427475807684539));
#43714=CARTESIAN_POINT('',(-0.00835114882150384,0.0173944633838914,0.0428260302906322));
#43715=CARTESIAN_POINT('',(-0.00664836906391361,0.0182624542001285,0.0425877615007644));
#43716=CARTESIAN_POINT('',(-0.00662222859555788,0.0181923787365993,0.0426120762142147));
#43717=CARTESIAN_POINT('',(-0.00659837148802767,0.0181331964817291,0.0426995761106777));
#43718=CARTESIAN_POINT('',(-0.00659653587630465,0.0181338616931928,0.042777840991438));
#43719=CARTESIAN_POINT('',(-0.00288750944558111,0.0192194487952228,0.0424922714769732));
#43720=CARTESIAN_POINT('',(-0.00287581787416988,0.0191455048095414,0.0425165325920182));
#43721=CARTESIAN_POINT('',(-0.00286423061226027,0.0190826492860442,0.0426040953733314));
#43722=CARTESIAN_POINT('',(-0.00286234625282073,0.0190829295288795,0.0426824119219572));
#43723=CARTESIAN_POINT('',(-0.000982578319707736,0.0194098494847792,0.0424463048591522));
#43724=CARTESIAN_POINT('',(-0.000978212251171632,0.0193349456530662,0.0424704332406481));
#43725=CARTESIAN_POINT('',(-0.000972814655148193,0.0192710005170299,0.0425581450577104));
#43726=CARTESIAN_POINT('',(-0.000970859241194737,0.0192710993398717,0.0426365837522657));
#43727=CARTESIAN_POINT('',(0.00287589180009033,0.0192202047701144,0.042349975600319));
#43728=CARTESIAN_POINT('',(0.00286539442935202,0.0191461251563339,0.0423742666714731));
#43729=CARTESIAN_POINT('',(0.00285809149226027,0.0190826922186695,0.042461793308621));
#43730=CARTESIAN_POINT('',(0.00286003397322915,0.0190824013977643,0.04254008008374));
#43731=CARTESIAN_POINT('',(0.00477346897214909,0.0188379101962389,0.0423026832697597));
#43732=CARTESIAN_POINT('',(0.00475566297139454,0.0187652520850334,0.0423269816551104));
#43733=CARTESIAN_POINT('',(0.0047420642066681,0.0187028826386092,0.0424145019720467));
#43734=CARTESIAN_POINT('',(0.00474391515520207,0.0187024134153455,0.0424927836716811));
#43735=CARTESIAN_POINT('',(0.00838993916839794,0.0175295632799056,0.0422088079806907));
#43736=CARTESIAN_POINT('',(0.00835806475986436,0.0174616169665215,0.0422329190972985));
#43737=CARTESIAN_POINT('',(0.008332296360323,0.0174028109599628,0.0423206520511072));
#43738=CARTESIAN_POINT('',(0.00833402349045457,0.0174019841115548,0.0423991081730488));
#43739=CARTESIAN_POINT('',(0.0101061585086325,0.0165984253158094,0.042160527287686));
#43740=CARTESIAN_POINT('',(0.010067698016863,0.0165341336698658,0.0421847389464463));
#43741=CARTESIAN_POINT('',(0.0100362946046989,0.0164783610062004,0.0422723555266183));
#43742=CARTESIAN_POINT('',(0.0100379807709512,0.0164773311856172,0.0423507160532588));
#43743=CARTESIAN_POINT('',(0.0131684392679074,0.0142905323206982,0.0420651643418744));
#43744=CARTESIAN_POINT('',(0.0131182003184821,0.014235164322694,0.0420894945050713));
#43745=CARTESIAN_POINT('',(0.0130765779767723,0.0141868495121099,0.0421769776058639));
#43746=CARTESIAN_POINT('',(0.0130779960586654,0.0141855391172854,0.0422552287543061));
#43747=CARTESIAN_POINT('',(0.0145429079810099,0.01288951653784,0.042018124682087));
#43748=CARTESIAN_POINT('',(0.0144871873247645,0.0128393724084036,0.0420423017411972));
#43749=CARTESIAN_POINT('',(0.0144406629767885,0.0127953267933943,0.0421299605576955));
#43750=CARTESIAN_POINT('',(0.0144419210348758,0.0127939131073594,0.0422083559096465));
#43751=CARTESIAN_POINT('',(0.0167879942968906,0.00978786677143619,0.0419237413668511));
#43752=CARTESIAN_POINT('',(0.016723506882985,0.00974958302562206,0.0419478919551198));
#43753=CARTESIAN_POINT('',(0.0166692535536996,0.00971540638638223,0.0420355776769293));
#43754=CARTESIAN_POINT('',(0.0166702533162291,0.00971369909710044,0.0421139949281423));
#43755=CARTESIAN_POINT('',(0.0176903844021271,0.00804166252515399,0.0418747153658528));
#43756=CARTESIAN_POINT('',(0.0176225658916305,0.00801018311428441,0.0418990411512617));
#43757=CARTESIAN_POINT('',(0.0175654344546478,0.00798183123197196,0.0419865287048129));
#43758=CARTESIAN_POINT('',(0.0175662368426482,0.00798005978833373,0.0420647834773854));
#43759=CARTESIAN_POINT('',(0.0189242191104922,0.00441631646227505,0.0417807159516119));
#43760=CARTESIAN_POINT('',(0.0188514220757375,0.00439873611332809,0.0418049488164648));
#43761=CARTESIAN_POINT('',(0.0187896496899181,0.00438214351233717,0.0418925439295008));
#43762=CARTESIAN_POINT('',(0.0187900792955159,0.00438029121242141,0.0419708870010681));
#43763=CARTESIAN_POINT('',(0.0192737625347307,0.00248610121336098,0.0417335775265417));
#43764=CARTESIAN_POINT('',(0.0191993895656811,0.00247593097639031,0.0417576755962962));
#43765=CARTESIAN_POINT('',(0.0191360014837637,0.0024655773417966,0.0418454216402157));
#43766=CARTESIAN_POINT('',(0.0191362522391118,0.00246363238888985,0.041923888411933));
#43767=CARTESIAN_POINT('',(0.0193860388687333,-0.0013478782594415,0.0416377966747266));
#43768=CARTESIAN_POINT('',(0.0193113542405968,-0.00134326722999368,0.0416620783959207));
#43769=CARTESIAN_POINT('',(0.0192475281217665,-0.00134100173440581,0.0417496155991939));
#43770=CARTESIAN_POINT('',(0.019247391478997,-0.00134296521202914,0.0418279110276031));
#43771=CARTESIAN_POINT('',(0.0191537270400506,-0.00328487522397506,0.0415900304891562));
#43772=CARTESIAN_POINT('',(0.0190799071367699,-0.00327281033809035,0.0416143356311441));
#43773=CARTESIAN_POINT('',(0.0190166777180566,-0.00326413751039363,0.0417018480438158));
#43774=CARTESIAN_POINT('',(0.0190163540233799,-0.00326602313964124,0.0417801232575495));
#43775=CARTESIAN_POINT('',(0.018131602323943,-0.00699439813966341,0.0414959847757827));
#43776=CARTESIAN_POINT('',(0.0180614082995736,-0.00696794459720087,0.0415201252490797));
#43777=CARTESIAN_POINT('',(0.0180008225277482,-0.00694687076797024,0.0416078248617962));
#43778=CARTESIAN_POINT('',(0.0180001325357559,-0.00694865858899434,0.0416862536254287));
#43779=CARTESIAN_POINT('',(0.0173476811165876,-0.00876108347613509,0.0414481936654002));
#43780=CARTESIAN_POINT('',(0.0172805763289672,-0.00872785066917969,0.0414724363477006));
#43781=CARTESIAN_POINT('',(0.0172225434833428,-0.00870098502212939,0.0415600177505497));
#43782=CARTESIAN_POINT('',(0.0172216523613874,-0.00870274320862069,0.0416383494356615));
#43783=CARTESIAN_POINT('',(0.0152701028102562,-0.0120213338287211,0.0413522878914658));
#43784=CARTESIAN_POINT('',(0.0152109922474703,-0.0119755308451478,0.0413766103003943));
#43785=CARTESIAN_POINT('',(0.0151595810536061,-0.0119377655573325,0.0414641024695183));
#43786=CARTESIAN_POINT('',(0.0151583887887771,-0.0119392754696399,0.041542361071393));
#43787=CARTESIAN_POINT('',(0.0140140902539154,-0.0134661964537371,0.0413065977037004));
#43788=CARTESIAN_POINT('',(0.0139596097477583,-0.0134146292067217,0.0413307404212872));
#43789=CARTESIAN_POINT('',(0.0139119301176914,-0.0133717242869215,0.0414184383077074));
#43790=CARTESIAN_POINT('',(0.0139106244354892,-0.0133730895427255,0.0414968657228129));
#43791=CARTESIAN_POINT('',(0.0110622629856551,-0.0159800311161299,0.0412109487492704));
#43792=CARTESIAN_POINT('',(0.0110190678886151,-0.0159186763628627,0.0412350758816643));
#43793=CARTESIAN_POINT('',(0.0109807473090292,-0.015867198836065,0.0413227878658976));
#43794=CARTESIAN_POINT('',(0.0109791159661971,-0.0158683335200576,0.041401226649222));
#43795=CARTESIAN_POINT('',(0.00942964141615498,-0.0169927028834982,0.0411629287682235));
#43796=CARTESIAN_POINT('',(0.00939283905067548,-0.0169276027821737,0.0411872473787582));
#43797=CARTESIAN_POINT('',(0.00936000297860796,-0.0168729037490331,0.0412747429321204));
#43798=CARTESIAN_POINT('',(0.00935829698368026,-0.0168738473224675,0.0413530042565083));
#43799=CARTESIAN_POINT('',(0.00588892122224943,-0.0185202352873659,0.0410681148857522));
#43800=CARTESIAN_POINT('',(0.00586568600622161,-0.0184490634292052,0.0410923677840248));
#43801=CARTESIAN_POINT('',(0.00584430466162974,-0.0183888183285153,0.0411799399593064));
#43802=CARTESIAN_POINT('',(0.00584248904222944,-0.0183893928036825,0.041258264213322));
#43803=CARTESIAN_POINT('',(0.00401040287879892,-0.0190152822736237,0.0410213640989462));
#43804=CARTESIAN_POINT('',(0.00399435979562309,-0.0189419983273946,0.0410454981125339));
#43805=CARTESIAN_POINT('',(0.00397901288415929,-0.0188797027745045,0.0411332034428664));
#43806=CARTESIAN_POINT('',(0.003977094168951,-0.0188801069727624,0.0412116368083255));
#43807=CARTESIAN_POINT('',(0.00019213328247138,-0.0194321011015831,0.0409255766983548));
#43808=CARTESIAN_POINT('',(0.000190813787669677,-0.0193573059724893,0.0409498744388859));
#43809=CARTESIAN_POINT('',(0.000188022001281524,-0.0192935317685946,0.0410373935668177));
#43810=CARTESIAN_POINT('',(0.000186060852112889,-0.0192935507020084,0.0411156741895074));
#43811=CARTESIAN_POINT('',(-0.00176339237332431,-0.0193524541760977,0.0408778356995182));
#43812=CARTESIAN_POINT('',(-0.00175718674408749,-0.019277896166484,0.0409021261523958));
#43813=CARTESIAN_POINT('',(-0.00175352229433959,-0.0192141535103437,0.0409896556080293));
#43814=CARTESIAN_POINT('',(-0.0017554214332428,-0.0192139805414387,0.041067944807168));
#43815=CARTESIAN_POINT('',(-0.00552669521047183,-0.0186307886709499,0.0407842954458791));
#43816=CARTESIAN_POINT('',(-0.00550590912885297,-0.0185586673831611,0.0408084000411789));
#43817=CARTESIAN_POINT('',(-0.00548971578084918,-0.0184965282212371,0.0408961402574824));
#43818=CARTESIAN_POINT('',(-0.0054915544559697,-0.0184959828695907,0.0409746023332713));
#43819=CARTESIAN_POINT('',(-0.00737943021860454,-0.0179765988957228,0.0407356098240556));
#43820=CARTESIAN_POINT('',(-0.00735152872707246,-0.0179070883826029,0.0407598318655682));
#43821=CARTESIAN_POINT('',(-0.00732926371575064,-0.0178471040041725,0.0408474366511579));
#43822=CARTESIAN_POINT('',(-0.00733108954015883,-0.0178463514792928,0.0409257875057461));
#43823=CARTESIAN_POINT('',(-0.0107539094744667,-0.0161849935846676,0.0406406636701057));
#43824=CARTESIAN_POINT('',(-0.0107130144414301,-0.0161224068015081,0.0406649920952624));
#43825=CARTESIAN_POINT('',(-0.0106795157575241,-0.0160681414903697,0.0407524772614855));
#43826=CARTESIAN_POINT('',(-0.0106811201319611,-0.0160670721568958,0.0408307301101068));
#43827=CARTESIAN_POINT('',(-0.0123287371074195,-0.0150241784256509,0.0405938515736219));
#43828=CARTESIAN_POINT('',(-0.0122816063227758,-0.0149658529672547,0.0406180147541832));
#43829=CARTESIAN_POINT('',(-0.0122425881867603,-0.0149149957976942,0.0407056893925126));
#43830=CARTESIAN_POINT('',(-0.0122440524668192,-0.0149137999712962,0.0407840977302332));
#43831=CARTESIAN_POINT('',(-0.015063442617279,-0.0122807277922009,0.0404982120005546));
#43832=CARTESIAN_POINT('',(-0.0150057002924285,-0.0122328858993998,0.0405223753795027));
#43833=CARTESIAN_POINT('',(-0.0149574411122037,-0.0121906940296751,0.0406100462467542));
#43834=CARTESIAN_POINT('',(-0.01495870084232,-0.0121891558158891,0.0406884512908035));
#43835=CARTESIAN_POINT('',(-0.0161979325896151,-0.0107387571335358,0.0404505183968822));
#43836=CARTESIAN_POINT('',(-0.0161359416433861,-0.0106969479749206,0.0404748470795084));
#43837=CARTESIAN_POINT('',(-0.0160840105493353,-0.0106599198137374,0.0405623314322008));
#43838=CARTESIAN_POINT('',(-0.0160850816918558,-0.0106582995432656,0.0406405835842443));
#43839=CARTESIAN_POINT('',(-0.0180045814485912,-0.00731727795952108,0.0403556178697589));
#43840=CARTESIAN_POINT('',(-0.0179354020292857,-0.00728854002582057,0.0403798402539448));
#43841=CARTESIAN_POINT('',(-0.0178769525958173,-0.00726249623056953,0.0404674473340524));
#43842=CARTESIAN_POINT('',(-0.017877665986857,-0.00726073419497197,0.0405458002220391));
#43843=CARTESIAN_POINT('',(-0.0186409127840566,-0.00549562960728315,0.0403091844876066));
#43844=CARTESIAN_POINT('',(-0.0185690795987422,-0.00547385462536609,0.0403332878371306));
#43845=CARTESIAN_POINT('',(-0.0185081269567373,-0.0054536303971612,0.0404210278087886));
#43846=CARTESIAN_POINT('',(-0.0185086819893113,-0.0054517463226931,0.0404994895905958));
#43847=CARTESIAN_POINT('',(-0.0193578808426837,-0.00171297754448892,0.0402130314685225));
#43848=CARTESIAN_POINT('',(-0.0192834066548136,-0.00170580555167016,0.0402373215284279));
#43849=CARTESIAN_POINT('',(-0.019220030134504,-0.00169802519972375,0.0403248493228966));
#43850=CARTESIAN_POINT('',(-0.01922020299048,-0.001696067201853,0.040403137040384));
#43851=CARTESIAN_POINT('',(-0.0194314445620402,0.000234326868795167,0.0401654061237091));
#43852=CARTESIAN_POINT('',(-0.0193566395852132,0.000234010517959497,0.0401897048712735));
#43853=CARTESIAN_POINT('',(-0.0192928221274484,0.000235378096732732,0.040277224670129));
#43854=CARTESIAN_POINT('',(-0.0192927990402418,0.000237288739506294,0.0403555059457344));
#43855=CARTESIAN_POINT('',(-0.0190071439374079,0.00404787190329747,0.0400716185672009));
#43856=CARTESIAN_POINT('',(-0.0189336516231657,0.00403281666980165,0.0400957533809963));
#43857=CARTESIAN_POINT('',(-0.0188704912700394,0.00402156036151489,0.0401834593019227));
#43858=CARTESIAN_POINT('',(-0.0188700914838369,0.00402343735438757,0.0402618932361842));
#43859=CARTESIAN_POINT('',(-0.0185019019710979,0.00594205710077393,0.040023053450417));
#43860=CARTESIAN_POINT('',(-0.0184304462375758,0.00591972522436116,0.0400473054411028));
#43861=CARTESIAN_POINT('',(-0.0183689512924275,0.00590226526823803,0.0401348762761194));
#43862=CARTESIAN_POINT('',(-0.0183683462818142,0.00590413969905943,0.0402131992968648));
#43863=CARTESIAN_POINT('',(-0.0169768882879332,0.00945543410936856,0.0399281103095153));
#43864=CARTESIAN_POINT('',(-0.0169112821115633,0.00941955212853585,0.0399524289425286));
#43865=CARTESIAN_POINT('',(-0.0168545467113079,0.00939038667184233,0.0400399254990433));
#43866=CARTESIAN_POINT('',(-0.0168536093313915,0.00939206384238749,0.0401181877041794));
#43867=CARTESIAN_POINT('',(-0.01593535832353,0.0111223090713971,0.0398812109428551));
#43868=CARTESIAN_POINT('',(-0.0158735159105026,0.0110798324171594,0.0399053389666608));
#43869=CARTESIAN_POINT('',(-0.0158197278755644,0.0110448507473462,0.0399930533704728));
#43870=CARTESIAN_POINT('',(-0.0158186484123805,0.0110464051239283,0.0400714943318944));
#43871=CARTESIAN_POINT('',(-0.0134454518985074,0.0140306589988565,0.0397865925416715));
#43872=CARTESIAN_POINT('',(-0.0133931288274549,0.013976916359118,0.0398107342991805));
#43873=CARTESIAN_POINT('',(-0.0133471833957635,0.0139321647231977,0.0398984295500356));
#43874=CARTESIAN_POINT('',(-0.0133457485652741,0.0139335458153675,0.0399768545933033));
#43875=CARTESIAN_POINT('',(-0.011960751940929,0.0153155583646799,0.0397375831615763));
#43876=CARTESIAN_POINT('',(-0.0119142639235653,0.0152569925928259,0.0397619054231763));
#43877=CARTESIAN_POINT('',(-0.0118733169879335,0.0152080831693273,0.0398493969333267));
#43878=CARTESIAN_POINT('',(-0.0118717815028061,0.0152092790370377,0.0399276549481262));
#43879=CARTESIAN_POINT('',(-0.00872162776691554,0.0173657492824739,0.0396434082267646));
#43880=CARTESIAN_POINT('',(-0.00868750821375636,0.0172990977852855,0.039667651378194));
#43881=CARTESIAN_POINT('',(-0.00865693076962195,0.0172429405691964,0.0397552346856925));
#43882=CARTESIAN_POINT('',(-0.00865522841726458,0.0172437926779991,0.0398335680705144));
#43883=CARTESIAN_POINT('',(-0.00693350364422637,0.0181547616987217,0.0395962668314319));
#43884=CARTESIAN_POINT('',(-0.00690620437943324,0.0180848943918416,0.0396204075659489));
#43885=CARTESIAN_POINT('',(-0.00688130993302412,0.018025776493363,0.0397081051752782));
#43886=CARTESIAN_POINT('',(-0.00687947509641899,0.0180264764200233,0.0397865321992344));
#43887=CARTESIAN_POINT('',(-0.00322453524254062,0.0191637764355218,0.0395004073005348));
#43888=CARTESIAN_POINT('',(-0.00321155329862424,0.019090113767052,0.0395247123010259));
#43889=CARTESIAN_POINT('',(-0.00319884187363129,0.0190275709231919,0.0396122232568542));
#43890=CARTESIAN_POINT('',(-0.00319691082962554,0.0190278950720074,0.0396904971845612));
#43891=CARTESIAN_POINT('',(-0.00129919072967843,0.0193905845890196,0.0394532179801282));
#43892=CARTESIAN_POINT('',(-0.00129360490319829,0.0193159612092455,0.0394775000810617));
#43893=CARTESIAN_POINT('',(-0.00128721010180883,0.0192524133851804,0.0395650391559288));
#43894=CARTESIAN_POINT('',(-0.00128530982278602,0.0192525411077439,0.0396433362491825));
#43895=CARTESIAN_POINT('',(0.00255902787432145,0.0192654480198307,0.0393589678198288));
#43896=CARTESIAN_POINT('',(0.00254972219577876,0.0191909555052613,0.0393830652854638));
#43897=CARTESIAN_POINT('',(0.00254340208585965,0.0191270341900853,0.0394708134257302));
#43898=CARTESIAN_POINT('',(0.00254530713983667,0.0191267815381943,0.0395492819968932));
#43899=CARTESIAN_POINT('',(0.00444305415507311,0.018920683340969,0.0393114195738665));
#43900=CARTESIAN_POINT('',(0.0044265025633268,0.018847634599306,0.0393356514402658));
#43901=CARTESIAN_POINT('',(0.00441401087617363,0.0187848918998344,0.0394232450563293));
#43902=CARTESIAN_POINT('',(0.00441593234193343,0.0187844376529192,0.0395015867513894));
#43903=CARTESIAN_POINT('',(0.0081155234358224,0.017659536267152,0.0392150014766233));
#43904=CARTESIAN_POINT('',(0.0080848214364896,0.0175913526381763,0.0392393282335753));
#43905=CARTESIAN_POINT('',(0.00806013444744089,0.0175325379856509,0.0393268154080085));
#43906=CARTESIAN_POINT('',(0.0080618825123445,0.0175317314245367,0.0394050699108451));
#43907=CARTESIAN_POINT('',(0.00981354217592872,0.0167748457507326,0.0391692829636585));
#43908=CARTESIAN_POINT('',(0.00977615945611022,0.0167098257968652,0.0391934345795327));
#43909=CARTESIAN_POINT('',(0.0097456154724898,0.0166534461042345,0.0392811220489701));
#43910=CARTESIAN_POINT('',(0.00974725611746331,0.0166524908972105,0.0393595408978778));
#43911=CARTESIAN_POINT('',(0.0129360951432808,0.0145036320981578,0.0390738099458165));
#43912=CARTESIAN_POINT('',(0.0128866379295421,0.0144472916781401,0.0390979857807174));
#43913=CARTESIAN_POINT('',(0.0128456567142085,0.0143980343100778,0.0391856425630789));
#43914=CARTESIAN_POINT('',(0.0128471421335855,0.0143967146912262,0.0392640360535999));
#43915=CARTESIAN_POINT('',(0.0143150193080017,0.0131425534125171,0.0390256063403529));
#43916=CARTESIAN_POINT('',(0.0142603468414684,0.0130915547374476,0.0390499362984668));
#43917=CARTESIAN_POINT('',(0.0142148599328177,0.0130468555414553,0.0391374193147547));
#43918=CARTESIAN_POINT('',(0.0142161697159497,0.0130454253788721,0.0392156703759364));
#43919=CARTESIAN_POINT('',(0.0166225528799177,0.010067382546611,0.038931373355256));
#43920=CARTESIAN_POINT('',(0.0165587714851361,0.0100280789617687,0.0389555861269347));
#43921=CARTESIAN_POINT('',(0.016505154392705,0.00999312567443186,0.0390432041584913));
#43922=CARTESIAN_POINT('',(0.0165061370301603,0.0099914986388418,0.0391215660289867));
#43923=CARTESIAN_POINT('',(0.0175492105589036,0.00834737793199038,0.0388842404592576));
#43924=CARTESIAN_POINT('',(0.0174816865750995,0.00831462399998431,0.0389083509308422));
#43925=CARTESIAN_POINT('',(0.017424670543974,0.00828510605380299,0.0389960827451585));
#43926=CARTESIAN_POINT('',(0.0174255147527736,0.00828332962245758,0.0390745378270751));
#43927=CARTESIAN_POINT('',(0.0188458641467242,0.00473953216237909,0.0387884879194788));
#43928=CARTESIAN_POINT('',(0.0187734603459155,0.00472072645929015,0.0388127852373821));
#43929=CARTESIAN_POINT('',(0.018712115027066,0.00470307102651411,0.0389003048529412));
#43930=CARTESIAN_POINT('',(0.018712593041949,0.00470116748051165,0.0389785858691391));
#43931=CARTESIAN_POINT('',(0.019227674046985,0.00281385318638663,0.0387405884459633));
#43932=CARTESIAN_POINT('',(0.0191537355807173,0.00280244196433158,0.0387648797081903));
#43933=CARTESIAN_POINT('',(0.0190909074720484,0.00279109067856667,0.0388524081339661));
#43934=CARTESIAN_POINT('',(0.0190911840350891,0.00278920249838559,0.0389306964894435));
#43935=CARTESIAN_POINT('',(0.019406698543977,-0.00101085205758943,0.0386469886990866));
#43936=CARTESIAN_POINT('',(0.0193317482426553,-0.00100753253556381,0.0386711182270064));
#43937=CARTESIAN_POINT('',(0.0192675947531134,-0.00100634376061779,0.0387588300103844));
#43938=CARTESIAN_POINT('',(0.0192674949877194,-0.0010082635254978,0.0388372687487328));
#43939=CARTESIAN_POINT('',(0.019204959553772,-0.00296586744453016,0.0385982170171152));
#43940=CARTESIAN_POINT('',(0.0191308966912634,-0.00295502470244232,0.0386224780246699));
#43941=CARTESIAN_POINT('',(0.0190674416992468,-0.00294743087934119,0.0387100386227964));
#43942=CARTESIAN_POINT('',(0.0190671383876761,-0.00294937568700589,0.0387883532508879));
#43943=CARTESIAN_POINT('',(0.0182501324132737,-0.00667478502307092,0.0385033576663385));
#43944=CARTESIAN_POINT('',(0.018179703890677,-0.0066496385805664,0.0385276720163145));
#43945=CARTESIAN_POINT('',(0.0181190878376674,-0.00662973132821225,0.0386151735487677));
#43946=CARTESIAN_POINT('',(0.0181184260275392,-0.00663153236608867,0.0386934398400686));
#43947=CARTESIAN_POINT('',(0.0174853534374695,-0.00848057633974107,0.0384566148691321));
#43948=CARTESIAN_POINT('',(0.0174175894303183,-0.00844833684682815,0.0384807306646094));
#43949=CARTESIAN_POINT('',(0.0173589470012821,-0.00842223583780885,0.0385684586167564));
#43950=CARTESIAN_POINT('',(0.0173581210465426,-0.00842394795680733,0.0386469106780912));
#43951=CARTESIAN_POINT('',(0.0154785716070732,-0.0117501651746574,0.0383616497868883));
#43952=CARTESIAN_POINT('',(0.015418486581854,-0.0117052963656775,0.0383858059075054));
#43953=CARTESIAN_POINT('',(0.0153661184052046,-0.0116683119178918,0.0384734849231699));
#43954=CARTESIAN_POINT('',(0.0153649179745633,-0.0116698997887883,0.0385518966467288));
#43955=CARTESIAN_POINT('',(0.0142234376982746,-0.0132419648869437,0.0383130552616885));
#43956=CARTESIAN_POINT('',(0.0141683093057633,-0.0131914491972484,0.0383373804449651));
#43957=CARTESIAN_POINT('',(0.0141201762729626,-0.0131495973635277,0.0384248687309179));
#43958=CARTESIAN_POINT('',(0.0141188501423668,-0.0131510181564485,0.0385031241067679));
#43959=CARTESIAN_POINT('',(0.0113346703524442,-0.0157858406654838,0.0382185630351736));
#43960=CARTESIAN_POINT('',(0.0112905221373944,-0.0157253443158286,0.0382427966886846));
#43961=CARTESIAN_POINT('',(0.0112515123813048,-0.0156746533547692,0.0383303908380344));
#43962=CARTESIAN_POINT('',(0.0112499648737552,-0.0156757614881421,0.0384087331156003));
#43963=CARTESIAN_POINT('',(0.00971288679571012,-0.0168337228282251,0.0381719175555109));
#43964=CARTESIAN_POINT('',(0.00967490223484882,-0.0167690440392301,0.0381960644883469));
#43965=CARTESIAN_POINT('',(0.00964099001599442,-0.0167146052157371,0.0382837549903342));
#43966=CARTESIAN_POINT('',(0.00963928646524814,-0.0167155869636415,0.0383621761779478));
#43967=CARTESIAN_POINT('',(0.00618680655579516,-0.0184232718057472,0.0380754658022996));
#43968=CARTESIAN_POINT('',(0.00616244848485818,-0.0183525547089153,0.0380997768839514));
#43969=CARTESIAN_POINT('',(0.00614010314766136,-0.0182927813444199,0.0381872809991016));
#43970=CARTESIAN_POINT('',(0.00613824926368048,-0.0182934028293015,0.0382655493232916));
#43971=CARTESIAN_POINT('',(0.00434434565899893,-0.0189430548430776,0.0380289637754413));
#43972=CARTESIAN_POINT('',(0.00432704675323807,-0.0188702357548829,0.0380532377199637));
#43973=CARTESIAN_POINT('',(0.00431069790203453,-0.0188084759455217,0.0381407861665265));
#43974=CARTESIAN_POINT('',(0.00430884367707529,-0.0188089018960293,0.038219090950365));
#43975=CARTESIAN_POINT('',(0.00049971302025047,-0.019428998627159,0.0379343239189305));
#43976=CARTESIAN_POINT('',(0.000497198041504029,-0.0193539599551106,0.0379584163646268));
#43977=CARTESIAN_POINT('',(0.000493392381103726,-0.0192898275737404,0.0380461700429039));
#43978=CARTESIAN_POINT('',(0.000491467655240249,-0.0192898777578237,0.0381246431523179));
#43979=CARTESIAN_POINT('',(-0.00142299260754889,-0.0193817406272071,0.0378864924453864));
#43980=CARTESIAN_POINT('',(-0.00141809504677111,-0.0193070186093912,0.0379107340192279));
#43981=CARTESIAN_POINT('',(-0.00141559149936843,-0.0192431173300155,0.0379983166189465));
#43982=CARTESIAN_POINT('',(-0.00141755890393027,-0.0192429698914113,0.0380766492816992));
#43983=CARTESIAN_POINT('',(-0.00522021770879957,-0.0187193940741252,0.0377908527938189));
#43984=CARTESIAN_POINT('',(-0.00520068545450459,-0.0186472141752514,0.037815176260299));
#43985=CARTESIAN_POINT('',(-0.00518560869929645,-0.0185852340872855,0.0379026672625595));
#43986=CARTESIAN_POINT('',(-0.00518745998008488,-0.0185847147527988,0.0379809249098162));
#43987=CARTESIAN_POINT('',(-0.00706460087853033,-0.0181039357281884,0.0377444334742754));
#43988=CARTESIAN_POINT('',(-0.00703786096634784,-0.0180338545865875,0.0377685751215507));
#43989=CARTESIAN_POINT('',(-0.00701652477839413,-0.017973368867882,0.0378562736143509));
#43990=CARTESIAN_POINT('',(-0.00701830189552598,-0.017972679116116,0.0379347014913153));
#43991=CARTESIAN_POINT('',(-0.0104861914121819,-0.0163613825910883,0.0376493565744482));
#43992=CARTESIAN_POINT('',(-0.0104462485127058,-0.0162979652177063,0.0376735450790744));
#43993=CARTESIAN_POINT('',(-0.0104135603769271,-0.0162428867200877,0.0377611875441761));
#43994=CARTESIAN_POINT('',(-0.0104152336700229,-0.0162418183620689,0.0378395692912002));
#43995=CARTESIAN_POINT('',(-0.01207891400749,-0.0152223783460422,0.037600711886929));
#43996=CARTESIAN_POINT('',(-0.012032908068334,-0.0151634470378172,0.0376250425234767));
#43997=CARTESIAN_POINT('',(-0.0119949858388776,-0.0151121779194518,0.0377125248898505));
#43998=CARTESIAN_POINT('',(-0.0119965012289499,-0.0151109726135702,0.0377907754230611));
#43999=CARTESIAN_POINT('',(-0.0148311285373011,-0.0125568682379528,0.0375068681710913));
#44000=CARTESIAN_POINT('',(-0.0147743172321318,-0.0125080120355757,0.0375310707473459));
#44001=CARTESIAN_POINT('',(-0.0147268542025376,-0.0124650460047888,0.0376187003831675));
#44002=CARTESIAN_POINT('',(-0.0147280807018185,-0.0124635939401517,0.0376970717716093));
#44003=CARTESIAN_POINT('',(-0.016023338217248,-0.0109952313659276,0.0374593571749295));
#44004=CARTESIAN_POINT('',(-0.0159617938164897,-0.0109523019516451,0.0374834754164168));
#44005=CARTESIAN_POINT('',(-0.0159101251848468,-0.01091421724169,0.0375711983470121));
#44006=CARTESIAN_POINT('',(-0.0159112385943021,-0.0109125929807456,0.037649646134008));
#44007=CARTESIAN_POINT('',(-0.0178674960710242,-0.00764011945348385,0.0373637399470384));
#44008=CARTESIAN_POINT('',(-0.0177989527475963,-0.00761018147434739,0.037388044166753));
#44009=CARTESIAN_POINT('',(-0.0177411529848847,-0.00758312021038884,0.0374755560085341));
#44010=CARTESIAN_POINT('',(-0.0177419225641817,-0.00758131801831355,0.0375538306562103));
#44011=CARTESIAN_POINT('',(-0.018547838985748,-0.00579698411247787,0.0373158897342672));
#44012=CARTESIAN_POINT('',(-0.018476597245384,-0.00577410683765023,0.0373401729609822));
#44013=CARTESIAN_POINT('',(-0.0184163133217148,-0.00575303272943732,0.0374277106322001));
#44014=CARTESIAN_POINT('',(-0.0184168824207991,-0.00575121365323234,0.0375060065749605));
#44015=CARTESIAN_POINT('',(-0.0193252414788857,-0.00204511672800822,0.0372222028343277));
#44016=CARTESIAN_POINT('',(-0.0192506917089206,-0.00203663972521744,0.037246327760038));
#44017=CARTESIAN_POINT('',(-0.0191871368143089,-0.00202774823372296,0.0373340446144194));
#44018=CARTESIAN_POINT('',(-0.0191873400309585,-0.00202583294549132,0.0374124875069261));
#44019=CARTESIAN_POINT('',(-0.0194329094916537,-9.05799127225192E-5,0.0371735521390737));
#44020=CARTESIAN_POINT('',(-0.0193580721245975,-8.96423798313532E-5,0.037197821703061));
#44021=CARTESIAN_POINT('',(-0.0192942275335136,-8.71651879981286E-5,0.0372853725909127));
#44022=CARTESIAN_POINT('',(-0.0192942337078952,-8.51982643077479E-5,0.0373636792586044));
#44023=CARTESIAN_POINT('',(-0.0190711042104053,0.00373284239430641,0.0370785083301443));
#44024=CARTESIAN_POINT('',(-0.0189975972718238,0.00371904031452049,0.0371028178672844));
#44025=CARTESIAN_POINT('',(-0.0189345998782528,0.00370887329893731,0.0371903249792992));
#44026=CARTESIAN_POINT('',(-0.0189342288561442,0.00371075339281345,0.0372685958514727));
#44027=CARTESIAN_POINT('',(-0.0186041912754882,0.00561953539167989,0.0370322289124419));
#44028=CARTESIAN_POINT('',(-0.0185321777911545,0.00559837272669547,0.0370563348311793));
#44029=CARTESIAN_POINT('',(-0.0184701313765664,0.0055818380789744,0.0371440737029468));
#44030=CARTESIAN_POINT('',(-0.0184695829373792,0.00558366615936054,0.0372225347088254));
#44031=CARTESIAN_POINT('',(-0.0171287473134776,0.00918111797110836,0.0369366617089299));
#44032=CARTESIAN_POINT('',(-0.0170623892396143,0.00914621971976329,0.0369608316648687));
#44033=CARTESIAN_POINT('',(-0.0170048970494583,0.00911790250396981,0.0370484950420105));
#44034=CARTESIAN_POINT('',(-0.0170039602345416,0.00911965777877905,0.0371268939357847));
#44035=CARTESIAN_POINT('',(-0.0161383648576022,0.0108287162688267,0.0368888128118898));
#44036=CARTESIAN_POINT('',(-0.0160759447578151,0.0107875457132842,0.0369131404453162));
#44037=CARTESIAN_POINT('',(-0.0160218041980741,0.0107538247362759,0.0370006260387094));
#44038=CARTESIAN_POINT('',(-0.0160207207046064,0.0107554352591012,0.0370788792111389));
#44039=CARTESIAN_POINT('',(-0.0136685562721545,0.0138163527932191,0.036793714225605));
#44040=CARTESIAN_POINT('',(-0.0136154643792597,0.013763507738302,0.0368179391952823));
#44041=CARTESIAN_POINT('',(-0.0135689795293521,0.0137195390091569,0.0369055432451919));
#44042=CARTESIAN_POINT('',(-0.0135676247970923,0.0137208759513757,0.0369838936430815));
#44043=CARTESIAN_POINT('',(-0.0122429028720005,0.015093799560696,0.0367473781171091));
#44044=CARTESIAN_POINT('',(-0.0121952121305115,0.0150359205009187,0.0367715340771391));
#44045=CARTESIAN_POINT('',(-0.0121531586006765,0.0149875174588499,0.0368592142794031));
#44046=CARTESIAN_POINT('',(-0.0121516297248808,0.0149887559101737,0.0369376270142908));
#44047=CARTESIAN_POINT('',(-0.00901201976866163,0.0172184505126157,0.0366509953904922));
#44048=CARTESIAN_POINT('',(-0.00897682626097934,0.0171524556408082,0.0366753079862759));
#44049=CARTESIAN_POINT('',(-0.00894534739833079,0.0170969501197653,0.0367628104930834));
#44050=CARTESIAN_POINT('',(-0.00894361782180382,0.0170978539285752,0.0368410775073646));
#44051=CARTESIAN_POINT('',(-0.00725761413657459,0.0180274818560194,0.0366041627325707));
#44052=CARTESIAN_POINT('',(-0.00722911762950855,0.0179582554483319,0.0366284200075637));
#44053=CARTESIAN_POINT('',(-0.00720328902087814,0.0178997914362247,0.036715987498159));
#44054=CARTESIAN_POINT('',(-0.00720152656681416,0.0179005021385607,0.0367943079070936));
#44055=CARTESIAN_POINT('',(-0.00356301574194221,0.0191046951564421,0.0365101062998508));
#44056=CARTESIAN_POINT('',(-0.00354867545444478,0.0190309967968961,0.0365341948820525));
#44057=CARTESIAN_POINT('',(-0.00353477906593163,0.0189682693791576,0.0366219526836391));
#44058=CARTESIAN_POINT('',(-0.00353288083809403,0.018968624480678,0.0367004291670056));
#44059=CARTESIAN_POINT('',(-0.00163030801356091,0.0193644544794528,0.0364615160434953));
#44060=CARTESIAN_POINT('',(-0.00162344145580831,0.0192899054784977,0.0364857686894514));
#44061=CARTESIAN_POINT('',(-0.00161590810152796,0.0192264253025067,0.0365733387767667));
#44062=CARTESIAN_POINT('',(-0.00161394540795644,0.0192265874866579,0.0366516611856013));
#44063=CARTESIAN_POINT('',(0.00220542883222762,0.0193072407402312,0.0363665104815927));
#44064=CARTESIAN_POINT('',(0.00219751083367931,0.019232863449794,0.0363908148325363));
#44065=CARTESIAN_POINT('',(0.00219238166704181,0.0191692475419351,0.0364783278268363));
#44066=CARTESIAN_POINT('',(0.0021942866525446,0.0191690268988398,0.0365566035194738));
#44067=CARTESIAN_POINT('',(0.00414051581960644,0.0189869253580856,0.0363198423738946));
#44068=CARTESIAN_POINT('',(0.00412506819282153,0.0189134636193086,0.0363439366760617));
#44069=CARTESIAN_POINT('',(0.00411344152877879,0.0188502961119186,0.0364316890676605));
#44070=CARTESIAN_POINT('',(0.00411529796524559,0.0188498963213753,0.0365101611861028));
#44071=CARTESIAN_POINT('',(0.00778328794413445,0.0178060518634451,0.0362247298311951));
#44072=CARTESIAN_POINT('',(0.00775381675083955,0.0177371450529443,0.0362489191090306));
#44073=CARTESIAN_POINT('',(0.00773021475367226,0.0176776085770064,0.0363365599232303));
#44074=CARTESIAN_POINT('',(0.00773205627627711,0.0176768089430711,0.0364149402666696));
#44075=CARTESIAN_POINT('',(0.00954191235829089,0.0169280969611422,0.0361755156541392));
#44076=CARTESIAN_POINT('',(0.00950576273114558,0.0168627489131564,0.0361999086999894));
#44077=CARTESIAN_POINT('',(0.00947641473143195,0.0168062726093583,0.0362873196956842));
#44078=CARTESIAN_POINT('',(0.00947809970864682,0.0168053194180008,0.0363655117092009));
#44079=CARTESIAN_POINT('',(0.0118927992392535,0.0152786627980386,0.0361053928098151));
#44080=CARTESIAN_POINT('',(0.011847441887544,0.0152194627746643,0.0361296548029672));
#44081=CARTESIAN_POINT('',(0.0118100144218005,0.0151679553925195,0.0362172168520969));
#44082=CARTESIAN_POINT('',(0.0118115059446032,0.0151667930370143,0.0362955328114932));
#44083=CARTESIAN_POINT('',(0.0126350496435506,0.0146717197127624,0.0360823098046397));
#44084=CARTESIAN_POINT('',(0.0125867368716098,0.0146147506638112,0.0361064821793622));
#44085=CARTESIAN_POINT('',(0.0125466876309365,0.0145650265432641,0.0361941461617745));
#44086=CARTESIAN_POINT('',(0.0125481200948318,0.0145637940948934,0.0362725457412689));
#44087=CARTESIAN_POINT('',(0.0140340189138294,0.0133400741878172,0.0360349618928478));
#44088=CARTESIAN_POINT('',(0.0139802254604343,0.0132881392002742,0.0360590753278414));
#44089=CARTESIAN_POINT('',(0.0139353786065701,0.0132425296678159,0.036146804178451));
#44090=CARTESIAN_POINT('',(0.0139367178904866,0.0132411219612905,0.0362252568760622));
#44091=CARTESIAN_POINT('',(0.0146866155034336,0.0126151004153065,0.0360103473893038));
#44092=CARTESIAN_POINT('',(0.0146304266947731,0.0125664053612895,0.0360352070928211));
#44093=CARTESIAN_POINT('',(0.0145834087095037,0.0125248397387306,0.0361224688604089));
#44094=CARTESIAN_POINT('',(0.0145837132301085,0.012524467394925,0.0362005916858531));
#44095=CARTESIAN_POINT('',(0.0152851838289805,0.0118641087528759,0.0360041770055195));
#44096=CARTESIAN_POINT('',(0.0152229754605671,0.011815747174396,0.0360248428028356));
#44097=CARTESIAN_POINT('',(0.0151674788425261,0.0117723228643604,0.0361162090430061));
#44098=CARTESIAN_POINT('',(0.0151676306139985,0.0117721273165599,0.0361976690778631));
#44099=CARTESIAN_POINT('',(0.0143467680811991,0.0129670203653367,0.0450227433592973));
#44100=CARTESIAN_POINT('',(0.0156080128040208,0.0115714355419396,0.0449758659317047));
#44101=CARTESIAN_POINT('',(0.0172066386543741,0.00917185028715237,0.0449045572620493));
#44102=CARTESIAN_POINT('',(0.0185655005786739,0.00565703064731983,0.0448135755705688));
#44103=CARTESIAN_POINT('',(0.0191945950678217,0.00286361278847597,0.0447419841407263));
#44104=CARTESIAN_POINT('',(0.0194071949470191,6.00777136899667E-5,0.044672388798418));
#44105=CARTESIAN_POINT('',(0.0192041015517058,-0.0028054344836469,0.0446027222502955));
#44106=CARTESIAN_POINT('',(0.0185964962403323,-0.0055510102664849,0.0445333817125042));
#44107=CARTESIAN_POINT('',(0.0172386864719429,-0.00911657052892957,0.0444379929122851));
#44108=CARTESIAN_POINT('',(0.0151500718616308,-0.0122793685668817,0.0443473875819632));
#44109=CARTESIAN_POINT('',(0.0124063985660361,-0.0149232657153125,0.0442521229497016));
#44110=CARTESIAN_POINT('',(0.010117578367962,-0.0165615924118944,0.0441828847762095));
#44111=CARTESIAN_POINT('',(0.00756285891478142,-0.0178737072130057,0.0441133626517729));
#44112=CARTESIAN_POINT('',(0.00490243177550567,-0.0187778915477432,0.0440434614272629));
#44113=CARTESIAN_POINT('',(0.0020822622425663,-0.0192952805907951,0.0439720759472064));
#44114=CARTESIAN_POINT('',(-0.00167918760469326,-0.0194268328273352,0.0438807494904873));
#44115=CARTESIAN_POINT('',(-0.00545523429515539,-0.0187196130472065,0.0437856215390418));
#44116=CARTESIAN_POINT('',(-0.00891300648284402,-0.0172399362322272,0.0436934413975258));
#44117=CARTESIAN_POINT('',(-0.0113573504197405,-0.0157376069342165,0.04362384288412));
#44118=CARTESIAN_POINT('',(-0.0135102835960664,-0.0139325421260677,0.0435535746462952));
#44119=CARTESIAN_POINT('',(-0.0154180093269257,-0.0117870438403986,0.0434824863656544));
#44120=CARTESIAN_POINT('',(-0.0169618356024676,-0.00943085053462302,0.0434142434361397));
#44121=CARTESIAN_POINT('',(-0.018561552248414,-0.00597807502936931,0.043319871863772));
#44122=CARTESIAN_POINT('',(-0.0193687071465493,-0.00227159356300758,0.0432271688042743));
#44123=CARTESIAN_POINT('',(-0.0193459881530204,0.00154443687141394,0.043134160214351));
#44124=CARTESIAN_POINT('',(-0.0189197212929505,0.0043234240436967,0.0430637334209306));
#44125=CARTESIAN_POINT('',(-0.018074362755791,0.00706858698254036,0.0429930115786603));
#44126=CARTESIAN_POINT('',(-0.0168625782586977,0.00960726235925872,0.0429248070362474));
#44127=CARTESIAN_POINT('',(-0.015268013302165,0.0119817090270433,0.0428536025858245));
#44128=CARTESIAN_POINT('',(-0.013360235232493,0.0140750748851165,0.0427834074356023));
#44129=CARTESIAN_POINT('',(-0.0111697667217031,0.0158720510310536,0.0427147000605931));
#44130=CARTESIAN_POINT('',(-0.00871620076132663,0.0173399062434923,0.0426443517707747));
#44131=CARTESIAN_POINT('',(-0.00611636466270319,0.0184183849806335,0.0425739346463595));
#44132=CARTESIAN_POINT('',(-0.0033321215578175,0.0191193135415984,0.042503638306099));
#44133=CARTESIAN_POINT('',(-0.000534719349594548,0.0194001567923326,0.0424352481242054));
#44134=CARTESIAN_POINT('',(0.00327849885131586,0.0192236784280454,0.0423397283567898));
#44135=CARTESIAN_POINT('',(0.00693693435561955,0.0182248427665248,0.0422486928840703));
#44136=CARTESIAN_POINT('',(0.0103015416551695,0.0164475884952921,0.0421545163322705));
#44137=CARTESIAN_POINT('',(0.0125743260223434,0.0147828414026713,0.0420842344442644));
#44138=CARTESIAN_POINT('',(0.0146175543522543,0.0127663093377594,0.0420143045368343));
#44139=CARTESIAN_POINT('',(0.0163078319804017,0.0105219606378753,0.0419455699872781));
#44140=CARTESIAN_POINT('',(0.0176804778117793,0.00800303522391728,0.0418737798000558));
#44141=CARTESIAN_POINT('',(0.0189788691155733,0.00447263254597852,0.0417818750029852));
#44142=CARTESIAN_POINT('',(0.0194877865696638,0.000664950319516681,0.0416882131489404));
#44143=CARTESIAN_POINT('',(0.0191606344240293,-0.00308452734371485,0.0415945646754112));
#44144=CARTESIAN_POINT('',(0.0184972150414569,-0.00587405614797688,0.0415249961850151));
#44145=CARTESIAN_POINT('',(0.0174551688991988,-0.00848356918159712,0.0414557067014046));
#44146=CARTESIAN_POINT('',(0.0160118984407478,-0.0109666655171155,0.0413840608453789));
#44147=CARTESIAN_POINT('',(0.0142568879553151,-0.0131671967630898,0.0413154608515628));
#44148=CARTESIAN_POINT('',(0.0114739992840907,-0.0157687954816694,0.0412225537492099));
#44149=CARTESIAN_POINT('',(0.00820510218136591,-0.0176905682270122,0.041127987405849));
#44150=CARTESIAN_POINT('',(0.00457500630677842,-0.0188604491142679,0.0410356755215267));
#44151=CARTESIAN_POINT('',(0.00180103482447101,-0.0193238643528813,0.0409657832532925));
#44152=CARTESIAN_POINT('',(-0.00107107012237494,-0.0193776995117875,0.0408944417055149));
#44153=CARTESIAN_POINT('',(-0.00385957609717241,-0.0190194680803449,0.0408261940093936));
#44154=CARTESIAN_POINT('',(-0.00661674975701956,-0.0182460217520095,0.0407559615376911));
#44155=CARTESIAN_POINT('',(-0.00919615117806423,-0.0170879464996363,0.0406851519599111));
#44156=CARTESIAN_POINT('',(-0.0115757360312258,-0.0155783764814346,0.0406160327672618));
#44157=CARTESIAN_POINT('',(-0.0144816228512718,-0.0130632680781061,0.0405226059839666));
#44158=CARTESIAN_POINT('',(-0.0167255080784181,-0.0100258204989716,0.0404284451556143));
#44159=CARTESIAN_POINT('',(-0.018273821340579,-0.00653624939613813,0.0403361064322415));
#44160=CARTESIAN_POINT('',(-0.0190266203226373,-0.00382735491088818,0.0402665472857832));
#44161=CARTESIAN_POINT('',(-0.0193826548713618,-0.000976776954179603,0.040194831061496));
#44162=CARTESIAN_POINT('',(-0.0193202269220419,0.00183427021572927,0.0401262202187513));
#44163=CARTESIAN_POINT('',(-0.0188410320331117,0.00465684276915032,0.04005635983472));
#44164=CARTESIAN_POINT('',(-0.0176721712985505,0.00824010010470064,0.0399619467409778));
#44165=CARTESIAN_POINT('',(-0.0157139906954545,0.0115444562535526,0.0398700712706307));
#44166=CARTESIAN_POINT('',(-0.0131404121963109,0.0142825387260622,0.0397766036249347));
#44167=CARTESIAN_POINT('',(-0.0108892506373088,0.0160641909999058,0.0397052086483859));
#44168=CARTESIAN_POINT('',(-0.00845490209584555,0.0174688971648347,0.0396369495862849));
#44169=CARTESIAN_POINT('',(-0.0057901959548591,0.0185240850474543,0.039566438989386));
#44170=CARTESIAN_POINT('',(-0.00304034502797974,0.0191668077438134,0.0394959407562146));
#44171=CARTESIAN_POINT('',(-0.000205901340496404,0.0194070054520654,0.0394264264215391));
#44172=CARTESIAN_POINT('',(0.00263699327955384,0.0192272254647594,0.0393571893618666));
#44173=CARTESIAN_POINT('',(0.00539600038814193,0.0186426594092554,0.0392866544513076));
#44174=CARTESIAN_POINT('',(0.00808505590971417,0.0176426432032035,0.0392157074108896));
#44175=CARTESIAN_POINT('',(0.0105483699747408,0.0162909067686871,0.0391476200440295));
#44176=CARTESIAN_POINT('',(0.0128356568770419,0.0145569551839711,0.0390764682392641));
#44177=CARTESIAN_POINT('',(0.0154667936342723,0.0118723552378021,0.0389830095045639));
#44178=CARTESIAN_POINT('',(0.0174959375379232,0.00861028352118488,0.0388910983122013));
#44179=CARTESIAN_POINT('',(0.018737560948652,0.00505469577241424,0.0387967510809749));
#44180=CARTESIAN_POINT('',(0.0192773093553197,0.00224064998029077,0.0387263243880055));
#44181=CARTESIAN_POINT('',(0.0193996109462872,-0.000567772972921872,0.038658090573959));
#44182=CARTESIAN_POINT('',(0.019103237189323,-0.00342339164913732,0.0385865907481668));
#44183=CARTESIAN_POINT('',(0.018406524551842,-0.0061503438852885,0.038516874656554));
#44184=CARTESIAN_POINT('',(0.0169361589213083,-0.00966858061701975,0.038424581031263));
#44185=CARTESIAN_POINT('',(0.0147454945400407,-0.0127612251195262,0.038330334371663));
#44186=CARTESIAN_POINT('',(0.0119167773275786,-0.0153174725086515,0.0382369783791112));
#44187=CARTESIAN_POINT('',(0.00957733860555868,-0.0168803266372561,0.0381685058222812));
#44188=CARTESIAN_POINT('',(0.00698077170066027,-0.0181084047715643,0.0380966845785145));
#44189=CARTESIAN_POINT('',(0.0042918767418205,-0.0189264882216141,0.0380274832798624));
#44190=CARTESIAN_POINT('',(0.00145824599298628,-0.0193532361924154,0.0379581524639087));
#44191=CARTESIAN_POINT('',(-0.00230745717185322,-0.0193620370982988,0.0378643768735323));
#44192=CARTESIAN_POINT('',(-0.00605875712442595,-0.0185332614335168,0.037770630359556));
#44193=CARTESIAN_POINT('',(-0.00946539676442699,-0.0169433041032279,0.0376786997789487));
#44194=CARTESIAN_POINT('',(-0.0118601315399094,-0.0153614098090379,0.0376069200646522));
#44195=CARTESIAN_POINT('',(-0.0139539673129934,-0.0134878988356932,0.0375381410572525));
#44196=CARTESIAN_POINT('',(-0.0157915027794027,-0.0112835406068729,0.0374685270222508));
#44197=CARTESIAN_POINT('',(-0.0172579230800856,-0.00887577363203918,0.0373980765841363));
#44198=CARTESIAN_POINT('',(-0.0183727133494431,-0.00625378905721084,0.0373274841689959));
#44199=CARTESIAN_POINT('',(-0.0190884840066312,-0.00350098448769894,0.0372584724349144));
#44200=CARTESIAN_POINT('',(-0.0193957163038253,-0.000694067135523436,0.0371887234296306));
#44201=CARTESIAN_POINT('',(-0.0192850410734145,0.00217035261908061,0.0371172799265481));
#44202=CARTESIAN_POINT('',(-0.0187701121534513,0.00493301967824674,0.0370488310019022));
#44203=CARTESIAN_POINT('',(-0.0178372483489486,0.00764932587964424,0.0369788065708886));
#44204=CARTESIAN_POINT('',(-0.0165419620384625,0.010147864520342,0.0369082891947026));
#44205=CARTESIAN_POINT('',(-0.0148734158890986,0.0124680415791245,0.036837870820931));
#44206=CARTESIAN_POINT('',(-0.0128973916193517,0.0145010968396696,0.0367691497387133));
#44207=CARTESIAN_POINT('',(-0.0106519271325968,0.0162238286040827,0.0366987385269726));
#44208=CARTESIAN_POINT('',(-0.00814949887436442,0.0176125565764292,0.0366277713925307));
#44209=CARTESIAN_POINT('',(-0.00551879983682063,0.0186067070341556,0.0365595624449246));
#44210=CARTESIAN_POINT('',(-0.00271205952795247,0.0192174753444305,0.0364889202888244));
#44211=CARTESIAN_POINT('',(9.33714311773742E-5,0.0194065080580889,0.0364185370033719));
#44212=CARTESIAN_POINT('',(0.00389771074671841,0.0191082063674791,0.03632547293438));
#44213=CARTESIAN_POINT('',(0.00752080983387477,0.0179919526508517,0.0362324801372786));
#44214=CARTESIAN_POINT('',(0.0108287899040495,0.0161047355207281,0.0361378634417124));
#44215=CARTESIAN_POINT('',(0.0123060494137679,0.0149474122876113,0.0360927078861263));
#44216=CARTESIAN_POINT('',(0.0130058841653258,0.0143115250488958,0.036069621110675));
#44217=CARTESIAN_POINT('',(0.0133472924810068,0.013834004568283,0.0361523595743667));
#44218=CARTESIAN_POINT('',(0.0133936849724094,0.0137807465598252,0.0361621806530942));
#44219=CARTESIAN_POINT('',(0.0134819277095383,0.0136809336166974,0.0361806693828696));
#44220=CARTESIAN_POINT('',(0.0136838792255527,0.0134680380101868,0.036221212408854));
#44221=CARTESIAN_POINT('',(0.0137247775534597,0.0134264423745443,0.0362290943081679));
#44222=CARTESIAN_POINT('',(0.0137371265537183,0.013413795666025,0.0362315327602123));
#44223=CARTESIAN_POINT('',(-0.0192,0.,0.0373616076561507));
#44224=CARTESIAN_POINT('',(-0.0192,0.000371890410119982,0.0373522525296843));
#44225=CARTESIAN_POINT('',(-0.0191785530500175,0.00116597240745298,0.0373323651099912));
#44226=CARTESIAN_POINT('',(-0.0190533790090975,0.00250459018190321,0.0372989507415849));
#44227=CARTESIAN_POINT('',(-0.0188473405126322,0.00373007741948374,0.0372682487486553));
#44228=CARTESIAN_POINT('',(-0.0186320455861301,0.00464879561353362,0.03724500860155));
#44229=CARTESIAN_POINT('',(-0.0184910260779751,0.00517577049788258,0.0372315910441466));
#44230=CARTESIAN_POINT('',(-0.0183631738799605,0.00561124864393773,0.0372204437696751));
#44231=CARTESIAN_POINT('',(-0.0182640831751387,0.00592442485168977,0.0372123708776225));
#44232=CARTESIAN_POINT('',(-0.0181114229288877,0.00638129356744456,0.0372005013632639));
#44233=CARTESIAN_POINT('',(-0.0178282980344812,0.00715369007655939,0.0371801655718353));
#44234=CARTESIAN_POINT('',(-0.0174532063649077,0.00802611439628738,0.0371565444398454));
#44235=CARTESIAN_POINT('',(-0.0170319137943417,0.00887256924934606,0.0371328574091274));
#44236=CARTESIAN_POINT('',(-0.0166916512615943,0.00949703934327355,0.0371149616027724));
#44237=CARTESIAN_POINT('',(-0.0163920316200393,0.0100022368165151,0.0371001174124457));
#44238=CARTESIAN_POINT('',(-0.0161668301297771,0.0103582788158399,0.037089432092816));
#44239=CARTESIAN_POINT('',(-0.0160442954394929,0.0105467961338315,0.0370837216066706));
#44240=CARTESIAN_POINT('',(-0.0159259339101793,0.0107243466139525,0.0370782923415417));
#44241=CARTESIAN_POINT('',(-0.015902121562517,0.0107593087439536,0.0370772214540573));
#44242=CARTESIAN_POINT('',(-0.0158246774181559,0.0108733496105961,0.0370737446787212));
#44243=CARTESIAN_POINT('',(-0.0156785114667725,0.0110844976801846,0.0370673156842167));
#44244=CARTESIAN_POINT('',(-0.0153807730333783,0.0114997536190571,0.0370546167892147));
#44245=CARTESIAN_POINT('',(-0.014962269035776,0.0120387684412869,0.0370377633163098));
#44246=CARTESIAN_POINT('',(-0.0145507291330991,0.0125303807447499,0.0370219676193401));
#44247=CARTESIAN_POINT('',(-0.0140566959530989,0.0130876736332664,0.0370036516599521));
#44248=CARTESIAN_POINT('',(-0.0134911078549613,0.0136706063886826,0.036983680328007));
#44249=CARTESIAN_POINT('',(-0.0130066880814553,0.0141265515432096,0.036967283585551));
#44250=CARTESIAN_POINT('',(-0.0126777438236585,0.0144203680610192,0.0369563905284894));
#44251=CARTESIAN_POINT('',(-0.0124597249647613,0.0146087978374249,0.0369492596498424));
#44252=CARTESIAN_POINT('',(-0.0123099397336204,0.0147348872989819,0.0369444033292919));
#44253=CARTESIAN_POINT('',(-0.0121944734692698,0.0148302309493534,0.0369406777873217));
#44254=CARTESIAN_POINT('',(-0.0121492528362333,0.0148675088863959,0.0369392176100781));
#44255=CARTESIAN_POINT('',(-0.0119863805608889,0.0149993545089899,0.036933984538422));
#44256=CARTESIAN_POINT('',(-0.0118085399796179,0.015139992071706,0.0369283182662103));
#44257=CARTESIAN_POINT('',(-0.0114746059451049,0.0153972690138823,0.0369177724023816));
#44258=CARTESIAN_POINT('',(-0.0109992219992465,0.0157425412407583,0.036903044451745));
#44259=CARTESIAN_POINT('',(-0.0105013973511648,0.0160764140150835,0.0368879731719335));
#44260=CARTESIAN_POINT('',(-0.0101104080215209,0.0163238952481856,0.0368763158121412));
#44261=CARTESIAN_POINT('',(-0.00977639198801372,0.0165255784868323,0.0368664640946302));
#44262=CARTESIAN_POINT('',(-0.00958104132157012,0.0166391770763527,0.036860770200424));
#44263=CARTESIAN_POINT('',(-0.00923219712027506,0.0168370294522573,0.0368507156214954));
#44264=CARTESIAN_POINT('',(-0.00856053323848537,0.0171961213283961,0.0368317271371337));
#44265=CARTESIAN_POINT('',(-0.00758934787306023,0.0176566860768508,0.0368051955704689));
#44266=CARTESIAN_POINT('',(-0.00636643819771057,0.0181219912186938,0.036772976891564));
#44267=CARTESIAN_POINT('',(-0.0052667098920806,0.0184781293286437,0.0367444452964538));
#44268=CARTESIAN_POINT('',(-0.00400582762844146,0.0187957254590059,0.0367122907087581));
#44269=CARTESIAN_POINT('',(-0.00294566296814909,0.0189789958608912,0.0366855418485812));
#44270=CARTESIAN_POINT('',(-0.00232318507258854,0.0190604019775968,0.0366698466292546));
#44271=CARTESIAN_POINT('',(-0.00198376779530057,0.0190975924642744,0.0366612799344118));
#44272=CARTESIAN_POINT('',(-0.00179049704812089,0.0191170012041065,0.0366563916149323));
#44273=CARTESIAN_POINT('',(-0.00144107189914202,0.0191469089045128,0.0366475609085875));
#44274=CARTESIAN_POINT('',(-0.00102086988890093,0.0191748137169543,0.0366369845716538));
#44275=CARTESIAN_POINT('',(-0.000242744702888557,0.0192077009052938,0.0366174751610461));
#44276=CARTESIAN_POINT('',(0.000903540972486138,0.0191964529250526,0.0365889325725422));
#44277=CARTESIAN_POINT('',(0.00236686630270527,0.0190724376044203,0.0365525815476574));
#44278=CARTESIAN_POINT('',(0.00360662279469994,0.0188721503870318,0.0365217257376382));
#44279=CARTESIAN_POINT('',(0.00469151749077868,0.0186237860444726,0.0364943675307728));
#44280=CARTESIAN_POINT('',(0.00540082376038474,0.0184290014337655,0.0364761561957));
#44281=CARTESIAN_POINT('',(0.00593364138090763,0.0182624425984035,0.036462249397394));
#44282=CARTESIAN_POINT('',(0.00633445502197581,0.0181256641700199,0.0364516317998972));
#44283=CARTESIAN_POINT('',(0.00658566662395393,0.0180361904684984,0.0364449143813257));
#44284=CARTESIAN_POINT('',(0.00694154913776284,0.0179025878526453,0.0364353138516747));
#44285=CARTESIAN_POINT('',(0.00737542446485554,0.0177295306256606,0.0364235218690459));
#44286=CARTESIAN_POINT('',(0.00792504129770683,0.0174929818445577,0.0364084143183134));
#44287=CARTESIAN_POINT('',(0.00845826749280384,0.017239460962699,0.0363935064609552));
#44288=CARTESIAN_POINT('',(0.00883222304449844,0.0170485828373795,0.0363829021210688));
#44289=CARTESIAN_POINT('',(0.00903653051859202,0.0169408952112956,0.0363770691222274));
#44290=CARTESIAN_POINT('',(0.00921086669198421,0.0168465991202952,0.0363720612873765));
#44291=CARTESIAN_POINT('',(0.00930080306136933,0.0167969846854805,0.0363694715142351));
#44292=CARTESIAN_POINT('',(0.00946017099694578,0.0167081137134898,0.0363648869257377));
#44293=CARTESIAN_POINT('',(0.00974470880582175,0.0165452759759724,0.0363566902289924));
#44294=CARTESIAN_POINT('',(0.010216916845427,0.0162610675113002,0.0363430146333954));
#44295=CARTESIAN_POINT('',(0.0108590295515736,0.0158416026951709,0.0363241211007571));
#44296=CARTESIAN_POINT('',(0.0115972342310281,0.0153116725285745,0.0363018822071081));
#44297=CARTESIAN_POINT('',(0.0123260419243019,0.0147294470622927,0.0362790852966174));
#44298=CARTESIAN_POINT('',(0.0130972614005013,0.0140534113101744,0.0362539467117431));
#44299=CARTESIAN_POINT('',(0.0135202801000095,0.0136359227301335,0.0362393193646486));
#44300=CARTESIAN_POINT('',(0.0137371532346411,0.0134138220134304,0.0362316338257453));
#44301=CARTESIAN_POINT('',(-0.0192,2.09607971128427E-14,0.0373616076561507));
#44302=CARTESIAN_POINT('',(0.0192,6.20369116582113E-17,0.0388620248355153));
#44303=CARTESIAN_POINT('',(0.0192,-0.000124988712080034,0.0388589418972036));
#44304=CARTESIAN_POINT('',(0.019197908568983,-0.000469951366362968,0.0388503776671778));
#44305=CARTESIAN_POINT('',(0.0191708854160062,-0.00113849276069121,0.0388336681086579));
#44306=CARTESIAN_POINT('',(0.0191167543307171,-0.00181358675664011,0.0388167129967166));
#44307=CARTESIAN_POINT('',(0.019053823567411,-0.00239064344730558,0.0388021651865298));
#44308=CARTESIAN_POINT('',(0.0189785332376671,-0.00292447550362445,0.0387886436902797));
#44309=CARTESIAN_POINT('',(0.0189087227591735,-0.0033350115235191,0.0387781924280792));
#44310=CARTESIAN_POINT('',(0.0188663906766718,-0.00356565828611578,0.0387723058742901));
#44311=CARTESIAN_POINT('',(0.018825097103103,-0.00377681105440297,0.0387669036693559));
#44312=CARTESIAN_POINT('',(0.0188077282469835,-0.00386153097423765,0.0387647329733464));
#44313=CARTESIAN_POINT('',(0.0187750316529949,-0.00401877614816724,0.0387607045053975));
#44314=CARTESIAN_POINT('',(0.0187193199572928,-0.00427374897108696,0.0387541660083545));
#44315=CARTESIAN_POINT('',(0.0186304266466907,-0.00464970563988405,0.0387445081722731));
#44316=CARTESIAN_POINT('',(0.0185129476878379,-0.00509733713455083,0.0387329720111096));
#44317=CARTESIAN_POINT('',(0.0183398599789788,-0.00569735566998535,0.0387174493033485));
#44318=CARTESIAN_POINT('',(0.0180945951276823,-0.00644494954433084,0.0386979707530031));
#44319=CARTESIAN_POINT('',(0.0177437299560687,-0.00735566619832176,0.038673968118737));
#44320=CARTESIAN_POINT('',(0.0173645091276954,-0.0082100275935466,0.0386509980338975));
#44321=CARTESIAN_POINT('',(0.0169395232115261,-0.00905492681459564,0.0386276443282059));
#44322=CARTESIAN_POINT('',(0.0164747060732539,-0.00987520965215876,0.0386042864124672));
#44323=CARTESIAN_POINT('',(0.0159698691930589,-0.0106724061933238,0.0385808228137399));
#44324=CARTESIAN_POINT('',(0.015426561638605,-0.0114436727128365,0.0385572800129853));
#44325=CARTESIAN_POINT('',(0.0149428266243687,-0.0120633797631095,0.0385375913015805));
#44326=CARTESIAN_POINT('',(0.01453781514937,-0.0125445541649258,0.0385217941673181));
#44327=CARTESIAN_POINT('',(0.0142776465840892,-0.0128387126614965,0.0385119130566294));
#44328=CARTESIAN_POINT('',(0.0140645984954196,-0.013070769057157,0.0385039754056187));
#44329=CARTESIAN_POINT('',(0.0139043962979387,-0.0132411426968139,0.0384980777448022));
#44330=CARTESIAN_POINT('',(0.013763723147588,-0.0133868564728369,0.0384929650586733));
#44331=CARTESIAN_POINT('',(0.013662313595645,-0.0134903048716543,0.0384893064291248));
#44332=CARTESIAN_POINT('',(0.0135525008274683,-0.013600476147292,0.0384853748174183));
#44333=CARTESIAN_POINT('',(0.0135690565436169,-0.0135838157902813,0.0384859700957141));
#44334=CARTESIAN_POINT('',(0.0135391866005673,-0.0136136572054972,0.0384849120327072));
#44335=CARTESIAN_POINT('',(0.0134917789484498,-0.0136607045306038,0.0384832550069352));
#44336=CARTESIAN_POINT('',(0.0133655542699404,-0.0137849389174932,0.0384788679632096));
#44337=CARTESIAN_POINT('',(0.0131407368446433,-0.0140001630606948,0.038471180294041));
#44338=CARTESIAN_POINT('',(0.0128329907468812,-0.0142838284621455,0.0384608522080179));
#44339=CARTESIAN_POINT('',(0.0124394944651753,-0.014629051704642,0.0384479439399829));
#44340=CARTESIAN_POINT('',(0.0120350384336053,-0.0149629409663656,0.0384350171155988));
#44341=CARTESIAN_POINT('',(0.0116630824288502,-0.0152531313620447,0.0384233910564852));
#44342=CARTESIAN_POINT('',(0.0113578002512048,-0.0154819406315971,0.038413990371784));
#44343=CARTESIAN_POINT('',(0.0110852017754261,-0.0156778700166862,0.0384057194634792));
#44344=CARTESIAN_POINT('',(0.0108757691840278,-0.0158229190119628,0.0383994431066811));
#44345=CARTESIAN_POINT('',(0.0107633978180121,-0.0158995337565912,0.0383960924847546));
#44346=CARTESIAN_POINT('',(0.010647220670249,-0.0159774670540609,0.0383926461721934));
#44347=CARTESIAN_POINT('',(0.010644680199581,-0.015979057777509,0.0383925721061032));
#44348=CARTESIAN_POINT('',(0.0106004017580862,-0.0160085336640853,0.0383912603424084));
#44349=CARTESIAN_POINT('',(0.0105388855056911,-0.0160491332519111,0.0383894399309875));
#44350=CARTESIAN_POINT('',(0.0104337580683584,-0.0161178495328419,0.0383863325780379));
#44351=CARTESIAN_POINT('',(0.0102995596447433,-0.0162039569082081,0.0383823779216498));
#44352=CARTESIAN_POINT('',(0.0101026409934458,-0.0163279400315075,0.0383765955804146));
#44353=CARTESIAN_POINT('',(0.00982569348738544,-0.0164971000054074,0.0383685125932213));
#44354=CARTESIAN_POINT('',(0.00931229706094346,-0.0167953943362142,0.0383536861129244));
#44355=CARTESIAN_POINT('',(0.00869623024698729,-0.0171259186584117,0.0383361879893404));
#44356=CARTESIAN_POINT('',(0.00804598232123238,-0.0174348214410755,0.0383181275958529));
#44357=CARTESIAN_POINT('',(0.00766192783303044,-0.0176062593109793,0.0383075679160363));
#44358=CARTESIAN_POINT('',(0.00731139699448762,-0.0177542581748895,0.0382980077197107));
#44359=CARTESIAN_POINT('',(0.00712765573843583,-0.0178283104509261,0.0382930327414598));
#44360=CARTESIAN_POINT('',(0.00682289565956123,-0.0179482076378896,0.0382848198753714));
#44361=CARTESIAN_POINT('',(0.00645992069858502,-0.0180825892927988,0.0382751348480656));
#44362=CARTESIAN_POINT('',(0.00601258557271775,-0.0182363346904473,0.0382633299572721));
#44363=CARTESIAN_POINT('',(0.00556480119192505,-0.0183778750104654,0.0382516426298377));
#44364=CARTESIAN_POINT('',(0.00511355445316589,-0.0185084972990694,0.038239983726734));
#44365=CARTESIAN_POINT('',(0.00466130310345707,-0.0186275784942477,0.0382284093826885));
#44366=CARTESIAN_POINT('',(0.00427933841460029,-0.0187180967791853,0.0382187217286313));
#44367=CARTESIAN_POINT('',(0.00401789245348191,-0.0187752281188422,0.0382121305187804));
#44368=CARTESIAN_POINT('',(0.00385789607829158,-0.0188084863297999,0.0382081100715769));
#44369=CARTESIAN_POINT('',(0.00376711328860128,-0.018827031731736,0.0382058321410011));
#44370=CARTESIAN_POINT('',(0.00356421552584282,-0.0188666354876692,0.0382007513506392));
#44371=CARTESIAN_POINT('',(0.00333905036475743,-0.0189079866307164,0.0381951232778063));
#44372=CARTESIAN_POINT('',(0.00293936341804117,-0.0189761002733566,0.0381851532080257));
#44373=CARTESIAN_POINT('',(0.00241653091500352,-0.0190504529133085,0.0381721596825934));
#44374=CARTESIAN_POINT('',(0.00184779993776262,-0.0191134168112792,0.0381580649595237));
#44375=CARTESIAN_POINT('',(0.00134438187706576,-0.0191548105265659,0.0381456055678352));
#44376=CARTESIAN_POINT('',(0.000905072994749517,-0.0191800757495629,0.038134731794586));
#44377=CARTESIAN_POINT('',(0.000532799307105026,-0.0191936389183209,0.0381255046676114));
#44378=CARTESIAN_POINT('',(0.00027220902580008,-0.0191983861193444,0.0381190256016955));
#44379=CARTESIAN_POINT('',(0.000128419938523944,-0.0191996842940641,0.0381154391115202));
#44380=CARTESIAN_POINT('',(3.90987858716185E-5,-0.0191999474181661,0.0381132046010067));
#44381=CARTESIAN_POINT('',(1.95431978264071E-5,-0.0192001150269539,0.0381127151714058));
#44382=CARTESIAN_POINT('',(-0.000161500855682608,-0.0191995839834403,0.0381081740006597));
#44383=CARTESIAN_POINT('',(-0.000344994553467409,-0.0191972462183798,0.038103572552286));
#44384=CARTESIAN_POINT('',(-0.000689203714121839,-0.019189417004198,0.0380949412020279));
#44385=CARTESIAN_POINT('',(-0.00115754456909656,-0.0191677379106035,0.0380831957121736));
#44386=CARTESIAN_POINT('',(-0.00170968846669982,-0.0191263395125739,0.0380693347309524));
#44387=CARTESIAN_POINT('',(-0.00242229227603454,-0.0190523549997508,0.0380514148760769));
#44388=CARTESIAN_POINT('',(-0.00327277835673546,-0.0189278245373745,0.0380299489735858));
#44389=CARTESIAN_POINT('',(-0.00454268577104214,-0.0186737472496771,0.0379976696929144));
#44390=CARTESIAN_POINT('',(-0.00568050934246028,-0.0183541258273889,0.0379683371672561));
#44391=CARTESIAN_POINT('',(-0.0066719009761423,-0.0180092154984539,0.0379423639538944));
#44392=CARTESIAN_POINT('',(-0.00726202656726792,-0.0177759556110926,0.0379267344521425));
#44393=CARTESIAN_POINT('',(-0.00764324733329641,-0.0176141181512875,0.037916525073436));
#44394=CARTESIAN_POINT('',(-0.00809920545239486,-0.0174115610264153,0.0379041591448252));
#44395=CARTESIAN_POINT('',(-0.00874479716386492,-0.0171013740913796,0.0378863251899204));
#44396=CARTESIAN_POINT('',(-0.00949423536320096,-0.0166957978671014,0.0378650102089074));
#44397=CARTESIAN_POINT('',(-0.0100722264432436,-0.016347902852265,0.0378480854348865));
#44398=CARTESIAN_POINT('',(-0.0104051711420505,-0.0161371977584436,0.037838189497368));
#44399=CARTESIAN_POINT('',(-0.0106884929050717,-0.0159506554757344,0.0378296616784728));
#44400=CARTESIAN_POINT('',(-0.0108714091101842,-0.0158261890624888,0.0378241013526368));
#44401=CARTESIAN_POINT('',(-0.0111453733805073,-0.015635575467968,0.0378157253933416));
#44402=CARTESIAN_POINT('',(-0.0115986568668551,-0.0153064203204682,0.0378016947061641));
#44403=CARTESIAN_POINT('',(-0.0120998520795891,-0.0149133113635874,0.0377858059068655));
#44404=CARTESIAN_POINT('',(-0.0125756135298173,-0.014510852707208,0.0377703222271541));
#44405=CARTESIAN_POINT('',(-0.0129200908078643,-0.0142050469318278,0.0377589086192492));
#44406=CARTESIAN_POINT('',(-0.0132006411545733,-0.0139434429700079,0.0377494317412391));
#44407=CARTESIAN_POINT('',(-0.0133857111418757,-0.013765000810918,0.0377430936558732));
#44408=CARTESIAN_POINT('',(-0.0134998711245461,-0.0136526570365928,0.0377391496876206));
#44409=CARTESIAN_POINT('',(-0.0135570653366891,-0.0135961534484681,0.0377371713818215));
#44410=CARTESIAN_POINT('',(-0.0137194782686012,-0.0134325193052724,0.0377315005296542));
#44411=CARTESIAN_POINT('',(-0.013890846647042,-0.0132555097358427,0.0377254395139226));
#44412=CARTESIAN_POINT('',(-0.0141914410618802,-0.0129364066458154,0.0377146534601655));
#44413=CARTESIAN_POINT('',(-0.0145641887987515,-0.012516248297343,0.037700830463428));
#44414=CARTESIAN_POINT('',(-0.0149458174721339,-0.0120567748443482,0.0376861206343685));
#44415=CARTESIAN_POINT('',(-0.0152621379397411,-0.0116525098886725,0.0376734681880677));
#44416=CARTESIAN_POINT('',(-0.015519755577611,-0.0113060729252389,0.0376628139369461));
#44417=CARTESIAN_POINT('',(-0.0157216407675846,-0.0110227938931655,0.0376542150155887));
#44418=CARTESIAN_POINT('',(-0.0158495685055665,-0.0108369321344913,0.0376486208969609));
#44419=CARTESIAN_POINT('',(-0.0159131669067378,-0.0107430778913541,0.0376458014971848));
#44420=CARTESIAN_POINT('',(-0.0159509485593324,-0.0106867591251374,0.0376441090112356));
#44421=CARTESIAN_POINT('',(-0.0159555729316056,-0.0106800156854144,0.0376439054569211));
#44422=CARTESIAN_POINT('',(-0.0160366912572767,-0.0105579889100657,0.0376402359555261));
#44423=CARTESIAN_POINT('',(-0.0161171589222373,-0.0104348325909768,0.0376365510641637));
#44424=CARTESIAN_POINT('',(-0.016268398071352,-0.0101992684367464,0.037629536890784));
#44425=CARTESIAN_POINT('',(-0.0164718347676829,-0.00986866479784329,0.0376198039485842));
#44426=CARTESIAN_POINT('',(-0.0167088982025017,-0.00946187138190906,0.037607987549141));
#44427=CARTESIAN_POINT('',(-0.0169352425124742,-0.00905045159144459,0.0375961914250413));
#44428=CARTESIAN_POINT('',(-0.0171515224314667,-0.00863362799674667,0.0375843835572777));
#44429=CARTESIAN_POINT('',(-0.0173579642690949,-0.00821054566971484,0.0375725348777327));
#44430=CARTESIAN_POINT('',(-0.017519853357746,-0.00785750697306154,0.0375627505445255));
#44431=CARTESIAN_POINT('',(-0.0176315159093588,-0.0076012047946677,0.0375557017408629));
#44432=CARTESIAN_POINT('',(-0.0176894144861573,-0.00746532669201923,0.0375519767883745));
#44433=CARTESIAN_POINT('',(-0.0177451023052229,-0.00733173837843177,0.0375483250161489));
#44434=CARTESIAN_POINT('',(-0.0177507176499454,-0.00731790430173732,0.037547949788258));
#44435=CARTESIAN_POINT('',(-0.0177786056944096,-0.00725011263857024,0.0375461082256053));
#44436=CARTESIAN_POINT('',(-0.0178249505298768,-0.00713585437300043,0.037543024456147));
#44437=CARTESIAN_POINT('',(-0.017911869168981,-0.00691657760835478,0.0375371512036404));
#44438=CARTESIAN_POINT('',(-0.0180372299084404,-0.00658405541648223,0.0375283410975867));
#44439=CARTESIAN_POINT('',(-0.0181819996122516,-0.00617484022070445,0.0375176079482784));
#44440=CARTESIAN_POINT('',(-0.0183404129537489,-0.00568953373275272,0.0375050087314909));
#44441=CARTESIAN_POINT('',(-0.0185070965992825,-0.00512393103192481,0.0374904763843311));
#44442=CARTESIAN_POINT('',(-0.0186457068520012,-0.00459147257359349,0.0374769312162186));
#44443=CARTESIAN_POINT('',(-0.018741723435775,-0.00417253373587205,0.0374663558945341));
#44444=CARTESIAN_POINT('',(-0.0187919046418404,-0.00393965552253266,0.0374604956552035));
#44445=CARTESIAN_POINT('',(-0.0188378277371704,-0.00371279381327267,0.0374548032660863));
#44446=CARTESIAN_POINT('',(-0.0188477741035621,-0.00366081165764643,0.0374535007869088));
#44447=CARTESIAN_POINT('',(-0.0188734250289746,-0.00352750121917844,0.037450156909658));
#44448=CARTESIAN_POINT('',(-0.0189120412610658,-0.00331666349387629,0.0374448677960544));
#44449=CARTESIAN_POINT('',(-0.0189684945740984,-0.00298253617925169,0.0374364833505349));
#44450=CARTESIAN_POINT('',(-0.0190303728155349,-0.0025592179366185,0.037425860538847));
#44451=CARTESIAN_POINT('',(-0.0191047485512526,-0.00195409312532511,0.0374106767231135));
#44452=CARTESIAN_POINT('',(-0.0191765387773259,-0.00112634873242808,0.0373899094755316));
#44453=CARTESIAN_POINT('',(-0.0192,-0.000387773697818323,0.037371362336252));
#44454=CARTESIAN_POINT('',(-0.0192,8.05624845824862E-17,0.0373616076561507));
#44455=CARTESIAN_POINT('',(0.0192,1.96007229986627E-17,0.0388620248355153));
#44456=CARTESIAN_POINT('',(-0.0192,0.,0.0403612589235446));
#44457=CARTESIAN_POINT('',(-0.0192,0.00251327412287183,0.0402987908365434));
#44458=CARTESIAN_POINT('',(-0.0182002919343753,0.00753865073535337,0.040173854662541));
#44459=CARTESIAN_POINT('',(-0.0139299003749868,0.0139299426504137,0.0399864504015373));
#44460=CARTESIAN_POINT('',(-0.00753880775836791,0.0182002798556818,0.0397990461405336));
#44461=CARTESIAN_POINT('',(-3.10273503482896E-17,0.0196998600721591,0.03961164187953));
#44462=CARTESIAN_POINT('',(0.00753880775836785,0.0182002798556819,0.0394242376185263));
#44463=CARTESIAN_POINT('',(0.0139299003749868,0.0139299426504138,0.0392368333575227));
#44464=CARTESIAN_POINT('',(0.0182002919343752,0.00753865073535343,0.039049429096519));
#44465=CARTESIAN_POINT('',(0.0192,0.00251327412287189,0.0389244929225166));
#44466=CARTESIAN_POINT('',(0.0192,6.20369116582113E-17,0.0388620248355153));
#44467=CARTESIAN_POINT('',(-0.0192,-1.4501171666592E-17,0.0403612589235446));
#44468=CARTESIAN_POINT('',(0.0192,-4.02812422912431E-17,0.0418617389925214));
#44469=CARTESIAN_POINT('',(0.0192,-0.000627843242455304,0.0418459149896042));
#44470=CARTESIAN_POINT('',(0.0191537643301771,-0.00156960588184851,0.0418222692764327));
#44471=CARTESIAN_POINT('',(0.0190001188250343,-0.00281623939187291,0.0417909221529283));
#44472=CARTESIAN_POINT('',(0.01883918794397,-0.00374443486002948,0.0417675022340309));
#44473=CARTESIAN_POINT('',(0.0186329305165787,-0.00466364444896726,0.041744172032056));
#44474=CARTESIAN_POINT('',(0.0184237261443943,-0.00542023794619651,0.0417248071699552));
#44475=CARTESIAN_POINT('',(0.0182341939543165,-0.00601895963697044,0.041709356516343));
#44476=CARTESIAN_POINT('',(0.0181067373193245,-0.00638980793763761,0.0416997275496235));
#44477=CARTESIAN_POINT('',(0.0179990141098919,-0.00668531233952582,0.0416920153142986));
#44478=CARTESIAN_POINT('',(0.017916392612426,-0.00690382795499897,0.0416862924890993));
#44479=CARTESIAN_POINT('',(0.0178425052565168,-0.00709176327290445,0.0416813509509974));
#44480=CARTESIAN_POINT('',(0.0177883148431507,-0.00722653945516051,0.0416777980127546));
#44481=CARTESIAN_POINT('',(0.0177298981413602,-0.00736843643407748,0.0416740486377474));
#44482=CARTESIAN_POINT('',(0.0177361056959902,-0.00735322856386581,0.0416744462653413));
#44483=CARTESIAN_POINT('',(0.0177135634101485,-0.00740754993225115,0.0416729888207892));
#44484=CARTESIAN_POINT('',(0.0176680143708629,-0.00751609556693613,0.041670043125588));
#44485=CARTESIAN_POINT('',(0.0175448062254457,-0.00780316456919125,0.041662210094693));
#44486=CARTESIAN_POINT('',(0.017348210981071,-0.00823261039592076,0.0416503418793174));
#44487=CARTESIAN_POINT('',(0.0171581507082923,-0.00861763583287296,0.0416395442179049));
#44488=CARTESIAN_POINT('',(0.0170408569778842,-0.00884688509719389,0.041633066860205));
#44489=CARTESIAN_POINT('',(0.016927301857711,-0.00906191411808112,0.0416269489218333));
#44490=CARTESIAN_POINT('',(0.0168732845432318,-0.00916165575196913,0.0416240955502257));
#44491=CARTESIAN_POINT('',(0.0167812975926273,-0.00932980027693052,0.0416192760630031));
#44492=CARTESIAN_POINT('',(0.016631988134669,-0.00959517286625485,0.0416116243936469));
#44493=CARTESIAN_POINT('',(0.0164193261483387,-0.00995586530857537,0.0416011166646698));
#44494=CARTESIAN_POINT('',(0.0161847624984565,-0.0103324864458127,0.0415900052069004));
#44495=CARTESIAN_POINT('',(0.0159498587768442,-0.0106902384024307,0.0415793156198152));
#44496=CARTESIAN_POINT('',(0.015796244316713,-0.0109155198260444,0.041572531035281));
#44497=CARTESIAN_POINT('',(0.0155129752010751,-0.0113183676381549,0.0415603119633324));
#44498=CARTESIAN_POINT('',(0.0150924641525449,-0.0118804942876301,0.0415429661108013));
#44499=CARTESIAN_POINT('',(0.0145440817653639,-0.0125441050815185,0.041521767807207));
#44500=CARTESIAN_POINT('',(0.0140915599306013,-0.0130438517449637,0.0415051948603972));
#44501=CARTESIAN_POINT('',(0.0138418101853328,-0.0133064327326426,0.0414962928479585));
#44502=CARTESIAN_POINT('',(0.0137000435118975,-0.0134521125954502,0.0414913009244137));
#44503=CARTESIAN_POINT('',(0.0135721568664822,-0.01358097893778,0.0414868440266645));
#44504=CARTESIAN_POINT('',(0.0135127579654517,-0.0136399226716658,0.0414847888114123));
#44505=CARTESIAN_POINT('',(0.0134079418667648,-0.013743266022233,0.0414811698358558));
#44506=CARTESIAN_POINT('',(0.0132321544619379,-0.0139134442118671,0.0414751447406687));
#44507=CARTESIAN_POINT('',(0.0128578074911663,-0.0142643394281208,0.0414624736336486));
#44508=CARTESIAN_POINT('',(0.0122839075380286,-0.0147662800087533,0.0414435430200608));
#44509=CARTESIAN_POINT('',(0.0115197718166145,-0.0153709239660496,0.0414192000206712));
#44510=CARTESIAN_POINT('',(0.0106812149772433,-0.0159668181269291,0.0413933220512161));
#44511=CARTESIAN_POINT('',(0.00975690466001372,-0.0165472060690147,0.0413658437512961));
#44512=CARTESIAN_POINT('',(0.00890441110781952,-0.0170185858158063,0.0413414504706516));
#44513=CARTESIAN_POINT('',(0.00823467043365877,-0.0173488409284886,0.0413228317413075));
#44514=CARTESIAN_POINT('',(0.00771530984471599,-0.0175829815851227,0.0413086879133658));
#44515=CARTESIAN_POINT('',(0.00737764376545773,-0.0177277551035595,0.0412995976301186));
#44516=CARTESIAN_POINT('',(0.00691403151053966,-0.0179142109294009,0.0412872590562853));
#44517=CARTESIAN_POINT('',(0.00633275608651757,-0.0181300937591548,0.0412719520498979));
#44518=CARTESIAN_POINT('',(0.00558179665843677,-0.0183789366066925,0.0412524444884101));
#44519=CARTESIAN_POINT('',(0.00467350144335485,-0.0186304502234844,0.0412292194259067));
#44520=CARTESIAN_POINT('',(0.00375189364860263,-0.0188377440194866,0.0412059982606157));
#44521=CARTESIAN_POINT('',(0.00282298528495288,-0.0189991349645822,0.041182719351927));
#44522=CARTESIAN_POINT('',(0.0020426204353073,-0.0190955533563667,0.0411630849459833));
#44523=CARTESIAN_POINT('',(0.00141662338007611,-0.0191496192573831,0.0411472834710634));
#44524=CARTESIAN_POINT('',(0.00094492328585047,-0.0191786222294659,0.0411353397205267));
#44525=CARTESIAN_POINT('',(0.00055562148532413,-0.0191931629113999,0.0411254480643244));
#44526=CARTESIAN_POINT('',(0.000274635500326976,-0.019198259287767,0.0411182849436181));
#44527=CARTESIAN_POINT('',(0.0001270905012555,-0.019199752920174,0.0411145184785584));
#44528=CARTESIAN_POINT('',(-2.02964970173482E-5,-0.0192000691117518,0.0411107494338678));
#44529=CARTESIAN_POINT('',(-2.73070643263094E-5,-0.0191999691316681,0.0411105723125384));
#44530=CARTESIAN_POINT('',(-9.42927973934236E-5,-0.0191998346321775,0.0411088723275784));
#44531=CARTESIAN_POINT('',(-0.000205969520278353,-0.0191990996183042,0.0411060611825788));
#44532=CARTESIAN_POINT('',(-0.000518280221740988,-0.0191947419058968,0.0410982542710774));
#44533=CARTESIAN_POINT('',(-0.00103309894591407,-0.0191768017109537,0.0410854977049571));
#44534=CARTESIAN_POINT('',(-0.00171336636587479,-0.0191260939133093,0.0410686752816012));
#44535=CARTESIAN_POINT('',(-0.00230543730467123,-0.0190645268048041,0.0410540247051728));
#44536=CARTESIAN_POINT('',(-0.00286067294098488,-0.0189885112329839,0.0410402526882767));
#44537=CARTESIAN_POINT('',(-0.00329193554404226,-0.0189163249776132,0.0410295156066571));
#44538=CARTESIAN_POINT('',(-0.0035342242342768,-0.0188723538347853,0.0410234708837452));
#44539=CARTESIAN_POINT('',(-0.00375910804039232,-0.0188286630706858,0.0410178493118795));
#44540=CARTESIAN_POINT('',(-0.00384162655933352,-0.0188117972953263,0.0410157817445844));
#44541=CARTESIAN_POINT('',(-0.00400143706818024,-0.018778748732123,0.0410117720926416));
#44542=CARTESIAN_POINT('',(-0.00425819699640189,-0.0187228728404288,0.0410053066525806));
#44543=CARTESIAN_POINT('',(-0.00463771989515113,-0.0186334494088187,0.0409956885112588));
#44544=CARTESIAN_POINT('',(-0.00508851127973717,-0.0185153993939838,0.040984153418488));
#44545=CARTESIAN_POINT('',(-0.00569224122452594,-0.0183415009407844,0.0409685468614956));
#44546=CARTESIAN_POINT('',(-0.00644300606195459,-0.018095346477159,0.0409488352351614));
#44547=CARTESIAN_POINT('',(-0.00735583170749214,-0.0177436664305437,0.0409242354126093));
#44548=CARTESIAN_POINT('',(-0.00820912160318066,-0.0173649177393381,0.0409007285815477));
#44549=CARTESIAN_POINT('',(-0.0090538279450822,-0.01694010742605,0.040877039843528));
#44550=CARTESIAN_POINT('',(-0.00987370713245694,-0.016475597121502,0.0408535109429379));
#44551=CARTESIAN_POINT('',(-0.0106706046380784,-0.0159710614231159,0.0408300498006754));
#44552=CARTESIAN_POINT('',(-0.0114415208803768,-0.0154281587004333,0.0408066829887606));
#44553=CARTESIAN_POINT('',(-0.0120611630247417,-0.0149445875513516,0.0407872774133061));
#44554=CARTESIAN_POINT('',(-0.0125418597742535,-0.0145401658432658,0.0407718081455736));
#44555=CARTESIAN_POINT('',(-0.0128957072007173,-0.014227200367128,0.0407601975066044));
#44556=CARTESIAN_POINT('',(-0.0131812984549019,-0.0139620693089218,0.0407506373546599));
#44557=CARTESIAN_POINT('',(-0.0133832261727362,-0.013767278863127,0.0407437641941292));
#44558=CARTESIAN_POINT('',(-0.0134890079980719,-0.0136635724747964,0.0407401370570444));
#44559=CARTESIAN_POINT('',(-0.0135920490877858,-0.013560945588807,0.0407365795937386));
#44560=CARTESIAN_POINT('',(-0.0136020244899235,-0.0135508187127998,0.0407362285870597));
#44561=CARTESIAN_POINT('',(-0.0136593695095193,-0.0134931587835208,0.0407342215620005));
#44562=CARTESIAN_POINT('',(-0.0137674260651111,-0.0133833208258739,0.0407303919271764));
#44563=CARTESIAN_POINT('',(-0.013996397043834,-0.0131459926664997,0.040722152941196));
#44564=CARTESIAN_POINT('',(-0.0143081322534517,-0.0128059126383152,0.040710578123726));
#44565=CARTESIAN_POINT('',(-0.014597060811328,-0.0124744910247934,0.0406995286431268));
#44566=CARTESIAN_POINT('',(-0.0149345701175886,-0.0120710784827756,0.0406862962487426));
#44567=CARTESIAN_POINT('',(-0.0152524455295557,-0.0116664523525784,0.0406733520355922));
#44568=CARTESIAN_POINT('',(-0.0155706647652202,-0.0112369780874827,0.0406599171117849));
#44569=CARTESIAN_POINT('',(-0.0157645283850144,-0.0109610542320634,0.0406514507041408));
#44570=CARTESIAN_POINT('',(-0.0158919455376738,-0.0107745665543249,0.0406457889478978));
#44571=CARTESIAN_POINT('',(-0.0159519309316406,-0.0106856931805736,0.0406431040826272));
#44572=CARTESIAN_POINT('',(-0.0160654338153441,-0.0105145670838618,0.0406379731773375));
#44573=CARTESIAN_POINT('',(-0.0162016770731501,-0.010304023853768,0.0406317192796287));
#44574=CARTESIAN_POINT('',(-0.0164552144854539,-0.0098995951624851,0.0406198432844194));
#44575=CARTESIAN_POINT('',(-0.0168277519493567,-0.00926111915807136,0.0406015336613028));
#44576=CARTESIAN_POINT('',(-0.0172135131107076,-0.00851708721611685,0.0405808712722396));
#44577=CARTESIAN_POINT('',(-0.0175135330475122,-0.00787589007472945,0.0405634606948363));
#44578=CARTESIAN_POINT('',(-0.0177503849735952,-0.00732539050718729,0.0405487545920869));
#44579=CARTESIAN_POINT('',(-0.017922722387128,-0.00689108231165104,0.040537280282719));
#44580=CARTESIAN_POINT('',(-0.0181511767555939,-0.00627423918175756,0.040521067440932));
#44581=CARTESIAN_POINT('',(-0.0183961393016278,-0.00552402500539296,0.0405015295443943));
#44582=CARTESIAN_POINT('',(-0.0186009225445446,-0.00477507780306626,0.0404821756477855));
#44583=CARTESIAN_POINT('',(-0.0187209541078721,-0.00426730281736034,0.0404690999049196));
#44584=CARTESIAN_POINT('',(-0.0187862510926728,-0.00396592695886857,0.0404613500609706));
#44585=CARTESIAN_POINT('',(-0.0188251795061491,-0.00377850956076864,0.0404565299607827));
#44586=CARTESIAN_POINT('',(-0.0188886225474197,-0.00344903140273257,0.040448075166883));
#44587=CARTESIAN_POINT('',(-0.0189541146207765,-0.00307263170116469,0.0404384569554945));
#44588=CARTESIAN_POINT('',(-0.0190535010784377,-0.00241795211744246,0.0404218022349424));
#44589=CARTESIAN_POINT('',(-0.019142591264807,-0.00157900478061102,0.0404006391407023));
#44590=CARTESIAN_POINT('',(-0.0191926184988158,-0.000705848102638887,0.040378783110985));
#44591=CARTESIAN_POINT('',(-0.0192,-0.000219444370327988,0.0403666935404272));
#44592=CARTESIAN_POINT('',(-0.0192,8.05624845824862E-17,0.0403612589235446));
#44593=CARTESIAN_POINT('',(0.0192,-1.29239240960012E-18,0.0418617389925214));
#44594=CARTESIAN_POINT('',(-0.0192,0.,0.0433622164621474));
#44595=CARTESIAN_POINT('',(-0.0192,0.000147507211797211,0.043358580368065));
#44596=CARTESIAN_POINT('',(-0.0191968671072525,0.000525458418521057,0.0433492025507995));
#44597=CARTESIAN_POINT('',(-0.0191667659187235,0.00120492352254042,0.0433322092910609));
#44598=CARTESIAN_POINT('',(-0.0191111396477066,0.00187068354310731,0.0433154645381049));
#44599=CARTESIAN_POINT('',(-0.0190484499763511,0.00243151124645706,0.0433012997814833));
#44600=CARTESIAN_POINT('',(-0.0189751065261789,0.00294512260095273,0.0432882627843026));
#44601=CARTESIAN_POINT('',(-0.0189084433553087,0.00333635026762873,0.0432782816926402));
#44602=CARTESIAN_POINT('',(-0.018867967792637,0.00355705390119569,0.0432726367653853));
#44603=CARTESIAN_POINT('',(-0.0188296083107075,0.00375417659207935,0.0432675830486295));
#44604=CARTESIAN_POINT('',(-0.0188106259416012,0.00384747730435347,0.0432651876727724));
#44605=CARTESIAN_POINT('',(-0.0187773583892012,0.00400792394336318,0.0432610681996519));
#44606=CARTESIAN_POINT('',(-0.0187199017558882,0.00427152271885334,0.0432542932527772));
#44607=CARTESIAN_POINT('',(-0.0185927099205175,0.00480905822935209,0.0432404507442756));
#44608=CARTESIAN_POINT('',(-0.0183836195261831,0.00556575431155928,0.0432208669820836));
#44609=CARTESIAN_POINT('',(-0.0180873089804619,0.0064646645018153,0.0431973794975082));
#44610=CARTESIAN_POINT('',(-0.0177442040660365,0.00735402961973002,0.0431738834876022));
#44611=CARTESIAN_POINT('',(-0.0173632993142133,0.00821279140121295,0.0431507581437783));
#44612=CARTESIAN_POINT('',(-0.0169392847532721,0.00905524136579888,0.043127446598598));
#44613=CARTESIAN_POINT('',(-0.0164748479127218,0.00987497000160888,0.0431040980083793));
#44614=CARTESIAN_POINT('',(-0.0159706659023455,0.0106711723912282,0.0430806726152886));
#44615=CARTESIAN_POINT('',(-0.0154280486374394,0.0114416409274727,0.0430571802943427));
#44616=CARTESIAN_POINT('',(-0.0149449728707957,0.0120607045846526,0.0430375478018137));
#44617=CARTESIAN_POINT('',(-0.014540513942163,0.0125414184154737,0.0430218030197048));
#44618=CARTESIAN_POINT('',(-0.0142807307678563,0.0128352797598789,0.0430119587851853));
#44619=CARTESIAN_POINT('',(-0.0140679438908703,0.0130671648106762,0.043004050686227));
#44620=CARTESIAN_POINT('',(-0.0139080950559403,0.0132372608859938,0.0429981814449215));
#44621=CARTESIAN_POINT('',(-0.0137672328849502,0.0133832378360116,0.0429930765146623));
#44622=CARTESIAN_POINT('',(-0.0136667665316002,0.0134857999722318,0.0429894621544974));
#44623=CARTESIAN_POINT('',(-0.0135546774144437,0.0135983119843254,0.0429854613326154));
#44624=CARTESIAN_POINT('',(-0.0135803507422782,0.0135725269208031,0.0429863795009893));
#44625=CARTESIAN_POINT('',(-0.0135579609249865,0.0135949436866065,0.042985589934664));
#44626=CARTESIAN_POINT('',(-0.0135241260074496,0.0136286319576716,0.0429844163957469));
#44627=CARTESIAN_POINT('',(-0.0134122684980384,0.0137393669158131,0.0429805353181473));
#44628=CARTESIAN_POINT('',(-0.0131987708866369,0.013945378430781,0.0429732294322348));
#44629=CARTESIAN_POINT('',(-0.0128957040977496,0.014227232826039,0.0429630389328064));
#44630=CARTESIAN_POINT('',(-0.0124999931542044,0.0145775187949328,0.0429500291460551));
#44631=CARTESIAN_POINT('',(-0.0120874028980407,0.0149208543561088,0.0429368171809524));
#44632=CARTESIAN_POINT('',(-0.0117047957792533,0.0152212463926557,0.0429248432281859));
#44633=CARTESIAN_POINT('',(-0.0113893116609989,0.0154588971641096,0.0429151208160326));
#44634=CARTESIAN_POINT('',(-0.011106377823381,0.015662973841106,0.0429065341368306));
#44635=CARTESIAN_POINT('',(-0.0108884901785639,0.0158141883601005,0.0429000058007099));
#44636=CARTESIAN_POINT('',(-0.0107712324571543,0.0158942424996833,0.0428965109700417));
#44637=CARTESIAN_POINT('',(-0.0106505171116694,0.0159752774569547,0.0428929322227892));
#44638=CARTESIAN_POINT('',(-0.0106460205250655,0.0159781642821721,0.042892800425013));
#44639=CARTESIAN_POINT('',(-0.0105983640035796,0.0160098901889975,0.0428913896894949));
#44640=CARTESIAN_POINT('',(-0.0105316156086848,0.0160539203188257,0.04288941627459));
#44641=CARTESIAN_POINT('',(-0.0104195822931692,0.0161270482431749,0.0428861083490502));
#44642=CARTESIAN_POINT('',(-0.0102784486791453,0.0162173812691568,0.0428819542411143));
#44643=CARTESIAN_POINT('',(-0.0100739574925949,0.0163457058768856,0.0428759566447638));
#44644=CARTESIAN_POINT('',(-0.00979076681366074,0.0165178911957962,0.0428677007940556));
#44645=CARTESIAN_POINT('',(-0.00927468092065322,0.0168162097782484,0.0428528076913747));
#44646=CARTESIAN_POINT('',(-0.00866625429603682,0.0171406412178905,0.0428355294012159));
#44647=CARTESIAN_POINT('',(-0.00803551042611735,0.0174395582385297,0.0428179883621527));
#44648=CARTESIAN_POINT('',(-0.00766259866638816,0.0176058407656829,0.042807716932329));
#44649=CARTESIAN_POINT('',(-0.0073310592070669,0.0177461135495836,0.0427986527046041));
#44650=CARTESIAN_POINT('',(-0.00713356770854759,0.0178260102771758,0.042793290591069));
#44651=CARTESIAN_POINT('',(-0.0068231221615849,0.0179481502777101,0.042784905775808));
#44652=CARTESIAN_POINT('',(-0.00630114392385532,0.0181413482143627,0.042770945861394));
#44653=CARTESIAN_POINT('',(-0.00569487666756819,0.0183407643472124,0.0427550049086278));
#44654=CARTESIAN_POINT('',(-0.00509246246604135,0.0185142887079103,0.0427394087070486));
#44655=CARTESIAN_POINT('',(-0.00464231757800164,0.0186322966851656,0.0427278639663815));
#44656=CARTESIAN_POINT('',(-0.00426436225872812,0.0187214681324995,0.0427182582784477));
#44657=CARTESIAN_POINT('',(-0.00400818107344625,0.0187773012896955,0.0427117862363903));
#44658=CARTESIAN_POINT('',(-0.00384992820223385,0.0188101057953246,0.042707801538979));
#44659=CARTESIAN_POINT('',(-0.00376537048733135,0.0188273945620611,0.0427056751899009));
#44660=CARTESIAN_POINT('',(-0.00355088111217657,0.0188691891749171,0.0427002933345339));
#44661=CARTESIAN_POINT('',(-0.00331734099086169,0.0189118443746048,0.0426944453268529));
#44662=CARTESIAN_POINT('',(-0.00290184491701416,0.0189820651534296,0.0426840636256509));
#44663=CARTESIAN_POINT('',(-0.00236329931331893,0.0190572768250712,0.0426706619882368));
#44664=CARTESIAN_POINT('',(-0.00178375572217991,0.0191195601331886,0.0426562849943036));
#44665=CARTESIAN_POINT('',(-0.00127851800713429,0.0191592938373893,0.0426437722637567));
#44666=CARTESIAN_POINT('',(-0.000846210903470214,0.019182682757136,0.042633068638827));
#44667=CARTESIAN_POINT('',(-0.000489776321299228,0.019194662079583,0.0426242354581687));
#44668=CARTESIAN_POINT('',(-0.000249869930458502,0.0191986202501759,0.0426182746804729));
#44669=CARTESIAN_POINT('',(-0.000124192823849701,0.0191996863541797,0.0426151432531564));
#44670=CARTESIAN_POINT('',(-4.6679784386015E-5,0.0191999290556816,0.0426132061190403));
#44671=CARTESIAN_POINT('',(-3.55273807247816E-5,0.0192000724718196,0.0426129275911167));
#44672=CARTESIAN_POINT('',(0.000132725872022036,0.0191997674150739,0.0426087113417112));
#44673=CARTESIAN_POINT('',(0.000301334959408398,0.0191979264153387,0.0426044875461309));
#44674=CARTESIAN_POINT('',(0.000620058787525162,0.0191915262452281,0.0425965042664429));
#44675=CARTESIAN_POINT('',(0.00105625017562631,0.0191732552424566,0.042585580121496));
#44676=CARTESIAN_POINT('',(0.00157586498512921,0.0191375540444232,0.0425725590697522));
#44677=CARTESIAN_POINT('',(0.00225352720874131,0.0190725286873344,0.0425555563992737));
#44678=CARTESIAN_POINT('',(0.00307577592015579,0.0189604661224298,0.0425348667722705));
#44679=CARTESIAN_POINT('',(0.00433461762632953,0.0187229113146007,0.042502996563044));
#44680=CARTESIAN_POINT('',(0.00550296403284533,0.0184106330699154,0.0424730401318015));
#44681=CARTESIAN_POINT('',(0.00645166983970761,0.0180871524016339,0.0424482907150997));
#44682=CARTESIAN_POINT('',(0.0069619172411926,0.017895080795899,0.0424348530334128));
#44683=CARTESIAN_POINT('',(0.00735895883345079,0.0177350110020672,0.0424243268030787));
#44684=CARTESIAN_POINT('',(0.00764643716145475,0.0176127467126435,0.0424166296301185));
#44685=CARTESIAN_POINT('',(0.00811981898701091,0.0174022159675745,0.0424037960919214));
#44686=CARTESIAN_POINT('',(0.00876944710166559,0.0170887290080066,0.0423858318340952));
#44687=CARTESIAN_POINT('',(0.00951315708613044,0.0166847494227937,0.0423646407192132));
#44688=CARTESIAN_POINT('',(0.0100790413869899,0.0163436474742964,0.0423480383242041));
#44689=CARTESIAN_POINT('',(0.0104056123469378,0.0161368273680414,0.0423383123596306));
#44690=CARTESIAN_POINT('',(0.0106773257678165,0.0159581190475695,0.0423301204250104));
#44691=CARTESIAN_POINT('',(0.0108709588255067,0.0158265622046039,0.0423242248261542));
#44692=CARTESIAN_POINT('',(0.0111500967747105,0.015632249483432,0.0423156711224693));
#44693=CARTESIAN_POINT('',(0.0116135143005295,0.015295404023264,0.04230128967554));
#44694=CARTESIAN_POINT('',(0.0121187756985194,0.0148979561232106,0.0422852165665296));
#44695=CARTESIAN_POINT('',(0.0125939722026192,0.0144949013505583,0.0422696964213244));
#44696=CARTESIAN_POINT('',(0.0129353033061177,0.0141911492153154,0.0422583475135069));
#44697=CARTESIAN_POINT('',(0.0132118784921364,0.013932722585271,0.0422489739755852));
#44698=CARTESIAN_POINT('',(0.0133921363015402,0.0137587491919012,0.0422427835420144));
#44699=CARTESIAN_POINT('',(0.0135049874974253,0.0136475723361838,0.0422388740275091));
#44700=CARTESIAN_POINT('',(0.0135562891590839,0.013596963006152,0.0422370968087094));
#44701=CARTESIAN_POINT('',(0.0137309751687791,0.0134208586502648,0.0422309823553245));
#44702=CARTESIAN_POINT('',(0.0139110674958282,0.0132343715184421,0.0422245911612597));
#44703=CARTESIAN_POINT('',(0.014137592520735,0.0129930306245759,0.0422164308470755));
#44704=CARTESIAN_POINT('',(0.0143812101760025,0.012722482322191,0.0422074541024341));
#44705=CARTESIAN_POINT('',(0.0146807978338182,0.0123774570750208,0.0421961857196092));
#44706=CARTESIAN_POINT('',(0.0150050919875872,0.0119830224113509,0.0421835912660922));
#44707=CARTESIAN_POINT('',(0.0153221172843545,0.0115735139904246,0.0421708117041865));
#44708=CARTESIAN_POINT('',(0.0155727474341347,0.0112327867664899,0.0421603668629035));
#44709=CARTESIAN_POINT('',(0.0157608818977209,0.0109663563764849,0.0421523048467191));
#44710=CARTESIAN_POINT('',(0.0158724187713138,0.0108032907586352,0.0421474110573046));
#44711=CARTESIAN_POINT('',(0.015920938994233,0.0107315178459205,0.0421452606250145));
#44712=CARTESIAN_POINT('',(0.0159505791891584,0.0106873007672264,0.0421439337517554));
#44713=CARTESIAN_POINT('',(0.015945066621156,0.0106956996029432,0.0421441861147551));
#44714=CARTESIAN_POINT('',(0.0160294734566912,0.0105689614014762,0.0421403759015017));
#44715=CARTESIAN_POINT('',(0.016109585952249,0.0104465073799381,0.0421367138763467));
#44716=CARTESIAN_POINT('',(0.0162190528755293,0.0102763008430629,0.0421316482460841));
#44717=CARTESIAN_POINT('',(0.0163433133630848,0.0100774090294254,0.0421257758606307));
#44718=CARTESIAN_POINT('',(0.0165073176998543,0.00980776814333849,0.0421178704423418));
#44719=CARTESIAN_POINT('',(0.0167055244977741,0.00946782764719573,0.0421080091426432));
#44720=CARTESIAN_POINT('',(0.0169335320293294,0.00905371540032421,0.0420961542095714));
#44721=CARTESIAN_POINT('',(0.0171510782008102,0.00863455858579092,0.0420843034014677));
#44722=CARTESIAN_POINT('',(0.0173587805779037,0.00820886568577517,0.0420724088552192));
#44723=CARTESIAN_POINT('',(0.0175214623450828,0.00785396744808819,0.0420625985799328));
#44724=CARTESIAN_POINT('',(0.0176338988238206,0.00759567097700161,0.042055515377216));
#44725=CARTESIAN_POINT('',(0.0176918003353244,0.00745968562854511,0.0420517984670205));
#44726=CARTESIAN_POINT('',(0.0177486744917219,0.00732308913251824,0.0420480760415315));
#44727=CARTESIAN_POINT('',(0.0177509115770147,0.00731742321369519,0.0420479242320732));
#44728=CARTESIAN_POINT('',(0.0177761573272115,0.00725608237038993,0.0420462630915224));
#44729=CARTESIAN_POINT('',(0.0178177081338389,0.00715380871307502,0.0420435119330493));
#44730=CARTESIAN_POINT('',(0.0179324378360052,0.00686538158825476,0.0420358069385859));
#44731=CARTESIAN_POINT('',(0.018112361246438,0.00638436331410489,0.04202312787808));
#44732=CARTESIAN_POINT('',(0.018325840757539,0.00573631041106067,0.0420063211939584));
#44733=CARTESIAN_POINT('',(0.0184670742169264,0.00526192427057464,0.0419941430133837));
#44734=CARTESIAN_POINT('',(0.0185813044969062,0.00483863311912185,0.0419833616396935));
#44735=CARTESIAN_POINT('',(0.0186659401494481,0.00450204727579162,0.0419748302421681));
#44736=CARTESIAN_POINT('',(0.0187366075089475,0.00419556750954496,0.0419671013379643));
#44737=CARTESIAN_POINT('',(0.0187882700525209,0.00395705887023389,0.0419611053876857));
#44738=CARTESIAN_POINT('',(0.0188355216601128,0.00372453810855936,0.0419552769852958));
#44739=CARTESIAN_POINT('',(0.0188459268142927,0.00367031565686944,0.0419539197122962));
#44740=CARTESIAN_POINT('',(0.0188723933446082,0.00353309330142448,0.0419504809509566));
#44741=CARTESIAN_POINT('',(0.0189121053612324,0.00331649859254612,0.0419450518953231));
#44742=CARTESIAN_POINT('',(0.0189696566091318,0.00297547776343546,0.0419364996287203));
#44743=CARTESIAN_POINT('',(0.0190320962233435,0.00254661211898106,0.0419257401145415));
#44744=CARTESIAN_POINT('',(0.0191064706331641,0.00193756668593801,0.0419104555385234));
#44745=CARTESIAN_POINT('',(0.0191772638259746,0.00111160555292925,0.0418897173539831));
#44746=CARTESIAN_POINT('',(0.0192,0.000381663654322056,0.0418713583471171));
#44747=CARTESIAN_POINT('',(0.0192,-4.02812422912431E-17,0.0418617389925214));
#44748=CARTESIAN_POINT('',(-0.0192,-1.94617121099498E-14,0.0433622164621474));
#44749=CARTESIAN_POINT('',(0.0192,6.20369116582113E-17,0.044861351498379));
#44750=CARTESIAN_POINT('',(0.0192,-0.00251327412287178,0.044798887538536));
#44751=CARTESIAN_POINT('',(0.0182002919343753,-0.00753865073535333,0.0446739596188501));
#44752=CARTESIAN_POINT('',(0.0139299003749868,-0.0139299426504138,0.0444865677393211));
#44753=CARTESIAN_POINT('',(0.00753880775836791,-0.0182002798556818,0.0442991758597921));
#44754=CARTESIAN_POINT('',(-2.05686929275178E-17,-0.0196998600721591,0.0441117839802632));
#44755=CARTESIAN_POINT('',(-0.00753880775836791,-0.0182002798556818,0.0439243921007342));
#44756=CARTESIAN_POINT('',(-0.0139299003749868,-0.0139299426504137,0.0437370002212053));
#44757=CARTESIAN_POINT('',(-0.0182002919343753,-0.00753865073535333,0.0435496083416764));
#44758=CARTESIAN_POINT('',(-0.0192,-0.00251327412287176,0.0434246804219904));
#44759=CARTESIAN_POINT('',(-0.0192,8.05624845824862E-17,0.0433622164621474));
#44760=CARTESIAN_POINT('',(0.0192,3.74901540623289E-17,0.044861351498379));
#44761=CARTESIAN_POINT('',(0.0134577614771412,0.0136941102677163,0.0452414742614655));
#44762=CARTESIAN_POINT('',(0.0136855201965706,0.0134702824716422,0.0452335016921451));
#44763=CARTESIAN_POINT('',(0.0141298762423033,0.0130112461702288,0.0452175335389093));
#44764=CARTESIAN_POINT('',(0.0147611864198779,0.0122903912231453,0.0451935160925514));
#44765=CARTESIAN_POINT('',(0.0152568174315112,0.0116639372101018,0.0451734376386303));
#44766=CARTESIAN_POINT('',(0.0156338613138156,0.0111489679873024,0.0451573575763656));
#44767=CARTESIAN_POINT('',(0.0158622047786986,0.0108200703234377,0.0451472556778677));
#44768=CARTESIAN_POINT('',(0.0160161124866989,0.0105894382716242,0.0451402525654601));
#44769=CARTESIAN_POINT('',(0.0161053175604917,0.0104528771547491,0.0451361303424177));
#44770=CARTESIAN_POINT('',(0.016154666013204,0.0103764619483118,0.0451338308807265));
#44771=CARTESIAN_POINT('',(0.0162073223318096,0.0102938574043665,0.0451313536193738));
#44772=CARTESIAN_POINT('',(0.0162105065664181,0.0102887837226033,0.0451312024072254));
#44773=CARTESIAN_POINT('',(0.0162276362812458,0.0102618121619652,0.0451303990393071));
#44774=CARTESIAN_POINT('',(0.0162656449954779,0.0102015708728732,0.0451286212751449));
#44775=CARTESIAN_POINT('',(0.0163518542543136,0.0100635898383705,0.0451245826096027));
#44776=CARTESIAN_POINT('',(0.0165458020487241,0.0097441841874731,0.0451153427643101));
#44777=CARTESIAN_POINT('',(0.0168210008826648,0.00926799885690159,0.0451017819588008));
#44778=CARTESIAN_POINT('',(0.0171567968830624,0.00862548394619102,0.0450839282812965));
#44779=CARTESIAN_POINT('',(0.0174318062881837,0.00805757222941041,0.0450683983614061));
#44780=CARTESIAN_POINT('',(0.0176741525058544,0.00750847684832872,0.0450536336429448));
#44781=CARTESIAN_POINT('',(0.0178699501137322,0.00702574106353254,0.0450408207709287));
#44782=CARTESIAN_POINT('',(0.0179822065441399,0.00673081700074846,0.0450330602954559));
#44783=CARTESIAN_POINT('',(0.0180534349049712,0.00653593891772145,0.0450279578728813));
#44784=CARTESIAN_POINT('',(0.018108461643912,0.00638211837966673,0.0450239406980777));
#44785=CARTESIAN_POINT('',(0.0181209638386689,0.00634584696742375,0.0450229966878678));
#44786=CARTESIAN_POINT('',(0.0181500355739649,0.00626254619710393,0.0450208223787282));
#44787=CARTESIAN_POINT('',(0.0182027591255457,0.00610851249593621,0.0450168028334002));
#44788=CARTESIAN_POINT('',(0.0183281524290541,0.00573045201233244,0.0450069368917786));
#44789=CARTESIAN_POINT('',(0.018539378786679,0.00502322040266667,0.0449885388735071));
#44790=CARTESIAN_POINT('',(0.0187521753782728,0.00415974937968944,0.0449662614921629));
#44791=CARTESIAN_POINT('',(0.0189149832005711,0.00331540125865183,0.044944641160551));
#44792=CARTESIAN_POINT('',(0.0190333696277108,0.0025692626256965,0.0449256334103954));
#44793=CARTESIAN_POINT('',(0.0191322007628907,0.00170925695092131,0.0449039322303267));
#44794=CARTESIAN_POINT('',(0.0191903413400752,0.000786870471325928,0.0448808604775793));
#44795=CARTESIAN_POINT('',(0.0192,0.000249323547247888,0.0448675179844314));
#44796=CARTESIAN_POINT('',(0.0192,6.20369116582113E-17,0.044861351498379));
#44797=CARTESIAN_POINT('',(0.0134577620733179,0.0136941154998904,0.0452413722509897));
#44798=CARTESIAN_POINT('',(0.0134693251163026,0.0136827518905366,0.0452383139305518));
#44799=CARTESIAN_POINT('',(0.0135091245810281,0.0136433186594187,0.0452279191596696));
#44800=CARTESIAN_POINT('',(0.0137222886796034,0.0134398023342058,0.0451722602640239));
#44801=CARTESIAN_POINT('',(0.0138190249762464,0.0133538551974653,0.045147745444006));
#44802=CARTESIAN_POINT('',(0.0138718459707152,0.0133075728375538,0.0451344229377038));
#44803=CARTESIAN_POINT('',(0.,-0.0120000000000245,0.050900001));
#44804=CARTESIAN_POINT('',(0.,0.,0.050900001));
#44805=CARTESIAN_POINT('',(-0.0120000000000245,0.,0.050900001));
#44806=CARTESIAN_POINT('',(0.,0.,0.050900001));
#44807=CARTESIAN_POINT('',(-0.0192,0.,0.050900001));
#44808=CARTESIAN_POINT('',(0.,-0.0192,0.0489));
#44809=CARTESIAN_POINT('',(0.,0.,0.0489));
#44810=CARTESIAN_POINT('',(0.019,0.,0.0489));
#44811=CARTESIAN_POINT('',(0.,0.,0.0489));
#44812=CARTESIAN_POINT('',(0.0130000000000245,0.,0.0489));
#44813=CARTESIAN_POINT('',(0.,-0.0212,0.0332));
#44814=CARTESIAN_POINT('',(0.,0.,0.0332));
#44815=CARTESIAN_POINT('',(-0.0212,0.,0.0332));
#44816=CARTESIAN_POINT('',(0.,0.,0.0332));
#44817=CARTESIAN_POINT('',(0.0194,0.,0.0332));
#44818=CARTESIAN_POINT('',(0.0133472984199003,0.013834010563528,0.0361523640312405));
#44819=CARTESIAN_POINT('',(0.0136128985927427,0.0137274518465872,0.0359418834605953));
#44820=CARTESIAN_POINT('',(0.0136795294310282,0.0135039659523647,0.0356739008696272));
#44821=CARTESIAN_POINT('',(0.0134661557341698,0.0136975950548514,0.0361775333758731));
#44822=CARTESIAN_POINT('',(0.0136086981289552,0.0136172271430925,0.0360110987392474));
#44823=CARTESIAN_POINT('',(0.0136923375685161,0.013469742563547,0.035850717259336));
#44824=CARTESIAN_POINT('',(0.0135994539125629,0.0135548405221097,0.0362044425855375));
#44825=CARTESIAN_POINT('',(0.0136557312369491,0.0134970649841054,0.0361223786925854));
#44826=CARTESIAN_POINT('',(0.0137121251631036,0.0134394533765344,0.0360402698661124));
#44827=CARTESIAN_POINT('',(0.0137371549655767,0.0134138202407715,0.0362316337644044));
#44828=CARTESIAN_POINT('',(0.0137371549655767,0.0134138202407715,0.0362316337644044));
#44829=CARTESIAN_POINT('',(0.0137371549655767,0.0134138202407715,0.0362316337644044));
#44830=CARTESIAN_POINT('',(0.0136559709074636,0.013527425587518,0.034318741929522));
#44831=CARTESIAN_POINT('',(0.0135793479802664,0.013759152940594,0.0340623518581637));
#44832=CARTESIAN_POINT('',(0.0133075405240014,0.0138718879878007,0.0338655879801856));
#44833=CARTESIAN_POINT('',(0.0136626512276672,0.0134997252191483,0.0341411899032202));
#44834=CARTESIAN_POINT('',(0.013573293989727,0.0136518751809117,0.0339895570776138));
#44835=CARTESIAN_POINT('',(0.0134253578297479,0.0137374428278113,0.0338316666320085));
#44836=CARTESIAN_POINT('',(0.0136758218608079,0.013476371070873,0.03395063623351));
#44837=CARTESIAN_POINT('',(0.0136166570008004,0.0135364342732092,0.033872945275307));
#44838=CARTESIAN_POINT('',(0.0135576402206721,0.0135966282545905,0.033795255466116));
#44839=CARTESIAN_POINT('',(0.0136941106116928,0.0134577611271237,0.0337585246088596));
#44840=CARTESIAN_POINT('',(0.0136941106116928,0.0134577611271237,0.0337585246088596));
#44841=CARTESIAN_POINT('',(0.0136941106116929,0.0134577611271237,0.0337585246088596));
#44842=CARTESIAN_POINT('',(0.0135274197783297,0.0136559722321683,0.0446813017208849));
#44843=CARTESIAN_POINT('',(0.0137591216978861,0.0135793490080532,0.0449376690887189));
#44844=CARTESIAN_POINT('',(0.0138718493711407,0.0133075760157034,0.045134425378585));
#44845=CARTESIAN_POINT('',(0.0134997222462602,0.0136626530426041,0.0448588356204341));
#44846=CARTESIAN_POINT('',(0.0136518575203163,0.0135733015815387,0.0450104603247853));
#44847=CARTESIAN_POINT('',(0.0137374220236025,0.0134253776620627,0.0451683385915406));
#44848=CARTESIAN_POINT('',(0.0134763694953618,0.0136758234091799,0.0450493806425446));
#44849=CARTESIAN_POINT('',(0.0135364280715176,0.0136166631201245,0.0451270635743358));
#44850=CARTESIAN_POINT('',(0.0135966170774267,0.0135576512053218,0.0452047477806426));
#44851=CARTESIAN_POINT('',(0.0134577611073142,0.0136941106311604,0.045241474274411));
#44852=CARTESIAN_POINT('',(0.0134577611073142,0.0136941106311604,0.045241474274411));
#44853=CARTESIAN_POINT('',(0.0134577611073142,0.0136941106311604,0.0452414742744111));
#44854=CARTESIAN_POINT('',(0.0138344560633967,0.0133469119961932,0.0428477145766618));
#44855=CARTESIAN_POINT('',(0.0137278240280446,0.0136129157959794,0.0430583504712027));
#44856=CARTESIAN_POINT('',(0.0135040802168539,0.0136794867633816,0.0433266840430608));
#44857=CARTESIAN_POINT('',(0.0136984847986298,0.0134653599156988,0.0428226323586712));
#44858=CARTESIAN_POINT('',(0.0136177534369767,0.0136086105319708,0.0429893073493089));
#44859=CARTESIAN_POINT('',(0.013469952068938,0.0136922398391085,0.0431504402352761));
#44860=CARTESIAN_POINT('',(0.0135541740640735,0.0136001046836198,0.0427954286245404));
#44861=CARTESIAN_POINT('',(0.0134968084997804,0.0136559821004703,0.0428772848614511));
#44862=CARTESIAN_POINT('',(0.0134393323812074,0.0137122433104624,0.0429588263990224));
#44863=CARTESIAN_POINT('',(0.0134138202606126,0.0137371549462027,0.0427683673505048));
#44864=CARTESIAN_POINT('',(0.0134138202606126,0.0137371549462027,0.0427683673505048));
#44865=CARTESIAN_POINT('',(0.0134138202606126,0.0137371549462026,0.0427683673505048));
#44866=CARTESIAN_POINT('',(0.,0.,0.));
#44867=CARTESIAN_POINT('',(0.,0.,0.0487));
#44868=CARTESIAN_POINT('',(0.0192,0.,0.0487));
#44869=CARTESIAN_POINT('',(0.,0.,0.0334));
#44870=CARTESIAN_POINT('',(0.0192,0.,0.0334));
#44871=CARTESIAN_POINT('',(0.,0.,0.));
#44872=CARTESIAN_POINT('',(0.,0.,0.0499));
#44873=CARTESIAN_POINT('',(0.0120000000000245,0.,0.0499));
#44874=CARTESIAN_POINT('',(0.,0.,0.));
#44875=CARTESIAN_POINT('',(0.,0.,0.048900001));
#44876=CARTESIAN_POINT('',(-0.0212,0.,0.048900001));
#44877=CARTESIAN_POINT('',(0.0128751173724028,0.0144085717216295,0.0429735312461257));
#44878=CARTESIAN_POINT('',(0.0131333244250874,0.0141707592149881,0.042964717528887));
#44879=CARTESIAN_POINT('',(0.0133904435253121,0.0139280160341615,0.0429559068947327));
#44880=CARTESIAN_POINT('',(0.0158987497722569,0.0114264395544413,0.0428683193785747));
#44881=CARTESIAN_POINT('',(0.0175920161811642,0.00859581528207105,0.0427891876797143));
#44882=CARTESIAN_POINT('',(0.0194222911783444,0.00247676590716676,0.0426313696477661));
#44883=CARTESIAN_POINT('',(0.019562963909536,-0.000810843784974266,0.0425524653615877));
#44884=CARTESIAN_POINT('',(0.0182606575169193,-0.00706581685312737,0.0423944750844562));
#44885=CARTESIAN_POINT('',(0.0168183760123872,-0.0100242050478105,0.042315562410242));
#44886=CARTESIAN_POINT('',(0.0126966573657828,-0.0149044022188295,0.0421577017371009));
#44887=CARTESIAN_POINT('',(0.0100210068874356,-0.0168212406508217,0.0420787719850549));
#44888=CARTESIAN_POINT('',(0.00407243963060028,-0.0191515920325448,0.0419208058699113));
#44889=CARTESIAN_POINT('',(0.000806848361851911,-0.019562531967154,0.0418418755928234));
#44890=CARTESIAN_POINT('',(-0.00553306068688165,-0.018781161179321,0.0416840174919447));
#44891=CARTESIAN_POINT('',(-0.00860120532063141,-0.0175895931973386,0.0416050879420078));
#44892=CARTESIAN_POINT('',(-0.0138056580461542,-0.0138842419326171,0.0414471211199442));
#44893=CARTESIAN_POINT('',(-0.0159357918461525,-0.0113751566036123,0.0413681914665986));
#44894=CARTESIAN_POINT('',(-0.0187492557985244,-0.00564022844013249,0.0412103332713815));
#44895=CARTESIAN_POINT('',(-0.0194298312204639,-0.00241995492611967,0.0411314037292813));
#44896=CARTESIAN_POINT('',(-0.0191744011757895,0.0039636736746371,0.0409734369221964));
#44897=CARTESIAN_POINT('',(-0.0182389517901175,0.0071192897701119,0.040894507254258));
#44898=CARTESIAN_POINT('',(-0.0149766811072747,0.0126113358866933,0.0407366490611891));
#44899=CARTESIAN_POINT('',(-0.0126530155410305,0.0149424134885897,0.0406577195188047));
#44900=CARTESIAN_POINT('',(-0.00716914867521055,0.0182200899183962,0.040499752711441));
#44901=CARTESIAN_POINT('',(-0.0040157303431181,0.0191629214644348,0.0404208230437047));
#44902=CARTESIAN_POINT('',(0.00236631950412073,0.0194357223134969,0.0402629648507107));
#44903=CARTESIAN_POINT('',(0.00558874413207926,0.0187654059953617,0.0401840353082519));
#44904=CARTESIAN_POINT('',(0.011332095847439,0.0159672155702773,0.0400260685009428));
#44905=CARTESIAN_POINT('',(0.0138461591609683,0.0138429594282163,0.0399471388332248));
#44906=CARTESIAN_POINT('',(0.017565189295934,0.00864932915543225,0.0397892806401376));
#44907=CARTESIAN_POINT('',(0.0187665221595431,0.00558499500257808,0.0397103510977194));
#44908=CARTESIAN_POINT('',(0.0195652865780699,-0.000753611625385773,0.0395523842904227));
#44909=CARTESIAN_POINT('',(0.0191619928435045,-0.0040201591400539,0.0394734546227174));
#44910=CARTESIAN_POINT('',(0.0168481763607773,-0.00997425301230359,0.0393155964295924));
#44911=CARTESIAN_POINT('',(0.0149398853269601,-0.0126560005357337,0.039236666887228));
#44912=CARTESIAN_POINT('',(0.0100702990665986,-0.016791588551228,0.0390787000798614));
#44913=CARTESIAN_POINT('',(0.00711507422239091,-0.0182405967022088,0.0389997704121751));
#44914=CARTESIAN_POINT('',(0.000864968760624566,-0.0195601277829158,0.038841912219082));
#44915=CARTESIAN_POINT('',(-0.00242383663527852,-0.0194293473670445,0.0387629826766795));
#44916=CARTESIAN_POINT('',(-0.00854942352561615,-0.0176146452346672,0.0386050158693573));
#44917=CARTESIAN_POINT('',(-0.0113788393619798,-0.0159331623988121,0.038526086201702));
#44918=CARTESIAN_POINT('',(-0.0159019902197058,-0.0114224987144947,0.0383682280085025));
#44919=CARTESIAN_POINT('',(-0.0175913112934338,-0.00859769097603843,0.0382892984661209));
#44920=CARTESIAN_POINT('',(-0.0194224819673239,-0.00247700698301382,0.0381313316588633));
#44921=CARTESIAN_POINT('',(-0.0195623446832896,0.000811369048211784,0.0380524019910925));
#44922=CARTESIAN_POINT('',(-0.0182600972832356,0.00706509851662393,0.0378945437980595));
#44923=CARTESIAN_POINT('',(-0.016819233986536,0.0100243648801336,0.0378156142556532));
#44924=CARTESIAN_POINT('',(-0.0126967579507606,0.0149050564206465,0.0376576474482783));
#44925=CARTESIAN_POINT('',(-0.0100203374244886,0.0168207160115748,0.0375787177806155));
#44926=CARTESIAN_POINT('',(-0.004072662932392,0.0191509839559279,0.0374208595874837));
#44927=CARTESIAN_POINT('',(-0.000807186806473285,0.0195633067910464,0.0373419300450818));
#44928=CARTESIAN_POINT('',(0.00553354521670946,0.018781593295045,0.0371839632377971));
#44929=CARTESIAN_POINT('',(0.00860113448735149,0.0175887502336188,0.0371050335701185));
#44930=CARTESIAN_POINT('',(0.0138050263039444,0.0138840922850618,0.0369471753769281));
#44931=CARTESIAN_POINT('',(0.0159362553123575,0.0113758643522062,0.0368682458345405));
#44932=CARTESIAN_POINT('',(0.0187498826791494,0.00564005929796595,0.0367102790272858));
#44933=CARTESIAN_POINT('',(0.0194290867556229,0.00241955307612708,0.0366313493595608));
#44934=CARTESIAN_POINT('',(0.0191739303520504,-0.00396322655069507,0.036473491166433));
#44935=CARTESIAN_POINT('',(0.0182397977873896,-0.00711929068202113,0.0363945616240418));
#44936=CARTESIAN_POINT('',(0.0149768823760523,-0.0126119532056393,0.0362365948167335));
#44937=CARTESIAN_POINT('',(0.0126522719426653,-0.0149420100364957,0.0361576651490156));
#44938=CARTESIAN_POINT('',(0.00716926547582709,-0.0182194512093103,0.0359998069559463));
#44939=CARTESIAN_POINT('',(0.00401619229775511,-0.0191636302044921,0.0359208774133096));
#44940=CARTESIAN_POINT('',(-0.0023667262209589,-0.0194362284487689,0.0357629106062309));
#44941=CARTESIAN_POINT('',(-0.00558881308252601,-0.0187645628162864,0.0356839809387912));
#44942=CARTESIAN_POINT('',(-0.0113314972464994,-0.0159669640166278,0.0355261227436458));
#44943=CARTESIAN_POINT('',(-0.0138464999243795,-0.0138437337554346,0.0354471932155239));
#44944=CARTESIAN_POINT('',(-0.01756583540215,-0.00864926556607988,0.0352892263937148));
#44945=CARTESIAN_POINT('',(-0.018765854056893,-0.00558447602392299,0.0352102967174342));
#44946=CARTESIAN_POINT('',(-0.0195647493008025,0.000753248602856806,0.0350524386178169));
#44947=CARTESIAN_POINT('',(-0.0191628223557256,0.00402001703766339,0.0349735084674251));
#44948=CARTESIAN_POINT('',(-0.0168484806950671,0.00997483127891498,0.0348155423423861));
#44949=CARTESIAN_POINT('',(-0.014939075025363,0.0126557229800961,0.0347366124977029));
#44950=CARTESIAN_POINT('',(-0.0100702823681381,0.0167909070241343,0.0345787517858474));
#44951=CARTESIAN_POINT('',(-0.00711585876291648,0.0182414349753937,0.0344998392303287));
#44952=CARTESIAN_POINT('',(-0.000864400312993994,0.0195605093863205,0.0343418491020202));
#44953=CARTESIAN_POINT('',(0.0024235334564365,0.0194289217552847,0.0342629443605591));
#44954=CARTESIAN_POINT('',(0.0085476414010583,0.0176156446635616,0.0341051266538377));
#44955=CARTESIAN_POINT('',(0.0113888335904153,0.0159241881786858,0.0340257855313145));
#44956=CARTESIAN_POINT('',(0.0138919024844783,0.013427851971904,0.0339383847815977));
#44957=CARTESIAN_POINT('',(0.014134362965028,0.0131716883241156,0.0339295970016211));
#44958=CARTESIAN_POINT('',(0.0143721856923585,0.0129134700672116,0.0339207829037038));
#44959=CARTESIAN_POINT('',(0.013244880717954,0.0148039903320255,0.0431369141780147));
#44960=CARTESIAN_POINT('',(0.0135065467987276,0.014562992009576,0.0431279823892726));
#44961=CARTESIAN_POINT('',(0.0137690967913546,0.0143151389119729,0.0431191067182131));
#44962=CARTESIAN_POINT('',(0.0163483463147584,0.0117415761632288,0.04303142627739));
#44963=CARTESIAN_POINT('',(0.0180872928602693,0.00883212246784146,0.0429523232752052));
#44964=CARTESIAN_POINT('',(0.0199672051382433,0.00254146260767922,0.042794576298));
#44965=CARTESIAN_POINT('',(0.0201112200424338,-0.00083757785566147,0.042715711296312));
#44966=CARTESIAN_POINT('',(0.0187705210453593,-0.00726924770963437,0.0425575818040092));
#44967=CARTESIAN_POINT('',(0.0172869776211763,-0.0103097002776528,0.0424787150432717));
#44968=CARTESIAN_POINT('',(0.0130490476432779,-0.0153249931900973,0.0423209135715474));
#44969=CARTESIAN_POINT('',(0.0102983988238696,-0.0172948889052652,0.0422420144205481));
#44970=CARTESIAN_POINT('',(0.00418102238433576,-0.019689679955431,0.0420839261351123));
#44971=CARTESIAN_POINT('',(0.000824147707122541,-0.020110982597467,0.0420050253753412));
#44972=CARTESIAN_POINT('',(-0.00569243630278051,-0.0193062101235236,0.0418472297219421));
#44973=CARTESIAN_POINT('',(-0.00884600679789724,-0.0180808786993726,0.0417683304244268));
#44974=CARTESIAN_POINT('',(-0.0141967388150451,-0.0142694498651659,0.0416102406980189));
#44975=CARTESIAN_POINT('',(-0.0163854744768955,-0.0116896130235589,0.0415313413624343));
#44976=CARTESIAN_POINT('',(-0.0192759793352938,-0.00579397917775157,0.041373545475094));
#44977=CARTESIAN_POINT('',(-0.0199750126908028,-0.00248372302623619,0.0412946462125953));
#44978=CARTESIAN_POINT('',(-0.0197107852448881,0.00408038461059604,0.0411365565175739));
#44979=CARTESIAN_POINT('',(-0.0187481572506002,0.00732375763574827,0.0410576571475741));
#44980=CARTESIAN_POINT('',(-0.0153934865396828,0.0129681974909316,0.0408998612656592));
#44981=CARTESIAN_POINT('',(-0.0130045860573409,0.0153639432955975,0.0408209620020816));
#44982=CARTESIAN_POINT('',(-0.00736481647076704,0.0187329675119329,0.040662872306547));
#44983=CARTESIAN_POINT('',(-0.00412306568888511,0.0197010445290123,0.0405839729369947));
#44984=CARTESIAN_POINT('',(0.00243710111309297,0.019979842646596,0.0404261770552279));
#44985=CARTESIAN_POINT('',(0.00574934390972627,0.0192902839979054,0.0403472777915276));
#44986=CARTESIAN_POINT('',(0.0116544396358271,0.0164115395447182,0.0401891880960528));
#44987=CARTESIAN_POINT('',(0.0142379508821379,0.0142271424006341,0.0401102887265381));
#44988=CARTESIAN_POINT('',(0.0180594224696077,0.00888767877911417,0.0399524928446313));
#44989=CARTESIAN_POINT('',(0.0192937721810321,0.00573762730904085,0.0398735935809895));
#44990=CARTESIAN_POINT('',(0.0201135650562981,-0.000780444860065475,0.0397155038855382));
#44991=CARTESIAN_POINT('',(0.0196979077097771,-0.00413802586633374,0.0396366045160817));
#44992=CARTESIAN_POINT('',(0.0173180345998703,-0.0102576435700848,0.039478808634035));
#44993=CARTESIAN_POINT('',(0.015356042405559,-0.0130139146204963,0.0393999093704902));
#44994=CARTESIAN_POINT('',(0.0103477150858215,-0.0172652653022394,0.0392418196749849));
#44995=CARTESIAN_POINT('',(0.00730951779926764,-0.0187537136523111,0.0391629203054914));
#44996=CARTESIAN_POINT('',(0.000884711783842049,-0.020108477293814,0.0390051244235729));
#44997=CARTESIAN_POINT('',(-0.0024958539615088,-0.0199735005723642,0.0389262251599531));
#44998=CARTESIAN_POINT('',(-0.00879423764234924,-0.0181059652530067,0.0387681354644694));
#44999=CARTESIAN_POINT('',(-0.011702053115772,-0.0163765924140203,0.0386892360951575));
#45000=CARTESIAN_POINT('',(-0.016350251638447,-0.0117389456667314,0.038531440212854));
#45001=CARTESIAN_POINT('',(-0.0180862478599091,-0.00883502407804941,0.0384525409493668));
#45002=CARTESIAN_POINT('',(-0.0199676992469986,-0.00254078339015984,0.0382944512540031));
#45003=CARTESIAN_POINT('',(-0.0201103505948417,0.000839419538129869,0.0382155518843851));
#45004=CARTESIAN_POINT('',(-0.0187701918210865,0.00726728787221907,0.0380577560025739));
#45005=CARTESIAN_POINT('',(-0.0172886259471365,0.0103089002794402,0.037978856738934));
#45006=CARTESIAN_POINT('',(-0.0130483550078281,0.015326611662146,0.0378207670433832));
#45007=CARTESIAN_POINT('',(-0.0102965853185908,0.0172948303544054,0.0377418676739293));
#45008=CARTESIAN_POINT('',(-0.00418239204957526,0.0196886050994017,0.037584071791977));
#45009=CARTESIAN_POINT('',(-0.000825716376582044,0.0201118921182084,0.0375051725283272));
#45010=CARTESIAN_POINT('',(0.0056941517708637,0.0193065074279527,0.0373470828329373));
#45011=CARTESIAN_POINT('',(0.00884695384515193,0.0180793316767743,0.0372681834635453));
#45012=CARTESIAN_POINT('',(0.0141950885647465,0.0142700047178758,0.0371103875813084));
#45013=CARTESIAN_POINT('',(0.0163853778444867,0.0116914244214254,0.0370314883177673));
#45014=CARTESIAN_POINT('',(0.0192771666541589,0.00579270569280173,0.0368733986224446));
#45015=CARTESIAN_POINT('',(0.0199742355396882,0.00248208396680975,0.03679449925292));
#45016=CARTESIAN_POINT('',(0.0197103471394279,-0.00407869950554762,0.0366367033708807));
#45017=CARTESIAN_POINT('',(0.018749620840931,-0.00732268601191894,0.0365578041072789));
#45018=CARTESIAN_POINT('',(0.0153930698197874,-0.0129698880095284,0.036399714411885));
#45019=CARTESIAN_POINT('',(0.0130027888314922,-0.0153641891687384,0.0363208150423589));
#45020=CARTESIAN_POINT('',(0.00736598756274524,-0.0187316790820181,0.036163019160431));
#45021=CARTESIAN_POINT('',(0.0041247633259904,-0.0197016836759312,0.0360841198963006));
#45022=CARTESIAN_POINT('',(-0.00243874428503272,-0.0199804184070515,0.0359260302013203));
#45023=CARTESIAN_POINT('',(-0.0057505327317695,-0.0192889139048742,0.0358471308327378));
#45024=CARTESIAN_POINT('',(-0.0116527204687135,-0.0164118152451721,0.0356893349457639));
#45025=CARTESIAN_POINT('',(-0.0142375575240833,-0.0142289131365525,0.0356104357158766));
#45026=CARTESIAN_POINT('',(-0.0180608031458059,-0.00888661814352176,0.0354523459896135));
#45027=CARTESIAN_POINT('',(-0.0192932754654998,-0.00573588273138894,0.0353734465854948));
#45028=CARTESIAN_POINT('',(-0.0201128562646196,0.000778855422054386,0.0352156509329156));
#45029=CARTESIAN_POINT('',(-0.0196991696809191,0.00413672481531792,0.0351367502803128));
#45030=CARTESIAN_POINT('',(-0.0173179069910243,0.0102593800136393,0.0349786619865434));
#45031=CARTESIAN_POINT('',(-0.0153542920277628,0.0130144577141355,0.0348997627572814));
#45032=CARTESIAN_POINT('',(-0.0103486360334633,0.017263766075639,0.034741961252782));
#45033=CARTESIAN_POINT('',(-0.00731153357968647,0.0187542778224974,0.0346630945924325));
#45034=CARTESIAN_POINT('',(-0.00088283361010462,0.0201091459479512,0.0345049652257676));
#45035=CARTESIAN_POINT('',(0.00249648070157979,0.0199728080362074,0.0344260998394164));
#45036=CARTESIAN_POINT('',(0.00879141509936053,0.0181072591432389,0.0342683531370332));
#45037=CARTESIAN_POINT('',(0.0117108803520172,0.0163687603127585,0.0341890347296195));
#45038=CARTESIAN_POINT('',(0.0142847430045092,0.0138005869114252,0.0341015476699935));
#45039=CARTESIAN_POINT('',(0.0145322375581197,0.0135389638897274,0.0340926962624872));
#45040=CARTESIAN_POINT('',(0.0147732447934845,0.0132772880232293,0.0340837641415089));
#45041=CARTESIAN_POINT('',(0.0134164396611127,0.0149734662699873,0.0435900976144594));
#45042=CARTESIAN_POINT('',(0.0136796474430364,0.0147310480180751,0.0435811132008271));
#45043=CARTESIAN_POINT('',(0.0139445606758513,0.0144808533047822,0.0435722084496325));
#45044=CARTESIAN_POINT('',(0.0165541803787265,0.0118740244693021,0.0434844866053923));
#45045=CARTESIAN_POINT('',(0.0183120729305598,0.00892862932083445,0.0434053963917));
#45046=CARTESIAN_POINT('',(0.0202110140523984,0.00256064972205639,0.0432476811088157));
#45047=CARTESIAN_POINT('',(0.0203548755530947,-0.000859156831837742,0.0431688335154196));
#45048=CARTESIAN_POINT('',(0.0189940535653762,-0.00736886204407924,0.0430106420675322));
#45049=CARTESIAN_POINT('',(0.0174906492691983,-0.0104451356738669,0.0429317957701886));
#45050=CARTESIAN_POINT('',(0.0131985459197013,-0.0155185165039707,0.0427740206496132));
#45051=CARTESIAN_POINT('',(0.0104135587920133,-0.0175106919071648,0.0426951351063101));
#45052=CARTESIAN_POINT('',(0.00421989511762802,-0.0199312807768646,0.0425369924254557));
#45053=CARTESIAN_POINT('',(0.000822165829661969,-0.0203555687823335,0.0424581048304965));
#45054=CARTESIAN_POINT('',(-0.00577268415217634,-0.0195372110262576,0.0423003369807169));
#45055=CARTESIAN_POINT('',(-0.00896368245745464,-0.0182953203640746,0.0422214511295832));
#45056=CARTESIAN_POINT('',(-0.014377738173501,-0.0144341362566882,0.042063306682774));
#45057=CARTESIAN_POINT('',(-0.0165913177413619,-0.0118217297559613,0.0419844208681352));
#45058=CARTESIAN_POINT('',(-0.0195132569626783,-0.00585314394204532,0.0418266527220008));
#45059=CARTESIAN_POINT('',(-0.0202188985482763,-0.00250249737859145,0.0417477669181936));
#45060=CARTESIAN_POINT('',(-0.0199476524226673,0.00414183628428791,0.0415896225100204));
#45061=CARTESIAN_POINT('',(-0.0189713465461571,0.0074238217144122,0.0415107366521508));
#45062=CARTESIAN_POINT('',(-0.0155727958581524,0.0131344783069039,0.0413529685129072));
#45063=CARTESIAN_POINT('',(-0.0131536962360839,0.0155578477627397,0.0412740827076612));
#45064=CARTESIAN_POINT('',(-0.00744292525627976,0.0189648756528633,0.0411159382988743));
#45065=CARTESIAN_POINT('',(-0.00416136837068427,0.0199426209891001,0.041037052441561));
#45066=CARTESIAN_POINT('',(0.0024782329367654,0.0202209013832472,0.0408792843024956));
#45067=CARTESIAN_POINT('',(0.00583011869197187,0.0195211697322738,0.0408003984971062));
#45068=CARTESIAN_POINT('',(0.0118058639010852,0.0166037713321414,0.0406422540883824));
#45069=CARTESIAN_POINT('',(0.0144192410151831,0.0143913379217445,0.0405633682311128));
#45070=CARTESIAN_POINT('',(0.0182837257384388,0.00898509122716692,0.0404056000918904));
#45071=CARTESIAN_POINT('',(0.0195312415965337,0.00579628789620374,0.0403267142865668));
#45072=CARTESIAN_POINT('',(0.0203573162877559,-0.000802071356869746,0.0401685698778692));
#45073=CARTESIAN_POINT('',(0.0199345230002467,-0.00419998945070916,0.0400896840206814));
#45074=CARTESIAN_POINT('',(0.0175222672957333,-0.0103921431886806,0.0399319158812692));
#45075=CARTESIAN_POINT('',(0.0155350345421537,-0.0131806317546663,0.0398530300760634));
#45076=CARTESIAN_POINT('',(0.010462929394733,-0.0174811542348422,0.03969488566732));
#45077=CARTESIAN_POINT('',(0.00738706026086871,-0.0189856909101189,0.039615999810069));
#45078=CARTESIAN_POINT('',(0.000883817908637908,-0.0203530183791772,0.0394582316708292));
#45079=CARTESIAN_POINT('',(-0.00253752453815646,-0.0202145324184487,0.0393793458655338));
#45080=CARTESIAN_POINT('',(-0.00891195636570637,-0.0183204988642966,0.0392212014567969));
#45081=CARTESIAN_POINT('',(-0.0118538449930932,-0.016568387897323,0.0391423155997955));
#45082=CARTESIAN_POINT('',(-0.0165554621411534,-0.0118719486406755,0.0389845474600498));
#45083=CARTESIAN_POINT('',(-0.0183108232868112,-0.00893197079241942,0.0389056616549338));
#45084=CARTESIAN_POINT('',(-0.0202116856337268,-0.0025595719846472,0.0387475172463442));
#45085=CARTESIAN_POINT('',(-0.0203539376319971,0.000861592423192441,0.0386686313889525));
#45086=CARTESIAN_POINT('',(-0.0189937769587308,0.00736633749442342,0.0385108632498404));
#45087=CARTESIAN_POINT('',(-0.0174926176026702,0.0104438824718023,0.0384319774445165));
#45088=CARTESIAN_POINT('',(-0.0131975320941528,0.0155205924991396,0.0382738330357088));
#45089=CARTESIAN_POINT('',(-0.0104112524037978,0.0175108806750789,0.0381949471785047));
#45090=CARTESIAN_POINT('',(-0.00422176050540625,0.0199299580901202,0.0380371790392355));
#45091=CARTESIAN_POINT('',(-0.000824286670233699,0.020356495355586,0.0379582932338931));
#45092=CARTESIAN_POINT('',(0.00577495389241394,0.0195374909454256,0.0378001488252795));
#45093=CARTESIAN_POINT('',(0.00896510698013095,0.01829349544155,0.0377212629681725));
#45094=CARTESIAN_POINT('',(0.014375608693655,0.014434970243203,0.0375634948285151));
#45095=CARTESIAN_POINT('',(0.0165909334505597,0.0118240128093593,0.0374846090233243));
#45096=CARTESIAN_POINT('',(0.0195147328835605,0.00585139687469778,0.0373264646147958));
#45097=CARTESIAN_POINT('',(0.0202181499040229,0.00250030659957759,0.0372475787575161));
#45098=CARTESIAN_POINT('',(0.0199471858992586,-0.0041395973158831,0.0370898106181184));
#45099=CARTESIAN_POINT('',(0.0189730476548394,-0.00742225130017299,0.0370109248128424));
#45100=CARTESIAN_POINT('',(0.0155721405214547,-0.0131366694593094,0.036852780404231));
#45101=CARTESIAN_POINT('',(0.0131514527210815,-0.0155584192627295,0.0367738945469489));
#45102=CARTESIAN_POINT('',(0.00744454448079525,-0.0189632604976578,0.0366161264076841));
#45103=CARTESIAN_POINT('',(0.00416361348869007,-0.0199431861661279,0.0365372406017529));
#45104=CARTESIAN_POINT('',(-0.00248042573380237,-0.0202215512025244,0.0363790961936408));
#45105=CARTESIAN_POINT('',(-0.00583182421418022,-0.0195196041217457,0.0363002103375919));
#45106=CARTESIAN_POINT('',(-0.0118036261064655,-0.0166042434939482,0.0361424421919664));
#45107=CARTESIAN_POINT('',(-0.0144184862761918,-0.0143935265254053,0.0360635564290704));
#45108=CARTESIAN_POINT('',(-0.0182854690326266,-0.00898361096526036,0.0359054119822515));
#45109=CARTESIAN_POINT('',(-0.0195308638237847,-0.00579400387153972,0.0358265260789878));
#45110=CARTESIAN_POINT('',(-0.0203564882148241,0.000799940324915589,0.0356687582293281));
#45111=CARTESIAN_POINT('',(-0.0199359375067954,0.00419815773277999,0.0355898706870897));
#45112=CARTESIAN_POINT('',(-0.0175219871768453,0.0103944117617503,0.0354317280021644));
#45113=CARTESIAN_POINT('',(-0.0155328938191153,0.0131815721981596,0.0353528424204919));
#45114=CARTESIAN_POINT('',(-0.0104642419482611,0.0174792590663091,0.0351950672837447));
#45115=CARTESIAN_POINT('',(-0.00738961226246486,0.0189860828077318,0.0351162210357799));
#45116=CARTESIAN_POINT('',(-0.000881364410376992,0.0203538577683945,0.0349580296493947));
#45117=CARTESIAN_POINT('',(0.00253857652463648,0.0202137634662172,0.0348791818673028));
#45118=CARTESIAN_POINT('',(0.00890865369405714,0.0183218706412125,0.0347214667192783));
#45119=CARTESIAN_POINT('',(0.0118621239181345,0.0165610351729331,0.034642158413343));
#45120=CARTESIAN_POINT('',(0.0144662895113594,0.0139596614511138,0.0345546329568948));
#45121=CARTESIAN_POINT('',(0.0147159584881365,0.0136955527308699,0.034545753344709));
#45122=CARTESIAN_POINT('',(0.0149583820325668,0.0134323390934634,0.0345367687330064));
#45123=CARTESIAN_POINT('',(0.0134243968563088,0.014965926637851,0.0440266469880068));
#45124=CARTESIAN_POINT('',(0.013687606574829,0.0147235066023048,0.04401766250827));
#45125=CARTESIAN_POINT('',(0.0139524570657552,0.0144732354661768,0.0440087576139998));
#45126=CARTESIAN_POINT('',(0.0165606827243585,0.0118650105264396,0.0439210357331533));
#45127=CARTESIAN_POINT('',(0.0183169785555386,0.00891864534677705,0.0438419455335554));
#45128=CARTESIAN_POINT('',(0.0202123964059005,0.00254961458525535,0.0436842303191043));
#45129=CARTESIAN_POINT('',(0.0203543744478548,-0.000870260450086682,0.0436053826318688));
#45130=CARTESIAN_POINT('',(0.0189900756022342,-0.00737923951972287,0.0434471912128856));
#45131=CARTESIAN_POINT('',(0.017484961083932,-0.0104546923800447,0.0433683449407809));
#45132=CARTESIAN_POINT('',(0.0131900644680276,-0.015525710760186,0.0432105698130354));
#45133=CARTESIAN_POINT('',(0.0104039896779972,-0.0175163459681026,0.0431316842509498));
#45134=CARTESIAN_POINT('',(0.00420902850051582,-0.0199336166445472,0.0429735415663171));
#45135=CARTESIAN_POINT('',(0.000811053872307399,-0.020356036240556,0.042894653998026));
#45136=CARTESIAN_POINT('',(-0.00578334574047468,-0.019534045015475,0.0427368861494216));
#45137=CARTESIAN_POINT('',(-0.00897364968385085,-0.0182904018976007,0.0426580002725041));
#45138=CARTESIAN_POINT('',(-0.0143856374953915,-0.0144263171073726,0.0424998558240156));
#45139=CARTESIAN_POINT('',(-0.0165977866640469,-0.0118126828312217,0.0424209700357734));
#45140=CARTESIAN_POINT('',(-0.0195164378422495,-0.0058424867825746,0.0422632018905156));
#45141=CARTESIAN_POINT('',(-0.0202202325281431,-0.00249146300533311,0.0421843160611639));
#45142=CARTESIAN_POINT('',(-0.0199454269988205,0.0041527259998003,0.0420261716512487));
#45143=CARTESIAN_POINT('',(-0.0189673109311248,0.00743418547945166,0.0419472858197865));
#45144=CARTESIAN_POINT('',(-0.0155656138172359,0.0131429701460771,0.041789517681426));
#45145=CARTESIAN_POINT('',(-0.0131451882465153,0.0155649997561152,0.0417106318506291));
#45146=CARTESIAN_POINT('',(-0.00743259156012253,0.0189689687126589,0.0415524874401043));
#45147=CARTESIAN_POINT('',(-0.00415048490179366,0.0199449109496952,0.0414736016091979));
#45148=CARTESIAN_POINT('',(0.00248927022391019,0.020219533415104,0.0413158334710133));
#45149=CARTESIAN_POINT('',(0.00584075953030216,0.0195179588982117,0.0412369476400729));
#45150=CARTESIAN_POINT('',(0.0118149424696186,0.0165973589996381,0.0410788032296136));
#45151=CARTESIAN_POINT('',(0.0144271107866775,0.0143834791361427,0.0409999173987475));
#45152=CARTESIAN_POINT('',(0.0182886173452566,0.00897510297271117,0.0408421492604103));
#45153=CARTESIAN_POINT('',(0.0195343735808227,0.00578562358327755,0.0407632634295357));
#45154=CARTESIAN_POINT('',(0.020356913604267,-0.000813178843569358,0.0406051190190981));
#45155=CARTESIAN_POINT('',(0.0199322482453678,-0.0042108761078978,0.0405262331883193));
#45156=CARTESIAN_POINT('',(0.0175165809193028,-0.0104017013353189,0.0403684650497858));
#45157=CARTESIAN_POINT('',(0.0155278197699022,-0.0131890865732395,0.0402895792190312));
#45158=CARTESIAN_POINT('',(0.0104534103322118,-0.0174868923411122,0.04013143480855));
#45159=CARTESIAN_POINT('',(0.00737670214342564,-0.0189897409987214,0.0400525489777058));
#45160=CARTESIAN_POINT('',(0.000872705995556211,-0.0203534857461097,0.0398947808393469));
#45161=CARTESIAN_POINT('',(-0.00254854873523769,-0.0202131168004107,0.0398158950085049));
#45162=CARTESIAN_POINT('',(-0.00892196654963962,-0.0183156682709116,0.0396577505980237));
#45163=CARTESIAN_POINT('',(-0.0118629009446791,-0.0165619316170496,0.0395788647674302));
#45164=CARTESIAN_POINT('',(-0.0165619310455589,-0.0118629017450905,0.0394210966285696));
#45165=CARTESIAN_POINT('',(-0.0183156678431523,-0.00892196743450048,0.0393422107979038));
#45166=CARTESIAN_POINT('',(-0.0202131166745193,-0.00254854971005675,0.0391840663875722));
#45167=CARTESIAN_POINT('',(-0.0203534857867463,0.000872705012919857,0.0391051805565894));
#45168=CARTESIAN_POINT('',(-0.0189897413562358,0.00737670122719252,0.0389474124183581));
#45169=CARTESIAN_POINT('',(-0.0174868928479001,0.0104534094901412,0.0388685265874864));
#45170=CARTESIAN_POINT('',(-0.0131890873204951,0.0155278191313265,0.0387103821769368));
#45171=CARTESIAN_POINT('',(-0.0104017021802572,0.017516580415848,0.0386314963461393));
#45172=CARTESIAN_POINT('',(-0.00421087707039726,0.0199322480435583,0.0384737282077554));
#45173=CARTESIAN_POINT('',(-0.000813179825758113,0.0203569135679558,0.038394842376862));
#45174=CARTESIAN_POINT('',(0.00578562264002206,0.0195343738571403,0.0382366979665085));
#45175=CARTESIAN_POINT('',(0.00897510208915741,0.0182886177771876,0.0381578121358093));
#45176=CARTESIAN_POINT('',(0.0143834784406977,0.01442711148213,0.0380000439970328));
#45177=CARTESIAN_POINT('',(0.0165973584320769,0.0118149432719776,0.0379211581662922));
#45178=CARTESIAN_POINT('',(0.0195179586135799,0.00584076047113161,0.0377630137560259));
#45179=CARTESIAN_POINT('',(0.0202195332934501,0.002489271199808,0.0376841279251519));
#45180=CARTESIAN_POINT('',(0.0199449111515263,-0.00415048393918659,0.0375263597866371));
#45181=CARTESIAN_POINT('',(0.0189689690739686,-0.00743259064608601,0.0374474739558123));
#45182=CARTESIAN_POINT('',(0.0155650003880389,-0.0131451874936908,0.0372893295454589));
#45183=CARTESIAN_POINT('',(0.0131429708966224,-0.015565613181577,0.0372104437145858));
#45184=CARTESIAN_POINT('',(0.00743418639561038,-0.0189673105736437,0.0370526755762019));
#45185=CARTESIAN_POINT('',(0.00415272696260282,-0.0199454268013481,0.036973789744721));
#45186=CARTESIAN_POINT('',(-0.0024914620294482,-0.0202202326454308,0.0368156453348712));
#45187=CARTESIAN_POINT('',(-0.00584248583997558,-0.0195164381228754,0.0367367595052236));
#45188=CARTESIAN_POINT('',(-0.0118126820307963,-0.0165977872355334,0.0365789913604876));
#45189=CARTESIAN_POINT('',(-0.0144263164154719,-0.0143856381934081,0.0365001055720521));
#45190=CARTESIAN_POINT('',(-0.018290401462013,-0.00897365056498236,0.0363419611234327));
#45191=CARTESIAN_POINT('',(-0.0195340447348365,-0.00578334668312191,0.0362630752468074));
#45192=CARTESIAN_POINT('',(-0.0203560362812166,0.000811052889691331,0.0361053073977451));
#45193=CARTESIAN_POINT('',(-0.0199336168504544,0.0042090275394474,0.0360264198296735));
#45194=CARTESIAN_POINT('',(-0.0175163464674805,0.0104039888314446,0.0358682771450641));
#45195=CARTESIAN_POINT('',(-0.0155257113958446,0.0131900637175812,0.035789391583042));
#45196=CARTESIAN_POINT('',(-0.0104546932247947,0.0174849605803254,0.0356316164551422));
#45197=CARTESIAN_POINT('',(-0.00737924043715088,0.01899007524981,0.0355527701832371));
#45198=CARTESIAN_POINT('',(-0.000870261431598303,0.0203543744029426,0.0353945787640066));
#45199=CARTESIAN_POINT('',(0.00254961361012549,0.02021239652742,0.0353157310768663));
#45200=CARTESIAN_POINT('',(0.00891864446487162,0.0183169789881492,0.035158015862421));
#45201=CARTESIAN_POINT('',(0.0118711468820354,0.0165545454869355,0.0350787075431251));
#45202=CARTESIAN_POINT('',(0.0144739176610643,0.0139517749677388,0.034991182120757));
#45203=CARTESIAN_POINT('',(0.014723509957734,0.0136876030217121,0.0349823026500466));
#45204=CARTESIAN_POINT('',(0.0149659317995843,0.0134243912328982,0.0349733181014439));
#45205=CARTESIAN_POINT('',(0.0134323507348915,0.014958390148285,0.0444630144047823));
#45206=CARTESIAN_POINT('',(0.0136955623892009,0.0147159683298484,0.0444540298589685));
#45207=CARTESIAN_POINT('',(0.0139603501643897,0.0144656208027388,0.0444451248216824));
#45208=CARTESIAN_POINT('',(0.0165671823597683,0.0118560003406502,0.0443574029042448));
#45209=CARTESIAN_POINT('',(0.0183218821358191,0.00890866553410848,0.0442783127187353));
#45210=CARTESIAN_POINT('',(0.0202137781832282,0.00253858404797499,0.044120597572689));
#45211=CARTESIAN_POINT('',(0.0203538735514792,-0.000881359440271408,0.0440417497916532));
#45212=CARTESIAN_POINT('',(0.0189860992971344,-0.0073896126699635,0.0438835584015622));
#45213=CARTESIAN_POINT('',(0.0174792752695404,-0.0104642451029217,0.043804712154686));
#45214=CARTESIAN_POINT('',(0.0131815865514812,-0.0155329020177859,0.0436469370197732));
#45215=CARTESIAN_POINT('',(0.0103944245524534,-0.0175219976723892,0.0435680514389131));
#45216=CARTESIAN_POINT('',(0.00419816641268413,-0.0199359515386241,0.0434099087505035));
#45217=CARTESIAN_POINT('',(0.000799946546492838,-0.0203565035039386,0.0433310212088694));
#45218=CARTESIAN_POINT('',(-0.00579400288494992,-0.0195308803243074,0.0431732533614397));
#45219=CARTESIAN_POINT('',(-0.00898361275583876,-0.0182854854811773,0.0430943674587492));
#45220=CARTESIAN_POINT('',(-0.0143935335247905,-0.014418501217132,0.042936223008582));
#45221=CARTESIAN_POINT('',(-0.0166042528904406,-0.0118036396773023,0.0428573372467254));
#45222=CARTESIAN_POINT('',(-0.0195196173960083,-0.00583183406508102,0.0426995691023438));
#45223=CARTESIAN_POINT('',(-0.0202215659519979,-0.00248043323127719,0.0426206832474583));
#45224=CARTESIAN_POINT('',(-0.0199432025025457,0.0041636111764046,0.0424625388358018));
#45225=CARTESIAN_POINT('',(-0.0189632769981644,0.0074445449248028,0.0423836530307362));
#45226=CARTESIAN_POINT('',(-0.0155584347698434,0.0131514584457935,0.0422258848932583));
#45227=CARTESIAN_POINT('',(-0.013136683803135,0.0155721487684907,0.042146999036921));
#45228=CARTESIAN_POINT('',(-0.0074222621711207,0.0189730600664392,0.0419888546246593));
#45229=CARTESIAN_POINT('',(-0.0041396059692075,0.0199471999558189,0.0419099688201486));
#45230=CARTESIAN_POINT('',(0.00250030291063802,0.0202181660171394,0.0417522006828445));
#45231=CARTESIAN_POINT('',(0.00585139593345808,0.0195147494024473,0.0416733148263639));
#45232=CARTESIAN_POINT('',(0.0118240172541425,0.0165909493398389,0.0415151704141697));
#45233=CARTESIAN_POINT('',(0.0144349772779972,0.0143756236261366,0.0414362846096961));
#45234=CARTESIAN_POINT('',(0.0182935069132192,0.00896511888142835,0.0412785164722437));
#45235=CARTESIAN_POINT('',(0.0195375042596792,0.0057749637153101,0.0411996306158288));
#45236=CARTESIAN_POINT('',(0.0203565110886193,-0.00082428170059236,0.0410414862036521));
#45237=CARTESIAN_POINT('',(0.0199299744386224,-0.00422175822745308,0.0409626003992711));
#45238=CARTESIAN_POINT('',(0.017510896912993,-0.0104112554980561,0.040804832261616));
#45239=CARTESIAN_POINT('',(0.0155206080048174,-0.0131975378677864,0.0407259464053232));
#45240=CARTESIAN_POINT('',(0.0104438952373011,-0.0174926280557002,0.040567801993105));
#45241=CARTESIAN_POINT('',(0.00736634834331694,-0.0189937893992192,0.0404889161886566));
#45242=CARTESIAN_POINT('',(0.000861598713996071,-0.0203539529182404,0.0403311480511781));
#45243=CARTESIAN_POINT('',(-0.002559568337358,-0.0202117017724119,0.0402522621948001));
#45244=CARTESIAN_POINT('',(-0.00893197256125958,-0.0183108396909511,0.0400941177825755));
#45245=CARTESIAN_POINT('',(-0.0118719531216823,-0.0165554780277981,0.0400152319783788));
#45246=CARTESIAN_POINT('',(-0.0165683972536806,-0.0118538586203137,0.039857463840403));
#45247=CARTESIAN_POINT('',(-0.0183205103802491,-0.0089119682460497,0.039778577984198));
#45248=CARTESIAN_POINT('',(-0.0202145471188442,-0.00253753202962592,0.039620433572125));
#45249=CARTESIAN_POINT('',(-0.0203530341298277,0.000883812970843685,0.0395415477675402));
#45250=CARTESIAN_POINT('',(-0.0189857074358077,0.00738706064028674,0.0393837796301893));
#45251=CARTESIAN_POINT('',(-0.0174811704792471,0.0104629325375536,0.0393048937737806));
#45252=CARTESIAN_POINT('',(-0.013180646066677,0.0155350427514035,0.0391467493614896));
#45253=CARTESIAN_POINT('',(-0.0103921559373152,0.0175222777809261,0.0390678635570879));
#45254=CARTESIAN_POINT('',(-0.00419999817167859,0.019934537042528,0.0389100954195888));
#45255=CARTESIAN_POINT('',(-0.000802077610691454,0.0203573316060118,0.0388312095631551));
#45256=CARTESIAN_POINT('',(0.00579628694082303,0.0195312580680787,0.0386730651510625));
#45257=CARTESIAN_POINT('',(0.0089850930321539,0.0182837421458691,0.0385941793467601));
#45258=CARTESIAN_POINT('',(0.0143913449075759,0.0144192559966424,0.0384364112088641));
#45259=CARTESIAN_POINT('',(0.0166037807356177,0.0118058775148413,0.0383575253525841));
#45260=CARTESIAN_POINT('',(0.019521182999093,0.00583012850089137,0.0381993809405809));
#45261=CARTESIAN_POINT('',(0.020220916106271,0.00247824039966869,0.0381204951361016));
#45262=CARTESIAN_POINT('',(0.0199426373519245,-0.00416136602487085,0.0379627269984695));
#45263=CARTESIAN_POINT('',(0.0189648921930783,-0.00744292568248877,0.0378838411421065));
#45264=CARTESIAN_POINT('',(0.0155578632306798,-0.0131537019776971,0.0377256967300117));
#45265=CARTESIAN_POINT('',(0.0131344926074458,-0.0155728041019498,0.0376468109255366));
#45266=CARTESIAN_POINT('',(0.00742383262774643,-0.0189713589615301,0.0374890427880331));
#45267=CARTESIAN_POINT('',(0.00414184497409428,-0.0199476665026562,0.0374101569310133));
#45268=CARTESIAN_POINT('',(-0.00250249372509033,-0.020218914637921,0.0372520125194265));
#45269=CARTESIAN_POINT('',(-0.00585314302193221,-0.0195132734436152,0.0371731267161692));
#45270=CARTESIAN_POINT('',(-0.0118217341805558,-0.0165913336681314,0.0370153585723223));
#45271=CARTESIAN_POINT('',(-0.0144341432910962,-0.0143777531493217,0.036936472758358));
#45272=CARTESIAN_POINT('',(-0.0182953318355289,-0.00896369431626748,0.0367783283079389));
#45273=CARTESIAN_POINT('',(-0.0195372243200628,-0.00577269393669329,0.0366994424579409));
#45274=CARTESIAN_POINT('',(-0.0203555845359782,0.000822160822673886,0.0365416746094756));
#45275=CARTESIAN_POINT('',(-0.019931297161379,0.00421989281550488,0.0364627870155816));
#45276=CARTESIAN_POINT('',(-0.017510708109202,0.0104135619093506,0.0363046443312881));
#45277=CARTESIAN_POINT('',(-0.0155185319662571,0.0131985516976792,0.036225758788908));
#45278=CARTESIAN_POINT('',(-0.0104451484813017,0.0174906597179114,0.0360679836698519));
#45279=CARTESIAN_POINT('',(-0.00736887293488479,0.0189940660278109,0.0359891373740166));
#45280=CARTESIAN_POINT('',(-0.000859163080617291,0.0203548908221539,0.0358309459219546));
#45281=CARTESIAN_POINT('',(0.0025606460952816,0.0202110301583723,0.0357520983297262));
#45282=CARTESIAN_POINT('',(0.00892863107146433,0.0183120893739606,0.0355943830488878));
#45283=CARTESIAN_POINT('',(0.011880166085103,0.0165480585058836,0.0355150747162368));
#45284=CARTESIAN_POINT('',(0.0144815426313042,0.0139438917715042,0.0354275493279347));
#45285=CARTESIAN_POINT('',(0.0147310582798273,0.0136796566260476,0.0354186699986407));
#45286=CARTESIAN_POINT('',(0.0149734784198071,0.0134164466850558,0.0354096855131117));
#45287=CARTESIAN_POINT('',(0.0132774325567157,0.0147734032199086,0.0449158584910965));
#45288=CARTESIAN_POINT('',(0.0135391077187239,0.0145323965335079,0.0449069263923718));
#45289=CARTESIAN_POINT('',(0.0138014039135308,0.0142842302640092,0.0448980501159253));
#45290=CARTESIAN_POINT('',(0.0163749972709665,0.011704953790514,0.0448103694939715));
#45291=CARTESIAN_POINT('',(0.0181074530777823,0.00879152021484105,0.0447312665590919));
#45292=CARTESIAN_POINT('',(0.0199730255068591,0.00249651795811219,0.0445735198851828));
#45293=CARTESIAN_POINT('',(0.0201093666845512,-0.000882833009343425,0.0444946545146255));
#45294=CARTESIAN_POINT('',(0.0187544866881982,-0.00731160469610085,0.0443365250922151));
#45295=CARTESIAN_POINT('',(0.0172639601138449,-0.0103487409519681,0.0442576584501176));
#45296=CARTESIAN_POINT('',(0.0130146079248891,-0.0153544536244878,0.0440998569695397));
#45297=CARTESIAN_POINT('',(0.0102595012097063,-0.0173180914728919,0.0440209577525291));
#45298=CARTESIAN_POINT('',(0.00413677952879929,-0.0196993834358412,0.0438628694096752));
#45299=CARTESIAN_POINT('',(0.000778873719066263,-0.0201130760903658,0.0437839687687258));
#45300=CARTESIAN_POINT('',(-0.00573593586137178,-0.0192934896015891,0.0436261731415959));
#45301=CARTESIAN_POINT('',(-0.00888670629679085,-0.0180610055096835,0.0435472737494208));
#45302=CARTESIAN_POINT('',(-0.0142290621595103,-0.0142377202406875,0.0433891839738936));
#45303=CARTESIAN_POINT('',(-0.0164119892680786,-0.0116528560195468,0.0433102847563008));
#45304=CARTESIAN_POINT('',(-0.0192891222321422,-0.00575060537461488,0.0431524888939648));
#45305=CARTESIAN_POINT('',(-0.0199806360344781,-0.00243878116859957,0.043073589537792));
#45306=CARTESIAN_POINT('',(-0.0197019014047589,0.0041247990854508,0.0429154997933989));
#45307=CARTESIAN_POINT('',(-0.0187318877423047,0.0073660591097996,0.0428366005414287));
#45308=CARTESIAN_POINT('',(-0.0153643639269432,0.0130029235040371,0.042678804684548));
#45309=CARTESIAN_POINT('',(-0.0129700379181249,0.0153932318367515,0.0425999053272683));
#45310=CARTESIAN_POINT('',(-0.0073227751616878,0.0187498226748011,0.0424418155823795));
#45311=CARTESIAN_POINT('',(-0.0040787537352243,0.0197105609554491,0.0423629163308548));
#45312=CARTESIAN_POINT('',(0.00248210112658439,0.019974455500205,0.0422051204741111));
#45313=CARTESIAN_POINT('',(0.00579275933568636,0.0192773807675007,0.0421262211167112));
#45314=CARTESIAN_POINT('',(0.0116915446297296,0.0163855628703383,0.0419681313718886));
#45315=CARTESIAN_POINT('',(0.0142701540567164,0.0141952509103176,0.0418892321203894));
#45316=CARTESIAN_POINT('',(0.0180795252057958,0.00884705978653905,0.0417314362635233));
#45317=CARTESIAN_POINT('',(0.0193067160163676,0.00569422397168671,0.0416525369061795));
#45318=CARTESIAN_POINT('',(0.0201121127633341,-0.000825715811345802,0.0414944471613675));
#45319=CARTESIAN_POINT('',(0.0196888226900121,-0.00418242827643942,0.0414155479099439));
#45320=CARTESIAN_POINT('',(0.0172950248955886,-0.01029668939015,0.0412577520529161));
#45321=CARTESIAN_POINT('',(0.0153267861934022,-0.0130484901409762,0.041178852695677));
#45322=CARTESIAN_POINT('',(0.0103090214339838,-0.0172888103546578,0.0410207629508175));
#45323=CARTESIAN_POINT('',(0.00726737655517426,-0.0187703937948799,0.0409418636993504));
#45324=CARTESIAN_POINT('',(0.000839438816763122,-0.0201105703799344,0.0407840678424572));
#45325=CARTESIAN_POINT('',(-0.00254080105956695,-0.0199679192694803,0.0407051684851519));
#45326=CARTESIAN_POINT('',(-0.00883511219257549,-0.0180864501478478,0.0405470787402899));
#45327=CARTESIAN_POINT('',(-0.0117390662474826,-0.0163504363500681,0.0404681794890089));
#45328=CARTESIAN_POINT('',(-0.0163767658662786,-0.0117021894662202,0.0403103836317459));
#45329=CARTESIAN_POINT('',(-0.0181061591128077,-0.00879434319095104,0.04023148427456));
#45330=CARTESIAN_POINT('',(-0.0199737181150179,-0.00249589083605073,0.0400733945298292));
#45331=CARTESIAN_POINT('',(-0.020108697879637,0.000884711702365825,0.0399944952782453));
#45332=CARTESIAN_POINT('',(-0.0187539226697023,0.00730958843101573,0.0398366994214571));
#45333=CARTESIAN_POINT('',(-0.017265459695178,0.0103478196490916,0.0397578000641271));
#45334=CARTESIAN_POINT('',(-0.0130140644752542,0.015356204356557,0.0395997103192093));
#45335=CARTESIAN_POINT('',(-0.0102577642874015,0.0173182192223741,0.0395208110677819));
#45336=CARTESIAN_POINT('',(-0.00413808105738116,0.0196981213240248,0.0393630152108678));
#45337=CARTESIAN_POINT('',(-0.000780463646085143,0.0201137849862969,0.039284115853516));
#45338=CARTESIAN_POINT('',(0.00573768092622813,0.0192939862131531,0.0391260261087678));
#45339=CARTESIAN_POINT('',(0.00888776731266,0.0180596245087814,0.0390471268574055));
#45340=CARTESIAN_POINT('',(0.0142272910447909,0.0142381139224078,0.0388893310001916));
#45341=CARTESIAN_POINT('',(0.0164117133878414,0.0116545756531483,0.0388104316429529));
#45342=CARTESIAN_POINT('',(0.0192904925041646,0.00574941608770125,0.0386523418982784));
#45343=CARTESIAN_POINT('',(0.0199800602103527,0.00243713750068655,0.0385734426467758));
#45344=CARTESIAN_POINT('',(0.0197012623214353,-0.00412310095417178,0.0384156467897683));
#45345=CARTESIAN_POINT('',(0.0187331764642615,-0.00736488761193141,0.0383367474324733));
#45346=CARTESIAN_POINT('',(0.0153641177626821,-0.0130047211342287,0.0381786576877099));
#45347=CARTESIAN_POINT('',(0.0129683469496416,-0.0153936487746862,0.0380997584362191));
#45348=CARTESIAN_POINT('',(0.00732384723385657,-0.0187483588673528,0.0379419625793142));
#45349=CARTESIAN_POINT('',(0.00408043933965481,-0.0197109990832421,0.0378630632214872));
#45350=CARTESIAN_POINT('',(-0.00248374068359378,-0.0199752326289125,0.0377049734771552));
#45351=CARTESIAN_POINT('',(-0.00579403324945224,-0.0192761931914336,0.0376260742265771));
#45352=CARTESIAN_POINT('',(-0.0116897328046641,-0.0163856597591573,0.0374682783646604));
#45353=CARTESIAN_POINT('',(-0.0142695989494591,-0.0141969015908406,0.0373893790411247));
#45354=CARTESIAN_POINT('',(-0.0180810724819061,-0.00884611231053172,0.0372312892652485));
#45355=CARTESIAN_POINT('',(-0.0193064187306797,-0.0056925080040017,0.0371523899800911));
#45356=CARTESIAN_POINT('',(-0.0201112032241304,0.000824146644046457,0.0369945943514264));
#45357=CARTESIAN_POINT('',(-0.0196898977667719,0.00418105816284977,0.0369156936037029));
#45358=CARTESIAN_POINT('',(-0.0172950832261643,0.0102985033413524,0.0367576052691976));
#45359=CARTESIAN_POINT('',(-0.0153251673105889,0.0130491830686049,0.0366787061305392));
#45360=CARTESIAN_POINT('',(-0.0103098218392397,0.0172871617375925,0.0365209046824581));
#45361=CARTESIAN_POINT('',(-0.00726933690112621,0.018770722967874,0.036442037940343));
#45362=CARTESIAN_POINT('',(-0.00083759659875895,0.0201114398926357,0.0362839083919405));
#45363=CARTESIAN_POINT('',(0.00254148063827732,0.0199674250037726,0.0362050434060442));
#45364=CARTESIAN_POINT('',(0.00883221018549675,0.0180874953282551,0.0360472964574278));
#45365=CARTESIAN_POINT('',(0.0117477586613136,0.0163424685172153,0.0359679780033833));
#45366=CARTESIAN_POINT('',(0.0143159619590558,0.0137685786180237,0.0358804910529425));
#45367=CARTESIAN_POINT('',(0.014563145781723,0.0135066960806843,0.0358716402000459));
#45368=CARTESIAN_POINT('',(0.0148041471746711,0.0132450265576457,0.0358627082955947));
#45369=CARTESIAN_POINT('',(0.0129138508916869,0.0143725930875827,0.0450790488739469));
#45370=CARTESIAN_POINT('',(0.0131720706341788,0.0141347688934417,0.0450702347235489));
#45371=CARTESIAN_POINT('',(0.0134288924071795,0.0138916521969391,0.0450614233363915));
#45372=CARTESIAN_POINT('',(0.0159305442659458,0.0113832729646018,0.0449738355536919));
#45373=CARTESIAN_POINT('',(0.0176161543656036,0.00854789414688023,0.0448947039506003));
#45374=CARTESIAN_POINT('',(0.0194294856532803,0.00242360909110657,0.0447368863175001));
#45375=CARTESIAN_POINT('',(0.0195610782100481,-0.000864419420761024,0.0446579816168119));
#45376=CARTESIAN_POINT('',(0.0182419666895939,-0.00711606163363783,0.0444999913442412));
#45377=CARTESIAN_POINT('',(0.0167913972841028,-0.0100705709602299,0.0444210788362177));
#45378=CARTESIAN_POINT('',(0.0126560949175306,-0.0149395055174694,0.0442632181858345));
#45379=CARTESIAN_POINT('',(0.00997512630113625,-0.0168489673916814,0.0441842883728412));
#45380=CARTESIAN_POINT('',(0.00402013804374216,-0.0191633784369803,0.0440263221211558));
#45381=CARTESIAN_POINT('',(0.000753275155927111,-0.0195653175752822,0.0439473920012669));
#45382=CARTESIAN_POINT('',(-0.00558463299752592,-0.0187664008856396,0.0437895339665373));
#45383=CARTESIAN_POINT('',(-0.00864951164828749,-0.0175663485840429,0.043710604321552));
#45384=CARTESIAN_POINT('',(-0.0138441331044444,-0.0138469053737105,0.0435526373723547));
#45385=CARTESIAN_POINT('',(-0.0159674252333963,-0.0113318302923382,0.0434737078756761));
#45386=CARTESIAN_POINT('',(-0.018765106459829,-0.00558898075670583,0.0433158497450324));
#45387=CARTESIAN_POINT('',(-0.0194367926615482,-0.00236680089305438,0.0432369201090668));
#45388=CARTESIAN_POINT('',(-0.0191641880564002,0.00401630485958065,0.043078953174557));
#45389=CARTESIAN_POINT('',(-0.0182199822859882,0.00716946943245308,0.0430000236633192));
#45390=CARTESIAN_POINT('',(-0.0149424477523284,0.0126526353535143,0.0428421655348627));
#45391=CARTESIAN_POINT('',(-0.0126123243137451,0.0149773138742785,0.0427632358985783));
#45392=CARTESIAN_POINT('',(-0.00711950156511704,0.0182403263678245,0.0426052689638103));
#45393=CARTESIAN_POINT('',(-0.00396334627656238,0.0191744865054583,0.0425263394527732));
#45394=CARTESIAN_POINT('',(0.00241961790374605,0.0194296519634247,0.0423684813243768));
#45395=CARTESIAN_POINT('',(0.00564021755686893,0.018750429365584,0.0422895516880225));
#45396=CARTESIAN_POINT('',(0.0113761915199589,0.015936720962703,0.0421315847533152));
#45397=CARTESIAN_POINT('',(0.0138844923942741,0.0138054307215434,0.042052655242283));
#45398=CARTESIAN_POINT('',(0.0175892588639255,0.00860138935517418,0.0418947971138141));
#45399=CARTESIAN_POINT('',(0.0187821375220497,0.00553371173675391,0.041815867477496));
#45400=CARTESIAN_POINT('',(0.0195638755616741,-0.000807206013704218,0.041657900542789));
#45401=CARTESIAN_POINT('',(0.0191515413594767,-0.0040727766949323,0.0415789710317868));
#45402=CARTESIAN_POINT('',(0.0168212075730868,-0.0100206238332644,0.0414211129032577));
#45403=CARTESIAN_POINT('',(0.0149054934897077,-0.012697122481573,0.0413421832670016));
#45404=CARTESIAN_POINT('',(0.0100246598884266,-0.0168197206475598,0.0411842163322308));
#45405=CARTESIAN_POINT('',(0.00706530814937353,-0.0182606261450326,0.0411052868212415));
#45406=CARTESIAN_POINT('',(0.000811398134958812,-0.0195629128528423,0.0409474286927504));
#45407=CARTESIAN_POINT('',(-0.00247707310188533,-0.0194230472462728,0.0408684990564665));
#45408=CARTESIAN_POINT('',(-0.00859793703807817,-0.0175918244429124,0.0407105321217132));
#45409=CARTESIAN_POINT('',(-0.0114228268016637,-0.0159024549772322,0.0406316026107603));
#45410=CARTESIAN_POINT('',(-0.0159336221423258,-0.0113791744716903,0.0404737444821789));
#45411=CARTESIAN_POINT('',(-0.0176151546309675,-0.0085496773513497,0.0403948148459005));
#45412=CARTESIAN_POINT('',(-0.0194299115416473,-0.00242391130659293,0.0402368479112266));
#45413=CARTESIAN_POINT('',(-0.0195606963090452,0.00086498922598336,0.0401579184001611));
#45414=CARTESIAN_POINT('',(-0.0182411287006575,0.0071152758165584,0.0400000602717256));
#45415=CARTESIAN_POINT('',(-0.0167920796589088,0.0100705866865345,0.0399211306354328));
#45416=CARTESIAN_POINT('',(-0.0126563716223977,0.014940316793741,0.0397631637006416));
#45417=CARTESIAN_POINT('',(-0.00997454683381245,0.0168486635053003,0.0396842341896759));
#45418=CARTESIAN_POINT('',(-0.0040202813476444,0.019162548476316,0.0395263760611581));
#45419=CARTESIAN_POINT('',(-0.00075363945007261,0.0195658550302225,0.0394474464248561));
#45420=CARTESIAN_POINT('',(0.00558515324695027,0.0187670688107491,0.0392894794901657));
#45421=CARTESIAN_POINT('',(0.00864957627121354,0.0175657017159631,0.0392105499791872));
#45422=CARTESIAN_POINT('',(0.0138433577443138,0.0138465653716977,0.0390526918505942));
#45423=CARTESIAN_POINT('',(0.0159676762407863,0.011332430055188,0.0389737622143119));
#45424=CARTESIAN_POINT('',(0.0187659501848109,0.00558891064506963,0.0388157952796574));
#45425=CARTESIAN_POINT('',(0.0194362864539758,0.00236639289421834,0.0387368657686242));
#45426=CARTESIAN_POINT('',(0.0191634793886099,-0.00401584162374749,0.0385790076401043));
#45427=CARTESIAN_POINT('',(0.0182206216688099,-0.00716935153876095,0.0385000780038236));
#45428=CARTESIAN_POINT('',(0.0149428505310971,-0.0126533800442663,0.0383421110690947));
#45429=CARTESIAN_POINT('',(0.0126117058821609,-0.0149771132462627,0.0382631815580843));
#45430=CARTESIAN_POINT('',(0.00711950176515704,-0.0182394797302009,0.0381053234296125));
#45431=CARTESIAN_POINT('',(0.00396379468394748,-0.0191749572951896,0.0380263937930821));
#45432=CARTESIAN_POINT('',(-0.002420021036381,-0.0194303964622404,0.0378684268586038));
#45433=CARTESIAN_POINT('',(-0.00564038784424458,-0.0187498019041688,0.0377894973478354));
#45434=CARTESIAN_POINT('',(-0.0113754826268754,-0.0159362580769357,0.0376316392173264));
#45435=CARTESIAN_POINT('',(-0.0138846413112407,-0.0138060635195378,0.0375527095953789));
#45436=CARTESIAN_POINT('',(-0.0175901025577762,-0.00860145913332057,0.0373947426458515));
#45437=CARTESIAN_POINT('',(-0.0187817055459195,-0.00553322593065883,0.0373158131273598));
#45438=CARTESIAN_POINT('',(-0.0195631005983065,0.000806866293556,0.0371579550911043));
#45439=CARTESIAN_POINT('',(-0.0191521499202236,0.00407255220458082,0.0370790248446952));
#45440=CARTESIAN_POINT('',(-0.01682173172892,0.0100212944823637,0.0369210586028574));
#45441=CARTESIAN_POINT('',(-0.0149048382880035,0.0126970227189995,0.0368421288825937));
#45442=CARTESIAN_POINT('',(-0.0100245010513865,0.0168188618539805,0.0366842682707503));
#45443=CARTESIAN_POINT('',(-0.00706602777302647,0.0182611861391709,0.0366053556442268));
#45444=CARTESIAN_POINT('',(-0.000810871506560531,0.0195635323386266,0.0364473652226556));
#45445=CARTESIAN_POINT('',(0.00247683298098486,0.0194228561427848,0.0363684609772384));
#45446=CARTESIAN_POINT('',(0.00859606028164421,0.0175925296827086,0.0362106430189561));
#45447=CARTESIAN_POINT('',(0.0114326608091759,0.0158933207565089,0.0361313018539961));
#45448=CARTESIAN_POINT('',(0.0139290714571154,0.0133901785987586,0.0360439011850484));
#45449=CARTESIAN_POINT('',(0.0141711670058611,0.0131337047426488,0.0360351140257455));
#45450=CARTESIAN_POINT('',(0.0144089846063591,0.012875492052252,0.0360263001178339));
#45451=CARTESIAN_POINT('',(0.,0.,0.0334));
#45452=CARTESIAN_POINT('',(0.,0.,0.0487));
#45453=CARTESIAN_POINT('',(0.,0.,0.0499));
#45454=CARTESIAN_POINT('',(0.,0.,0.048900001));
#45463=MECHANICAL_DESIGN_GEOMETRIC_PRESENTATION_REPRESENTATION('',(#13554),#45464);
#45464=(
GEOMETRIC_REPRESENTATION_CONTEXT(3)
GLOBAL_UNCERTAINTY_ASSIGNED_CONTEXT((#45492))
GLOBAL_UNIT_ASSIGNED_CONTEXT((#45522,#45521,#45520))
REPRESENTATION_CONTEXT('MAS-690','TOP_LEVEL_ASSEMBLY_PART')
);
#45490=(
GEOMETRIC_REPRESENTATION_CONTEXT(3)
GLOBAL_UNCERTAINTY_ASSIGNED_CONTEXT((#45518))
GLOBAL_UNIT_ASSIGNED_CONTEXT((#45522,#45521,#45520))
REPRESENTATION_CONTEXT('Bottle_Cap','COMPONENT_PART')
);
#45492=UNCERTAINTY_MEASURE_WITH_UNIT(LENGTH_MEASURE(1.E-8),#45522,
'DISTANCE_ACCURACY_VALUE','Maximum Tolerance applied to model');
#45518=UNCERTAINTY_MEASURE_WITH_UNIT(LENGTH_MEASURE(2.E-5),#45522,
'DISTANCE_ACCURACY_VALUE','Maximum Tolerance applied to model');
#45520=(
NAMED_UNIT(*)
SI_UNIT($,.STERADIAN.)
SOLID_ANGLE_UNIT()
);
#45521=(
NAMED_UNIT(*)
PLANE_ANGLE_UNIT()
SI_UNIT($,.RADIAN.)
);
#45522=(
LENGTH_UNIT()
NAMED_UNIT(*)
SI_UNIT($,.METRE.)
);
#45581=PRODUCT_DEFINITION_SHAPE('','',#45611);
#45611=PRODUCT_DEFINITION('','',#45667,#45639);
#45639=PRODUCT_DEFINITION_CONTEXT('',#45782,'design');
#45667=PRODUCT_DEFINITION_FORMATION_WITH_SPECIFIED_SOURCE('','',#45723,
 .NOT_KNOWN.);
#45723=PRODUCT('Bottle_Cap','Bottle_Cap','Bottle_Cap',(#45779));
#45779=PRODUCT_CONTEXT('',#45782,'mechanical');
#45782=APPLICATION_CONTEXT('managed model based 3d engineering');
ENDSEC;
END-ISO-10303-21;
